ISO-10303-21;
HEADER;
/* Generated by software containing ST-Developer
 * from STEP Tools, Inc. (www.steptools.com) 
 */

FILE_DESCRIPTION(
/* description */ (''),
/* implementation_level */ '2;1');

FILE_NAME(
/* name */ '06_Thrust_Bearing.step',
/* time_stamp */ '2026-10-25T01:10:36-07:00',
/* author */ (''),
/* organization */ (''),
/* preprocessor_version */ 'ST-DEVELOPER v20.2',
/* originating_system */ 'Autodesk Translation Framework v15.15.0.0',
/* authorisation */ '');

FILE_SCHEMA (('AUTOMOTIVE_DESIGN { 1 0 10303 214 3 1 1 }'));
ENDSEC;

DATA;
#10=MECHANICAL_DESIGN_GEOMETRIC_PRESENTATION_REPRESENTATION('',(#1298),#60365);
#70=SHAPE_REPRESENTATION_RELATIONSHIP('SRR','None',#60410,#80);
#80=ADVANCED_BREP_SHAPE_REPRESENTATION('',(#90),#60358);
#90=MANIFOLD_SOLID_BREP('Body1',#18300);
#208=FACE_BOUND('',#2627,.T.);
#209=FACE_BOUND('',#2630,.T.);
#210=FACE_BOUND('',#2631,.T.);
#211=FACE_BOUND('',#2632,.T.);
#212=FACE_BOUND('',#2633,.T.);
#213=FACE_BOUND('',#2634,.T.);
#214=FACE_BOUND('',#2635,.T.);
#215=FACE_BOUND('',#2636,.T.);
#216=FACE_BOUND('',#2637,.T.);
#217=FACE_BOUND('',#2638,.T.);
#218=FACE_BOUND('',#2639,.T.);
#219=FACE_BOUND('',#2646,.T.);
#220=FACE_BOUND('',#2647,.T.);
#221=FACE_BOUND('',#2648,.T.);
#222=FACE_BOUND('',#2649,.T.);
#223=FACE_BOUND('',#2650,.T.);
#224=FACE_BOUND('',#2651,.T.);
#225=FACE_BOUND('',#2652,.T.);
#226=FACE_BOUND('',#2653,.T.);
#227=FACE_BOUND('',#2654,.T.);
#228=FACE_BOUND('',#2655,.T.);
#403=PLANE('',#18939);
#404=PLANE('',#18940);
#405=PLANE('',#18942);
#406=PLANE('',#18943);
#407=PLANE('',#18951);
#408=PLANE('',#18955);
#409=PLANE('',#18956);
#410=PLANE('',#18957);
#411=PLANE('',#18981);
#412=PLANE('',#18982);
#413=PLANE('',#18983);
#414=PLANE('',#18984);
#415=PLANE('',#18985);
#416=PLANE('',#18986);
#417=PLANE('',#18987);
#418=PLANE('',#18988);
#419=PLANE('',#18989);
#420=PLANE('',#18990);
#421=PLANE('',#18991);
#422=PLANE('',#18992);
#423=PLANE('',#18993);
#424=PLANE('',#18994);
#425=PLANE('',#18995);
#426=PLANE('',#18996);
#427=PLANE('',#18997);
#428=PLANE('',#18998);
#429=PLANE('',#18999);
#430=PLANE('',#19000);
#431=PLANE('',#19001);
#432=PLANE('',#19002);
#433=PLANE('',#19003);
#434=PLANE('',#19004);
#435=PLANE('',#19005);
#436=PLANE('',#19006);
#437=PLANE('',#19007);
#438=PLANE('',#19008);
#439=PLANE('',#19009);
#440=PLANE('',#19010);
#441=PLANE('',#19011);
#442=PLANE('',#19012);
#443=PLANE('',#19013);
#444=PLANE('',#19014);
#445=PLANE('',#19015);
#446=PLANE('',#19016);
#447=PLANE('',#19017);
#448=PLANE('',#19018);
#449=PLANE('',#19019);
#450=PLANE('',#19020);
#451=PLANE('',#19021);
#452=PLANE('',#19022);
#453=PLANE('',#19023);
#454=PLANE('',#19024);
#455=PLANE('',#19025);
#456=PLANE('',#19026);
#457=PLANE('',#19027);
#458=PLANE('',#19028);
#459=PLANE('',#19029);
#460=PLANE('',#19030);
#461=PLANE('',#19031);
#462=PLANE('',#19032);
#463=PLANE('',#19033);
#464=PLANE('',#19034);
#465=PLANE('',#19035);
#466=PLANE('',#19036);
#467=PLANE('',#19037);
#468=PLANE('',#19038);
#469=PLANE('',#19039);
#470=PLANE('',#19040);
#471=PLANE('',#19041);
#472=PLANE('',#19042);
#473=PLANE('',#19043);
#474=PLANE('',#19044);
#475=PLANE('',#19045);
#476=PLANE('',#19046);
#477=PLANE('',#19047);
#478=PLANE('',#19048);
#479=PLANE('',#19049);
#480=PLANE('',#19050);
#481=PLANE('',#19051);
#482=PLANE('',#19052);
#483=PLANE('',#19053);
#484=PLANE('',#19054);
#485=PLANE('',#19055);
#486=PLANE('',#19056);
#487=PLANE('',#19057);
#488=PLANE('',#19058);
#489=PLANE('',#19059);
#490=PLANE('',#19060);
#491=PLANE('',#19061);
#492=PLANE('',#19062);
#493=PLANE('',#19063);
#494=PLANE('',#19064);
#495=PLANE('',#19065);
#496=PLANE('',#19066);
#497=PLANE('',#19067);
#498=PLANE('',#19068);
#499=PLANE('',#19069);
#500=PLANE('',#19070);
#501=PLANE('',#19071);
#502=PLANE('',#19072);
#503=PLANE('',#19073);
#504=PLANE('',#19074);
#505=PLANE('',#19075);
#506=PLANE('',#19076);
#507=PLANE('',#19077);
#508=PLANE('',#19078);
#509=PLANE('',#19079);
#510=PLANE('',#19080);
#511=PLANE('',#19081);
#512=PLANE('',#19082);
#513=PLANE('',#19083);
#514=PLANE('',#19084);
#515=PLANE('',#19085);
#516=PLANE('',#19086);
#517=PLANE('',#19087);
#518=PLANE('',#19088);
#519=PLANE('',#19089);
#520=PLANE('',#19090);
#521=PLANE('',#19091);
#522=PLANE('',#19092);
#523=PLANE('',#19093);
#524=PLANE('',#19094);
#525=PLANE('',#19095);
#526=PLANE('',#19096);
#527=PLANE('',#19097);
#528=PLANE('',#19098);
#529=PLANE('',#19099);
#530=PLANE('',#19100);
#531=PLANE('',#19101);
#532=PLANE('',#19102);
#533=PLANE('',#19103);
#534=PLANE('',#19104);
#535=PLANE('',#19105);
#536=PLANE('',#19106);
#537=PLANE('',#19107);
#538=PLANE('',#19108);
#539=PLANE('',#19109);
#540=PLANE('',#19110);
#541=PLANE('',#19111);
#542=PLANE('',#19112);
#543=PLANE('',#19113);
#544=PLANE('',#19114);
#545=PLANE('',#19115);
#546=PLANE('',#19116);
#547=PLANE('',#19117);
#548=PLANE('',#19118);
#549=PLANE('',#19119);
#550=PLANE('',#19120);
#551=PLANE('',#19121);
#552=PLANE('',#19122);
#553=PLANE('',#19123);
#554=PLANE('',#19124);
#555=PLANE('',#19125);
#556=PLANE('',#19126);
#557=PLANE('',#19127);
#558=PLANE('',#19128);
#559=PLANE('',#19129);
#560=PLANE('',#19130);
#561=PLANE('',#19131);
#562=PLANE('',#19132);
#563=PLANE('',#19133);
#564=PLANE('',#19134);
#565=PLANE('',#19135);
#566=PLANE('',#19136);
#567=PLANE('',#19137);
#568=PLANE('',#19138);
#569=PLANE('',#19139);
#570=PLANE('',#19140);
#571=PLANE('',#19141);
#572=PLANE('',#19142);
#573=PLANE('',#19143);
#574=PLANE('',#19144);
#575=PLANE('',#19145);
#576=PLANE('',#19146);
#577=PLANE('',#19147);
#578=PLANE('',#19148);
#579=PLANE('',#19149);
#580=PLANE('',#19150);
#581=PLANE('',#19151);
#582=PLANE('',#19152);
#583=PLANE('',#19153);
#584=PLANE('',#19154);
#585=PLANE('',#19155);
#586=PLANE('',#19156);
#587=PLANE('',#19157);
#588=PLANE('',#19158);
#589=PLANE('',#19159);
#590=PLANE('',#19160);
#591=PLANE('',#19162);
#906=CONICAL_SURFACE('',#18949,16.9,0.785398163397449);
#907=CONICAL_SURFACE('',#18952,16.9,0.785398163397448);
#908=CONICAL_SURFACE('',#18963,2.75,0.785398163397449);
#909=CONICAL_SURFACE('',#18967,2.75,0.785398163397448);
#910=CONICAL_SURFACE('',#18968,2.75,0.785398163397449);
#911=CONICAL_SURFACE('',#18972,2.75,0.785398163397448);
#912=CONICAL_SURFACE('',#18973,2.75,0.785398163397449);
#913=CONICAL_SURFACE('',#18977,2.75,0.785398163397448);
#914=CONICAL_SURFACE('',#18978,1.1,0.785398163397448);
#1050=(
BOUNDED_CURVE()
B_SPLINE_CURVE(2,(#43966,#43967,#43968),.UNSPECIFIED.,.F.,.F.)
B_SPLINE_CURVE_WITH_KNOTS((3,3),(0.,0.00144737940428136),.UNSPECIFIED.)
CURVE()
GEOMETRIC_REPRESENTATION_ITEM()
RATIONAL_B_SPLINE_CURVE((1.,1.00001544417762,1.00003081080475))
REPRESENTATION_ITEM('')
);
#1051=(
BOUNDED_CURVE()
B_SPLINE_CURVE(2,(#43981,#43982,#43983),.UNSPECIFIED.,.F.,.F.)
B_SPLINE_CURVE_WITH_KNOTS((3,3),(0.575043800428103,0.576491179832384),
 .UNSPECIFIED.)
CURVE()
GEOMETRIC_REPRESENTATION_ITEM()
RATIONAL_B_SPLINE_CURVE((1.00003081080475,1.00001544417762,1.))
REPRESENTATION_ITEM('')
);
#1052=(
BOUNDED_CURVE()
B_SPLINE_CURVE(2,(#43997,#43998,#43999),.UNSPECIFIED.,.F.,.F.)
B_SPLINE_CURVE_WITH_KNOTS((3,3),(0.575043800428102,0.576491179832384),
 .UNSPECIFIED.)
CURVE()
GEOMETRIC_REPRESENTATION_ITEM()
RATIONAL_B_SPLINE_CURVE((1.00003081080475,1.00001544417762,1.))
REPRESENTATION_ITEM('')
);
#1053=(
BOUNDED_CURVE()
B_SPLINE_CURVE(2,(#44003,#44004,#44005),.UNSPECIFIED.,.F.,.F.)
B_SPLINE_CURVE_WITH_KNOTS((3,3),(0.,0.00144737940428207),.UNSPECIFIED.)
CURVE()
GEOMETRIC_REPRESENTATION_ITEM()
RATIONAL_B_SPLINE_CURVE((1.,1.00001544417762,1.00003081080475))
REPRESENTATION_ITEM('')
);
#1298=STYLED_ITEM('',(#60527),#90);
#1650=FACE_OUTER_BOUND('',#2625,.T.);
#1651=FACE_OUTER_BOUND('',#2626,.T.);
#1652=FACE_OUTER_BOUND('',#2628,.T.);
#1653=FACE_OUTER_BOUND('',#2629,.T.);
#1654=FACE_OUTER_BOUND('',#2640,.T.);
#1655=FACE_OUTER_BOUND('',#2641,.T.);
#1656=FACE_OUTER_BOUND('',#2642,.T.);
#1657=FACE_OUTER_BOUND('',#2643,.T.);
#1658=FACE_OUTER_BOUND('',#2644,.T.);
#1659=FACE_OUTER_BOUND('',#2645,.T.);
#1660=FACE_OUTER_BOUND('',#2656,.T.);
#1661=FACE_OUTER_BOUND('',#2657,.T.);
#1662=FACE_OUTER_BOUND('',#2658,.T.);
#1663=FACE_OUTER_BOUND('',#2659,.T.);
#1664=FACE_OUTER_BOUND('',#2660,.T.);
#1665=FACE_OUTER_BOUND('',#2661,.T.);
#1666=FACE_OUTER_BOUND('',#2662,.T.);
#1667=FACE_OUTER_BOUND('',#2663,.T.);
#1668=FACE_OUTER_BOUND('',#2664,.T.);
#1669=FACE_OUTER_BOUND('',#2665,.T.);
#1670=FACE_OUTER_BOUND('',#2666,.T.);
#1671=FACE_OUTER_BOUND('',#2667,.T.);
#1672=FACE_OUTER_BOUND('',#2668,.T.);
#1673=FACE_OUTER_BOUND('',#2669,.T.);
#1674=FACE_OUTER_BOUND('',#2670,.T.);
#1675=FACE_OUTER_BOUND('',#2671,.T.);
#1676=FACE_OUTER_BOUND('',#2672,.T.);
#1677=FACE_OUTER_BOUND('',#2673,.T.);
#1678=FACE_OUTER_BOUND('',#2674,.T.);
#1679=FACE_OUTER_BOUND('',#2675,.T.);
#1680=FACE_OUTER_BOUND('',#2676,.T.);
#1681=FACE_OUTER_BOUND('',#2677,.T.);
#1682=FACE_OUTER_BOUND('',#2678,.T.);
#1683=FACE_OUTER_BOUND('',#2679,.T.);
#1684=FACE_OUTER_BOUND('',#2680,.T.);
#1685=FACE_OUTER_BOUND('',#2681,.T.);
#1686=FACE_OUTER_BOUND('',#2682,.T.);
#1687=FACE_OUTER_BOUND('',#2683,.T.);
#1688=FACE_OUTER_BOUND('',#2684,.T.);
#1689=FACE_OUTER_BOUND('',#2685,.T.);
#1690=FACE_OUTER_BOUND('',#2686,.T.);
#1691=FACE_OUTER_BOUND('',#2687,.T.);
#1692=FACE_OUTER_BOUND('',#2688,.T.);
#1693=FACE_OUTER_BOUND('',#2689,.T.);
#1694=FACE_OUTER_BOUND('',#2690,.T.);
#1695=FACE_OUTER_BOUND('',#2691,.T.);
#1696=FACE_OUTER_BOUND('',#2692,.T.);
#1697=FACE_OUTER_BOUND('',#2693,.T.);
#1698=FACE_OUTER_BOUND('',#2694,.T.);
#1699=FACE_OUTER_BOUND('',#2695,.T.);
#1700=FACE_OUTER_BOUND('',#2696,.T.);
#1701=FACE_OUTER_BOUND('',#2697,.T.);
#1702=FACE_OUTER_BOUND('',#2698,.T.);
#1703=FACE_OUTER_BOUND('',#2699,.T.);
#1704=FACE_OUTER_BOUND('',#2700,.T.);
#1705=FACE_OUTER_BOUND('',#2701,.T.);
#1706=FACE_OUTER_BOUND('',#2702,.T.);
#1707=FACE_OUTER_BOUND('',#2703,.T.);
#1708=FACE_OUTER_BOUND('',#2704,.T.);
#1709=FACE_OUTER_BOUND('',#2705,.T.);
#1710=FACE_OUTER_BOUND('',#2706,.T.);
#1711=FACE_OUTER_BOUND('',#2707,.T.);
#1712=FACE_OUTER_BOUND('',#2708,.T.);
#1713=FACE_OUTER_BOUND('',#2709,.T.);
#1714=FACE_OUTER_BOUND('',#2710,.T.);
#1715=FACE_OUTER_BOUND('',#2711,.T.);
#1716=FACE_OUTER_BOUND('',#2712,.T.);
#1717=FACE_OUTER_BOUND('',#2713,.T.);
#1718=FACE_OUTER_BOUND('',#2714,.T.);
#1719=FACE_OUTER_BOUND('',#2715,.T.);
#1720=FACE_OUTER_BOUND('',#2716,.T.);
#1721=FACE_OUTER_BOUND('',#2717,.T.);
#1722=FACE_OUTER_BOUND('',#2718,.T.);
#1723=FACE_OUTER_BOUND('',#2719,.T.);
#1724=FACE_OUTER_BOUND('',#2720,.T.);
#1725=FACE_OUTER_BOUND('',#2721,.T.);
#1726=FACE_OUTER_BOUND('',#2722,.T.);
#1727=FACE_OUTER_BOUND('',#2723,.T.);
#1728=FACE_OUTER_BOUND('',#2724,.T.);
#1729=FACE_OUTER_BOUND('',#2725,.T.);
#1730=FACE_OUTER_BOUND('',#2726,.T.);
#1731=FACE_OUTER_BOUND('',#2727,.T.);
#1732=FACE_OUTER_BOUND('',#2728,.T.);
#1733=FACE_OUTER_BOUND('',#2729,.T.);
#1734=FACE_OUTER_BOUND('',#2730,.T.);
#1735=FACE_OUTER_BOUND('',#2731,.T.);
#1736=FACE_OUTER_BOUND('',#2732,.T.);
#1737=FACE_OUTER_BOUND('',#2733,.T.);
#1738=FACE_OUTER_BOUND('',#2734,.T.);
#1739=FACE_OUTER_BOUND('',#2735,.T.);
#1740=FACE_OUTER_BOUND('',#2736,.T.);
#1741=FACE_OUTER_BOUND('',#2737,.T.);
#1742=FACE_OUTER_BOUND('',#2738,.T.);
#1743=FACE_OUTER_BOUND('',#2739,.T.);
#1744=FACE_OUTER_BOUND('',#2740,.T.);
#1745=FACE_OUTER_BOUND('',#2741,.T.);
#1746=FACE_OUTER_BOUND('',#2742,.T.);
#1747=FACE_OUTER_BOUND('',#2743,.T.);
#1748=FACE_OUTER_BOUND('',#2744,.T.);
#1749=FACE_OUTER_BOUND('',#2745,.T.);
#1750=FACE_OUTER_BOUND('',#2746,.T.);
#1751=FACE_OUTER_BOUND('',#2747,.T.);
#1752=FACE_OUTER_BOUND('',#2748,.T.);
#1753=FACE_OUTER_BOUND('',#2749,.T.);
#1754=FACE_OUTER_BOUND('',#2750,.T.);
#1755=FACE_OUTER_BOUND('',#2751,.T.);
#1756=FACE_OUTER_BOUND('',#2752,.T.);
#1757=FACE_OUTER_BOUND('',#2753,.T.);
#1758=FACE_OUTER_BOUND('',#2754,.T.);
#1759=FACE_OUTER_BOUND('',#2755,.T.);
#1760=FACE_OUTER_BOUND('',#2756,.T.);
#1761=FACE_OUTER_BOUND('',#2757,.T.);
#1762=FACE_OUTER_BOUND('',#2758,.T.);
#1763=FACE_OUTER_BOUND('',#2759,.T.);
#1764=FACE_OUTER_BOUND('',#2760,.T.);
#1765=FACE_OUTER_BOUND('',#2761,.T.);
#1766=FACE_OUTER_BOUND('',#2762,.T.);
#1767=FACE_OUTER_BOUND('',#2763,.T.);
#1768=FACE_OUTER_BOUND('',#2764,.T.);
#1769=FACE_OUTER_BOUND('',#2765,.T.);
#1770=FACE_OUTER_BOUND('',#2766,.T.);
#1771=FACE_OUTER_BOUND('',#2767,.T.);
#1772=FACE_OUTER_BOUND('',#2768,.T.);
#1773=FACE_OUTER_BOUND('',#2769,.T.);
#1774=FACE_OUTER_BOUND('',#2770,.T.);
#1775=FACE_OUTER_BOUND('',#2771,.T.);
#1776=FACE_OUTER_BOUND('',#2772,.T.);
#1777=FACE_OUTER_BOUND('',#2773,.T.);
#1778=FACE_OUTER_BOUND('',#2774,.T.);
#1779=FACE_OUTER_BOUND('',#2775,.T.);
#1780=FACE_OUTER_BOUND('',#2776,.T.);
#1781=FACE_OUTER_BOUND('',#2777,.T.);
#1782=FACE_OUTER_BOUND('',#2778,.T.);
#1783=FACE_OUTER_BOUND('',#2779,.T.);
#1784=FACE_OUTER_BOUND('',#2780,.T.);
#1785=FACE_OUTER_BOUND('',#2781,.T.);
#1786=FACE_OUTER_BOUND('',#2782,.T.);
#1787=FACE_OUTER_BOUND('',#2783,.T.);
#1788=FACE_OUTER_BOUND('',#2784,.T.);
#1789=FACE_OUTER_BOUND('',#2785,.T.);
#1790=FACE_OUTER_BOUND('',#2786,.T.);
#1791=FACE_OUTER_BOUND('',#2787,.T.);
#1792=FACE_OUTER_BOUND('',#2788,.T.);
#1793=FACE_OUTER_BOUND('',#2789,.T.);
#1794=FACE_OUTER_BOUND('',#2790,.T.);
#1795=FACE_OUTER_BOUND('',#2791,.T.);
#1796=FACE_OUTER_BOUND('',#2792,.T.);
#1797=FACE_OUTER_BOUND('',#2793,.T.);
#1798=FACE_OUTER_BOUND('',#2794,.T.);
#1799=FACE_OUTER_BOUND('',#2795,.T.);
#1800=FACE_OUTER_BOUND('',#2796,.T.);
#1801=FACE_OUTER_BOUND('',#2797,.T.);
#1802=FACE_OUTER_BOUND('',#2798,.T.);
#1803=FACE_OUTER_BOUND('',#2799,.T.);
#1804=FACE_OUTER_BOUND('',#2800,.T.);
#1805=FACE_OUTER_BOUND('',#2801,.T.);
#1806=FACE_OUTER_BOUND('',#2802,.T.);
#1807=FACE_OUTER_BOUND('',#2803,.T.);
#1808=FACE_OUTER_BOUND('',#2804,.T.);
#1809=FACE_OUTER_BOUND('',#2805,.T.);
#1810=FACE_OUTER_BOUND('',#2806,.T.);
#1811=FACE_OUTER_BOUND('',#2807,.T.);
#1812=FACE_OUTER_BOUND('',#2808,.T.);
#1813=FACE_OUTER_BOUND('',#2809,.T.);
#1814=FACE_OUTER_BOUND('',#2810,.T.);
#1815=FACE_OUTER_BOUND('',#2811,.T.);
#1816=FACE_OUTER_BOUND('',#2812,.T.);
#1817=FACE_OUTER_BOUND('',#2813,.T.);
#1818=FACE_OUTER_BOUND('',#2814,.T.);
#1819=FACE_OUTER_BOUND('',#2815,.T.);
#1820=FACE_OUTER_BOUND('',#2816,.T.);
#1821=FACE_OUTER_BOUND('',#2817,.T.);
#1822=FACE_OUTER_BOUND('',#2818,.T.);
#1823=FACE_OUTER_BOUND('',#2819,.T.);
#1824=FACE_OUTER_BOUND('',#2820,.T.);
#1825=FACE_OUTER_BOUND('',#2821,.T.);
#1826=FACE_OUTER_BOUND('',#2822,.T.);
#1827=FACE_OUTER_BOUND('',#2823,.T.);
#1828=FACE_OUTER_BOUND('',#2824,.T.);
#1829=FACE_OUTER_BOUND('',#2825,.T.);
#1830=FACE_OUTER_BOUND('',#2826,.T.);
#1831=FACE_OUTER_BOUND('',#2827,.T.);
#1832=FACE_OUTER_BOUND('',#2828,.T.);
#1833=FACE_OUTER_BOUND('',#2829,.T.);
#1834=FACE_OUTER_BOUND('',#2830,.T.);
#1835=FACE_OUTER_BOUND('',#2831,.T.);
#1836=FACE_OUTER_BOUND('',#2832,.T.);
#1837=FACE_OUTER_BOUND('',#2833,.T.);
#1838=FACE_OUTER_BOUND('',#2834,.T.);
#1839=FACE_OUTER_BOUND('',#2835,.T.);
#1840=FACE_OUTER_BOUND('',#2836,.T.);
#1841=FACE_OUTER_BOUND('',#2837,.T.);
#1842=FACE_OUTER_BOUND('',#2838,.T.);
#1843=FACE_OUTER_BOUND('',#2839,.T.);
#1844=FACE_OUTER_BOUND('',#2840,.T.);
#1845=FACE_OUTER_BOUND('',#2841,.T.);
#1846=FACE_OUTER_BOUND('',#2842,.T.);
#1847=FACE_OUTER_BOUND('',#2843,.T.);
#1848=FACE_OUTER_BOUND('',#2844,.T.);
#1849=FACE_OUTER_BOUND('',#2845,.T.);
#1850=FACE_OUTER_BOUND('',#2846,.T.);
#1851=FACE_OUTER_BOUND('',#2847,.T.);
#1852=FACE_OUTER_BOUND('',#2848,.T.);
#1853=FACE_OUTER_BOUND('',#2849,.T.);
#2625=EDGE_LOOP('',(#13751,#13752,#13753,#13754));
#2626=EDGE_LOOP('',(#13755,#13756,#13757,#13758));
#2627=EDGE_LOOP('',(#13759));
#2628=EDGE_LOOP('',(#13760,#13761,#13762,#13763));
#2629=EDGE_LOOP('',(#13764,#13765,#13766,#13767));
#2630=EDGE_LOOP('',(#13768));
#2631=EDGE_LOOP('',(#13769));
#2632=EDGE_LOOP('',(#13770));
#2633=EDGE_LOOP('',(#13771,#13772,#13773,#13774,#13775,#13776,#13777,#13778,
#13779,#13780,#13781,#13782,#13783,#13784));
#2634=EDGE_LOOP('',(#13785,#13786,#13787,#13788,#13789,#13790,#13791,#13792,
#13793,#13794,#13795,#13796,#13797,#13798));
#2635=EDGE_LOOP('',(#13799,#13800,#13801,#13802,#13803,#13804,#13805,#13806,
#13807,#13808,#13809,#13810,#13811,#13812));
#2636=EDGE_LOOP('',(#13813,#13814,#13815,#13816,#13817,#13818,#13819,#13820,
#13821,#13822,#13823,#13824,#13825,#13826));
#2637=EDGE_LOOP('',(#13827,#13828,#13829,#13830,#13831,#13832,#13833,#13834,
#13835,#13836,#13837,#13838,#13839,#13840));
#2638=EDGE_LOOP('',(#13841,#13842,#13843,#13844,#13845,#13846,#13847,#13848,
#13849,#13850,#13851,#13852,#13853,#13854));
#2639=EDGE_LOOP('',(#13855));
#2640=EDGE_LOOP('',(#13856,#13857,#13858,#13859,#13860,#13861));
#2641=EDGE_LOOP('',(#13862,#13863,#13864,#13865));
#2642=EDGE_LOOP('',(#13866,#13867,#13868,#13869,#13870,#13871));
#2643=EDGE_LOOP('',(#13872,#13873,#13874,#13875));
#2644=EDGE_LOOP('',(#13876,#13877,#13878,#13879,#13880,#13881,#13882,#13883));
#2645=EDGE_LOOP('',(#13884,#13885,#13886,#13887));
#2646=EDGE_LOOP('',(#13888));
#2647=EDGE_LOOP('',(#13889));
#2648=EDGE_LOOP('',(#13890));
#2649=EDGE_LOOP('',(#13891,#13892,#13893,#13894,#13895,#13896,#13897,#13898,
#13899,#13900,#13901,#13902,#13903,#13904));
#2650=EDGE_LOOP('',(#13905,#13906,#13907,#13908,#13909,#13910,#13911,#13912,
#13913,#13914,#13915,#13916,#13917,#13918));
#2651=EDGE_LOOP('',(#13919,#13920,#13921,#13922,#13923,#13924,#13925,#13926,
#13927,#13928,#13929,#13930,#13931,#13932));
#2652=EDGE_LOOP('',(#13933,#13934,#13935,#13936,#13937,#13938,#13939,#13940,
#13941,#13942,#13943,#13944,#13945,#13946));
#2653=EDGE_LOOP('',(#13947,#13948,#13949,#13950,#13951,#13952,#13953,#13954,
#13955,#13956,#13957,#13958,#13959,#13960));
#2654=EDGE_LOOP('',(#13961,#13962,#13963,#13964,#13965,#13966,#13967,#13968,
#13969,#13970,#13971,#13972,#13973,#13974));
#2655=EDGE_LOOP('',(#13975));
#2656=EDGE_LOOP('',(#13976,#13977,#13978,#13979));
#2657=EDGE_LOOP('',(#13980,#13981,#13982,#13983));
#2658=EDGE_LOOP('',(#13984,#13985,#13986,#13987));
#2659=EDGE_LOOP('',(#13988,#13989,#13990,#13991));
#2660=EDGE_LOOP('',(#13992,#13993,#13994,#13995));
#2661=EDGE_LOOP('',(#13996,#13997,#13998,#13999));
#2662=EDGE_LOOP('',(#14000,#14001,#14002,#14003));
#2663=EDGE_LOOP('',(#14004,#14005,#14006,#14007));
#2664=EDGE_LOOP('',(#14008,#14009,#14010,#14011));
#2665=EDGE_LOOP('',(#14012,#14013,#14014,#14015));
#2666=EDGE_LOOP('',(#14016,#14017,#14018,#14019));
#2667=EDGE_LOOP('',(#14020,#14021,#14022,#14023,#14024,#14025));
#2668=EDGE_LOOP('',(#14026,#14027,#14028,#14029));
#2669=EDGE_LOOP('',(#14030,#14031,#14032,#14033));
#2670=EDGE_LOOP('',(#14034,#14035,#14036,#14037));
#2671=EDGE_LOOP('',(#14038,#14039,#14040,#14041));
#2672=EDGE_LOOP('',(#14042,#14043,#14044,#14045));
#2673=EDGE_LOOP('',(#14046,#14047,#14048,#14049));
#2674=EDGE_LOOP('',(#14050,#14051,#14052,#14053));
#2675=EDGE_LOOP('',(#14054,#14055,#14056,#14057));
#2676=EDGE_LOOP('',(#14058,#14059,#14060,#14061));
#2677=EDGE_LOOP('',(#14062,#14063,#14064,#14065));
#2678=EDGE_LOOP('',(#14066,#14067,#14068,#14069));
#2679=EDGE_LOOP('',(#14070,#14071,#14072,#14073));
#2680=EDGE_LOOP('',(#14074,#14075,#14076,#14077));
#2681=EDGE_LOOP('',(#14078,#14079,#14080,#14081));
#2682=EDGE_LOOP('',(#14082,#14083,#14084,#14085,#14086,#14087,#14088,#14089,
#14090,#14091,#14092,#14093,#14094,#14095));
#2683=EDGE_LOOP('',(#14096,#14097,#14098,#14099));
#2684=EDGE_LOOP('',(#14100,#14101,#14102,#14103));
#2685=EDGE_LOOP('',(#14104,#14105,#14106,#14107));
#2686=EDGE_LOOP('',(#14108,#14109,#14110,#14111));
#2687=EDGE_LOOP('',(#14112,#14113,#14114,#14115));
#2688=EDGE_LOOP('',(#14116,#14117,#14118,#14119));
#2689=EDGE_LOOP('',(#14120,#14121,#14122,#14123));
#2690=EDGE_LOOP('',(#14124,#14125,#14126,#14127));
#2691=EDGE_LOOP('',(#14128,#14129,#14130,#14131));
#2692=EDGE_LOOP('',(#14132,#14133,#14134,#14135));
#2693=EDGE_LOOP('',(#14136,#14137,#14138,#14139));
#2694=EDGE_LOOP('',(#14140,#14141,#14142,#14143));
#2695=EDGE_LOOP('',(#14144,#14145,#14146,#14147));
#2696=EDGE_LOOP('',(#14148,#14149,#14150,#14151));
#2697=EDGE_LOOP('',(#14152,#14153,#14154,#14155,#14156,#14157,#14158,#14159,
#14160,#14161,#14162,#14163,#14164,#14165));
#2698=EDGE_LOOP('',(#14166,#14167,#14168,#14169));
#2699=EDGE_LOOP('',(#14170,#14171,#14172,#14173));
#2700=EDGE_LOOP('',(#14174,#14175,#14176,#14177));
#2701=EDGE_LOOP('',(#14178,#14179,#14180,#14181));
#2702=EDGE_LOOP('',(#14182,#14183,#14184,#14185));
#2703=EDGE_LOOP('',(#14186,#14187,#14188,#14189));
#2704=EDGE_LOOP('',(#14190,#14191,#14192,#14193));
#2705=EDGE_LOOP('',(#14194,#14195,#14196,#14197));
#2706=EDGE_LOOP('',(#14198,#14199,#14200,#14201));
#2707=EDGE_LOOP('',(#14202,#14203,#14204,#14205));
#2708=EDGE_LOOP('',(#14206,#14207,#14208,#14209));
#2709=EDGE_LOOP('',(#14210,#14211,#14212,#14213));
#2710=EDGE_LOOP('',(#14214,#14215,#14216,#14217));
#2711=EDGE_LOOP('',(#14218,#14219,#14220,#14221));
#2712=EDGE_LOOP('',(#14222,#14223,#14224,#14225,#14226,#14227,#14228,#14229,
#14230,#14231,#14232,#14233,#14234,#14235));
#2713=EDGE_LOOP('',(#14236,#14237,#14238,#14239));
#2714=EDGE_LOOP('',(#14240,#14241,#14242,#14243));
#2715=EDGE_LOOP('',(#14244,#14245,#14246,#14247));
#2716=EDGE_LOOP('',(#14248,#14249,#14250,#14251));
#2717=EDGE_LOOP('',(#14252,#14253,#14254,#14255));
#2718=EDGE_LOOP('',(#14256,#14257,#14258,#14259));
#2719=EDGE_LOOP('',(#14260,#14261,#14262,#14263));
#2720=EDGE_LOOP('',(#14264,#14265,#14266,#14267));
#2721=EDGE_LOOP('',(#14268,#14269,#14270,#14271));
#2722=EDGE_LOOP('',(#14272,#14273,#14274,#14275));
#2723=EDGE_LOOP('',(#14276,#14277,#14278,#14279));
#2724=EDGE_LOOP('',(#14280,#14281,#14282,#14283));
#2725=EDGE_LOOP('',(#14284,#14285,#14286,#14287));
#2726=EDGE_LOOP('',(#14288,#14289,#14290,#14291));
#2727=EDGE_LOOP('',(#14292,#14293,#14294,#14295,#14296,#14297,#14298,#14299,
#14300,#14301,#14302,#14303,#14304,#14305));
#2728=EDGE_LOOP('',(#14306,#14307,#14308,#14309));
#2729=EDGE_LOOP('',(#14310,#14311,#14312,#14313));
#2730=EDGE_LOOP('',(#14314,#14315,#14316,#14317));
#2731=EDGE_LOOP('',(#14318,#14319,#14320,#14321));
#2732=EDGE_LOOP('',(#14322,#14323,#14324,#14325));
#2733=EDGE_LOOP('',(#14326,#14327,#14328,#14329));
#2734=EDGE_LOOP('',(#14330,#14331,#14332,#14333));
#2735=EDGE_LOOP('',(#14334,#14335,#14336,#14337));
#2736=EDGE_LOOP('',(#14338,#14339,#14340,#14341));
#2737=EDGE_LOOP('',(#14342,#14343,#14344,#14345));
#2738=EDGE_LOOP('',(#14346,#14347,#14348,#14349));
#2739=EDGE_LOOP('',(#14350,#14351,#14352,#14353));
#2740=EDGE_LOOP('',(#14354,#14355,#14356,#14357));
#2741=EDGE_LOOP('',(#14358,#14359,#14360,#14361));
#2742=EDGE_LOOP('',(#14362,#14363,#14364,#14365,#14366,#14367,#14368,#14369,
#14370,#14371,#14372,#14373,#14374,#14375));
#2743=EDGE_LOOP('',(#14376,#14377,#14378,#14379));
#2744=EDGE_LOOP('',(#14380,#14381,#14382,#14383));
#2745=EDGE_LOOP('',(#14384,#14385,#14386,#14387));
#2746=EDGE_LOOP('',(#14388,#14389,#14390,#14391));
#2747=EDGE_LOOP('',(#14392,#14393,#14394,#14395));
#2748=EDGE_LOOP('',(#14396,#14397,#14398,#14399));
#2749=EDGE_LOOP('',(#14400,#14401,#14402,#14403));
#2750=EDGE_LOOP('',(#14404,#14405,#14406,#14407));
#2751=EDGE_LOOP('',(#14408,#14409,#14410,#14411));
#2752=EDGE_LOOP('',(#14412,#14413,#14414,#14415));
#2753=EDGE_LOOP('',(#14416,#14417,#14418,#14419));
#2754=EDGE_LOOP('',(#14420,#14421,#14422,#14423));
#2755=EDGE_LOOP('',(#14424,#14425,#14426,#14427));
#2756=EDGE_LOOP('',(#14428,#14429,#14430,#14431));
#2757=EDGE_LOOP('',(#14432,#14433,#14434,#14435,#14436,#14437,#14438,#14439,
#14440,#14441,#14442,#14443,#14444,#14445));
#2758=EDGE_LOOP('',(#14446,#14447,#14448,#14449));
#2759=EDGE_LOOP('',(#14450,#14451,#14452,#14453));
#2760=EDGE_LOOP('',(#14454,#14455,#14456,#14457));
#2761=EDGE_LOOP('',(#14458,#14459,#14460,#14461));
#2762=EDGE_LOOP('',(#14462,#14463,#14464,#14465));
#2763=EDGE_LOOP('',(#14466,#14467,#14468,#14469));
#2764=EDGE_LOOP('',(#14470,#14471,#14472,#14473));
#2765=EDGE_LOOP('',(#14474,#14475,#14476,#14477));
#2766=EDGE_LOOP('',(#14478,#14479,#14480,#14481));
#2767=EDGE_LOOP('',(#14482,#14483,#14484,#14485));
#2768=EDGE_LOOP('',(#14486,#14487,#14488,#14489));
#2769=EDGE_LOOP('',(#14490,#14491,#14492,#14493));
#2770=EDGE_LOOP('',(#14494,#14495,#14496,#14497));
#2771=EDGE_LOOP('',(#14498,#14499,#14500,#14501));
#2772=EDGE_LOOP('',(#14502,#14503,#14504,#14505,#14506,#14507,#14508,#14509,
#14510,#14511,#14512,#14513,#14514,#14515));
#2773=EDGE_LOOP('',(#14516,#14517,#14518,#14519));
#2774=EDGE_LOOP('',(#14520,#14521,#14522,#14523));
#2775=EDGE_LOOP('',(#14524,#14525,#14526,#14527));
#2776=EDGE_LOOP('',(#14528,#14529,#14530,#14531));
#2777=EDGE_LOOP('',(#14532,#14533,#14534,#14535));
#2778=EDGE_LOOP('',(#14536,#14537,#14538,#14539));
#2779=EDGE_LOOP('',(#14540,#14541,#14542,#14543));
#2780=EDGE_LOOP('',(#14544,#14545,#14546,#14547));
#2781=EDGE_LOOP('',(#14548,#14549,#14550,#14551));
#2782=EDGE_LOOP('',(#14552,#14553,#14554,#14555));
#2783=EDGE_LOOP('',(#14556,#14557,#14558,#14559));
#2784=EDGE_LOOP('',(#14560,#14561,#14562,#14563));
#2785=EDGE_LOOP('',(#14564,#14565,#14566,#14567));
#2786=EDGE_LOOP('',(#14568,#14569,#14570,#14571));
#2787=EDGE_LOOP('',(#14572,#14573,#14574,#14575,#14576,#14577,#14578,#14579,
#14580,#14581,#14582,#14583,#14584,#14585));
#2788=EDGE_LOOP('',(#14586,#14587,#14588,#14589));
#2789=EDGE_LOOP('',(#14590,#14591,#14592,#14593));
#2790=EDGE_LOOP('',(#14594,#14595,#14596,#14597));
#2791=EDGE_LOOP('',(#14598,#14599,#14600,#14601));
#2792=EDGE_LOOP('',(#14602,#14603,#14604,#14605));
#2793=EDGE_LOOP('',(#14606,#14607,#14608,#14609));
#2794=EDGE_LOOP('',(#14610,#14611,#14612,#14613));
#2795=EDGE_LOOP('',(#14614,#14615,#14616,#14617));
#2796=EDGE_LOOP('',(#14618,#14619,#14620,#14621));
#2797=EDGE_LOOP('',(#14622,#14623,#14624,#14625));
#2798=EDGE_LOOP('',(#14626,#14627,#14628,#14629));
#2799=EDGE_LOOP('',(#14630,#14631,#14632,#14633));
#2800=EDGE_LOOP('',(#14634,#14635,#14636,#14637));
#2801=EDGE_LOOP('',(#14638,#14639,#14640,#14641));
#2802=EDGE_LOOP('',(#14642,#14643,#14644,#14645,#14646,#14647,#14648,#14649,
#14650,#14651,#14652,#14653,#14654,#14655));
#2803=EDGE_LOOP('',(#14656,#14657,#14658,#14659));
#2804=EDGE_LOOP('',(#14660,#14661,#14662,#14663));
#2805=EDGE_LOOP('',(#14664,#14665,#14666,#14667));
#2806=EDGE_LOOP('',(#14668,#14669,#14670,#14671));
#2807=EDGE_LOOP('',(#14672,#14673,#14674,#14675));
#2808=EDGE_LOOP('',(#14676,#14677,#14678,#14679));
#2809=EDGE_LOOP('',(#14680,#14681,#14682,#14683));
#2810=EDGE_LOOP('',(#14684,#14685,#14686,#14687));
#2811=EDGE_LOOP('',(#14688,#14689,#14690,#14691));
#2812=EDGE_LOOP('',(#14692,#14693,#14694,#14695));
#2813=EDGE_LOOP('',(#14696,#14697,#14698,#14699));
#2814=EDGE_LOOP('',(#14700,#14701,#14702,#14703));
#2815=EDGE_LOOP('',(#14704,#14705,#14706,#14707));
#2816=EDGE_LOOP('',(#14708,#14709,#14710,#14711));
#2817=EDGE_LOOP('',(#14712,#14713,#14714,#14715,#14716,#14717,#14718,#14719,
#14720,#14721,#14722,#14723,#14724,#14725));
#2818=EDGE_LOOP('',(#14726,#14727,#14728,#14729));
#2819=EDGE_LOOP('',(#14730,#14731,#14732,#14733));
#2820=EDGE_LOOP('',(#14734,#14735,#14736,#14737));
#2821=EDGE_LOOP('',(#14738,#14739,#14740,#14741));
#2822=EDGE_LOOP('',(#14742,#14743,#14744,#14745));
#2823=EDGE_LOOP('',(#14746,#14747,#14748,#14749));
#2824=EDGE_LOOP('',(#14750,#14751,#14752,#14753));
#2825=EDGE_LOOP('',(#14754,#14755,#14756,#14757));
#2826=EDGE_LOOP('',(#14758,#14759,#14760,#14761));
#2827=EDGE_LOOP('',(#14762,#14763,#14764,#14765));
#2828=EDGE_LOOP('',(#14766,#14767,#14768,#14769));
#2829=EDGE_LOOP('',(#14770,#14771,#14772,#14773));
#2830=EDGE_LOOP('',(#14774,#14775,#14776,#14777));
#2831=EDGE_LOOP('',(#14778,#14779,#14780,#14781));
#2832=EDGE_LOOP('',(#14782,#14783,#14784,#14785,#14786,#14787,#14788,#14789,
#14790,#14791,#14792,#14793,#14794,#14795));
#2833=EDGE_LOOP('',(#14796,#14797,#14798,#14799));
#2834=EDGE_LOOP('',(#14800,#14801,#14802,#14803));
#2835=EDGE_LOOP('',(#14804,#14805,#14806,#14807));
#2836=EDGE_LOOP('',(#14808,#14809,#14810,#14811));
#2837=EDGE_LOOP('',(#14812,#14813,#14814,#14815));
#2838=EDGE_LOOP('',(#14816,#14817,#14818,#14819));
#2839=EDGE_LOOP('',(#14820,#14821,#14822,#14823));
#2840=EDGE_LOOP('',(#14824,#14825,#14826,#14827));
#2841=EDGE_LOOP('',(#14828,#14829,#14830,#14831));
#2842=EDGE_LOOP('',(#14832,#14833,#14834,#14835));
#2843=EDGE_LOOP('',(#14836,#14837,#14838,#14839));
#2844=EDGE_LOOP('',(#14840,#14841,#14842,#14843));
#2845=EDGE_LOOP('',(#14844,#14845,#14846,#14847));
#2846=EDGE_LOOP('',(#14848,#14849,#14850,#14851));
#2847=EDGE_LOOP('',(#14852,#14853,#14854,#14855,#14856,#14857,#14858,#14859,
#14860,#14861,#14862,#14863,#14864,#14865));
#2848=EDGE_LOOP('',(#14866,#14867,#14868,#14869,#14870,#14871,#14872,#14873,
#14874));
#2849=EDGE_LOOP('',(#14875,#14876,#14877,#14878,#14879,#14880,#14881,#14882));
#3517=CIRCLE('',#18941,1.2);
#3518=CIRCLE('',#18944,16.8);
#3519=CIRCLE('',#18945,2.85);
#3520=CIRCLE('',#18946,2.85);
#3521=CIRCLE('',#18947,5.85);
#3522=CIRCLE('',#18948,2.85);
#3523=CIRCLE('',#18950,17.);
#3524=CIRCLE('',#18953,17.);
#3525=CIRCLE('',#18954,16.8);
#3526=CIRCLE('',#18958,2.85);
#3527=CIRCLE('',#18959,2.85);
#3528=CIRCLE('',#18960,5.85);
#3529=CIRCLE('',#18961,2.85);
#3530=CIRCLE('',#18964,2.65);
#3531=CIRCLE('',#18966,2.65);
#3532=CIRCLE('',#18969,2.65);
#3533=CIRCLE('',#18971,2.65);
#3534=CIRCLE('',#18974,2.65);
#3535=CIRCLE('',#18976,2.65);
#3536=CIRCLE('',#18979,1.);
#4096=B_SPLINE_CURVE_WITH_KNOTS('',3,(#43970,#43971,#43972,#43973),
 .UNSPECIFIED.,.F.,.F.,(4,4),(0.,0.0304160109013453),.UNSPECIFIED.);
#4097=B_SPLINE_CURVE_WITH_KNOTS('',3,(#43977,#43978,#43979,#43980),
 .UNSPECIFIED.,.F.,.F.,(4,4),(0.,0.0304159808371363),.UNSPECIFIED.);
#4098=B_SPLINE_CURVE_WITH_KNOTS('',3,(#43989,#43990,#43991,#43992),
 .UNSPECIFIED.,.F.,.F.,(4,4),(0.,0.0304160109012714),.UNSPECIFIED.);
#4099=B_SPLINE_CURVE_WITH_KNOTS('',3,(#44006,#44007,#44008,#44009),
 .UNSPECIFIED.,.F.,.F.,(4,4),(0.,0.0304159808372897),.UNSPECIFIED.);
#4100=B_SPLINE_CURVE_WITH_KNOTS('',3,(#44232,#44233,#44234,#44235,#44236,
#44237,#44238,#44239,#44240,#44241),.UNSPECIFIED.,.F.,.F.,(4,2,2,2,4),(0.,
0.0377490101969186,0.0754980203938373,0.113245913367995,0.150993806342152),
 .UNSPECIFIED.);
#4101=B_SPLINE_CURVE_WITH_KNOTS('',3,(#44243,#44244,#44245,#44246,#44247,
#44248,#44249,#44250,#44251,#44252),.UNSPECIFIED.,.F.,.F.,(4,2,2,2,4),(0.452981419026456,
0.490729312000613,0.52847720497477,0.566226215171689,0.603975225368608),
 .UNSPECIFIED.);
#4102=B_SPLINE_CURVE_WITH_KNOTS('',3,(#44253,#44254,#44255,#44256,#44257,
#44258,#44259,#44260,#44261,#44262,#44263,#44264,#44265,#44266,#44267,#44268,
#44269,#44270),.UNSPECIFIED.,.F.,.F.,(4,2,2,2,2,2,2,2,4),(0.150993806342152,
0.188741699316309,0.226489592290467,0.264238602487385,0.301987612684304,
0.339736622881222,0.377485633078141,0.415233526052298,0.452981419026456),
 .UNSPECIFIED.);
#4786=LINE('',#43762,#6198);
#4787=LINE('',#43764,#6199);
#4788=LINE('',#43766,#6200);
#4789=LINE('',#43767,#6201);
#4790=LINE('',#43770,#6202);
#4791=LINE('',#43772,#6203);
#4792=LINE('',#43773,#6204);
#4793=LINE('',#43778,#6205);
#4794=LINE('',#43780,#6206);
#4795=LINE('',#43781,#6207);
#4796=LINE('',#43784,#6208);
#4797=LINE('',#43786,#6209);
#4798=LINE('',#43796,#6210);
#4799=LINE('',#43798,#6211);
#4800=LINE('',#43800,#6212);
#4801=LINE('',#43802,#6213);
#4802=LINE('',#43804,#6214);
#4803=LINE('',#43806,#6215);
#4804=LINE('',#43808,#6216);
#4805=LINE('',#43810,#6217);
#4806=LINE('',#43812,#6218);
#4807=LINE('',#43814,#6219);
#4808=LINE('',#43816,#6220);
#4809=LINE('',#43818,#6221);
#4810=LINE('',#43820,#6222);
#4811=LINE('',#43821,#6223);
#4812=LINE('',#43824,#6224);
#4813=LINE('',#43826,#6225);
#4814=LINE('',#43828,#6226);
#4815=LINE('',#43830,#6227);
#4816=LINE('',#43832,#6228);
#4817=LINE('',#43834,#6229);
#4818=LINE('',#43836,#6230);
#4819=LINE('',#43838,#6231);
#4820=LINE('',#43840,#6232);
#4821=LINE('',#43842,#6233);
#4822=LINE('',#43844,#6234);
#4823=LINE('',#43846,#6235);
#4824=LINE('',#43848,#6236);
#4825=LINE('',#43849,#6237);
#4826=LINE('',#43852,#6238);
#4827=LINE('',#43854,#6239);
#4828=LINE('',#43856,#6240);
#4829=LINE('',#43858,#6241);
#4830=LINE('',#43860,#6242);
#4831=LINE('',#43862,#6243);
#4832=LINE('',#43864,#6244);
#4833=LINE('',#43866,#6245);
#4834=LINE('',#43868,#6246);
#4835=LINE('',#43870,#6247);
#4836=LINE('',#43872,#6248);
#4837=LINE('',#43874,#6249);
#4838=LINE('',#43876,#6250);
#4839=LINE('',#43877,#6251);
#4840=LINE('',#43880,#6252);
#4841=LINE('',#43882,#6253);
#4842=LINE('',#43884,#6254);
#4843=LINE('',#43886,#6255);
#4844=LINE('',#43888,#6256);
#4845=LINE('',#43890,#6257);
#4846=LINE('',#43892,#6258);
#4847=LINE('',#43894,#6259);
#4848=LINE('',#43896,#6260);
#4849=LINE('',#43898,#6261);
#4850=LINE('',#43900,#6262);
#4851=LINE('',#43902,#6263);
#4852=LINE('',#43904,#6264);
#4853=LINE('',#43905,#6265);
#4854=LINE('',#43908,#6266);
#4855=LINE('',#43910,#6267);
#4856=LINE('',#43912,#6268);
#4857=LINE('',#43914,#6269);
#4858=LINE('',#43916,#6270);
#4859=LINE('',#43918,#6271);
#4860=LINE('',#43920,#6272);
#4861=LINE('',#43922,#6273);
#4862=LINE('',#43924,#6274);
#4863=LINE('',#43926,#6275);
#4864=LINE('',#43928,#6276);
#4865=LINE('',#43930,#6277);
#4866=LINE('',#43932,#6278);
#4867=LINE('',#43933,#6279);
#4868=LINE('',#43936,#6280);
#4869=LINE('',#43938,#6281);
#4870=LINE('',#43940,#6282);
#4871=LINE('',#43942,#6283);
#4872=LINE('',#43944,#6284);
#4873=LINE('',#43946,#6285);
#4874=LINE('',#43948,#6286);
#4875=LINE('',#43950,#6287);
#4876=LINE('',#43952,#6288);
#4877=LINE('',#43954,#6289);
#4878=LINE('',#43956,#6290);
#4879=LINE('',#43958,#6291);
#4880=LINE('',#43960,#6292);
#4881=LINE('',#43961,#6293);
#4882=LINE('',#43986,#6294);
#4883=LINE('',#43988,#6295);
#4884=LINE('',#44011,#6296);
#4885=LINE('',#44012,#6297);
#4886=LINE('',#44014,#6298);
#4887=LINE('',#44016,#6299);
#4888=LINE('',#44025,#6300);
#4889=LINE('',#44027,#6301);
#4890=LINE('',#44029,#6302);
#4891=LINE('',#44031,#6303);
#4892=LINE('',#44033,#6304);
#4893=LINE('',#44035,#6305);
#4894=LINE('',#44037,#6306);
#4895=LINE('',#44039,#6307);
#4896=LINE('',#44041,#6308);
#4897=LINE('',#44043,#6309);
#4898=LINE('',#44045,#6310);
#4899=LINE('',#44047,#6311);
#4900=LINE('',#44049,#6312);
#4901=LINE('',#44050,#6313);
#4902=LINE('',#44053,#6314);
#4903=LINE('',#44055,#6315);
#4904=LINE('',#44057,#6316);
#4905=LINE('',#44059,#6317);
#4906=LINE('',#44061,#6318);
#4907=LINE('',#44063,#6319);
#4908=LINE('',#44065,#6320);
#4909=LINE('',#44067,#6321);
#4910=LINE('',#44069,#6322);
#4911=LINE('',#44071,#6323);
#4912=LINE('',#44073,#6324);
#4913=LINE('',#44075,#6325);
#4914=LINE('',#44077,#6326);
#4915=LINE('',#44078,#6327);
#4916=LINE('',#44081,#6328);
#4917=LINE('',#44083,#6329);
#4918=LINE('',#44085,#6330);
#4919=LINE('',#44087,#6331);
#4920=LINE('',#44089,#6332);
#4921=LINE('',#44091,#6333);
#4922=LINE('',#44093,#6334);
#4923=LINE('',#44095,#6335);
#4924=LINE('',#44097,#6336);
#4925=LINE('',#44099,#6337);
#4926=LINE('',#44101,#6338);
#4927=LINE('',#44103,#6339);
#4928=LINE('',#44105,#6340);
#4929=LINE('',#44106,#6341);
#4930=LINE('',#44109,#6342);
#4931=LINE('',#44111,#6343);
#4932=LINE('',#44113,#6344);
#4933=LINE('',#44115,#6345);
#4934=LINE('',#44117,#6346);
#4935=LINE('',#44119,#6347);
#4936=LINE('',#44121,#6348);
#4937=LINE('',#44123,#6349);
#4938=LINE('',#44125,#6350);
#4939=LINE('',#44127,#6351);
#4940=LINE('',#44129,#6352);
#4941=LINE('',#44131,#6353);
#4942=LINE('',#44133,#6354);
#4943=LINE('',#44134,#6355);
#4944=LINE('',#44137,#6356);
#4945=LINE('',#44139,#6357);
#4946=LINE('',#44141,#6358);
#4947=LINE('',#44143,#6359);
#4948=LINE('',#44145,#6360);
#4949=LINE('',#44147,#6361);
#4950=LINE('',#44149,#6362);
#4951=LINE('',#44151,#6363);
#4952=LINE('',#44153,#6364);
#4953=LINE('',#44155,#6365);
#4954=LINE('',#44157,#6366);
#4955=LINE('',#44159,#6367);
#4956=LINE('',#44161,#6368);
#4957=LINE('',#44162,#6369);
#4958=LINE('',#44165,#6370);
#4959=LINE('',#44167,#6371);
#4960=LINE('',#44169,#6372);
#4961=LINE('',#44171,#6373);
#4962=LINE('',#44173,#6374);
#4963=LINE('',#44175,#6375);
#4964=LINE('',#44177,#6376);
#4965=LINE('',#44179,#6377);
#4966=LINE('',#44181,#6378);
#4967=LINE('',#44183,#6379);
#4968=LINE('',#44185,#6380);
#4969=LINE('',#44187,#6381);
#4970=LINE('',#44189,#6382);
#4971=LINE('',#44190,#6383);
#4972=LINE('',#44196,#6384);
#4973=LINE('',#44200,#6385);
#4974=LINE('',#44203,#6386);
#4975=LINE('',#44206,#6387);
#4976=LINE('',#44210,#6388);
#4977=LINE('',#44213,#6389);
#4978=LINE('',#44216,#6390);
#4979=LINE('',#44220,#6391);
#4980=LINE('',#44223,#6392);
#4981=LINE('',#44226,#6393);
#4982=LINE('',#44230,#6394);
#4983=LINE('',#44273,#6395);
#4984=LINE('',#44275,#6396);
#4985=LINE('',#44276,#6397);
#4986=LINE('',#44279,#6398);
#4987=LINE('',#44280,#6399);
#4988=LINE('',#44283,#6400);
#4989=LINE('',#44284,#6401);
#4990=LINE('',#44287,#6402);
#4991=LINE('',#44288,#6403);
#4992=LINE('',#44291,#6404);
#4993=LINE('',#44292,#6405);
#4994=LINE('',#44295,#6406);
#4995=LINE('',#44296,#6407);
#4996=LINE('',#44299,#6408);
#4997=LINE('',#44300,#6409);
#4998=LINE('',#44303,#6410);
#4999=LINE('',#44304,#6411);
#5000=LINE('',#44307,#6412);
#5001=LINE('',#44308,#6413);
#5002=LINE('',#44311,#6414);
#5003=LINE('',#44312,#6415);
#5004=LINE('',#44315,#6416);
#5005=LINE('',#44316,#6417);
#5006=LINE('',#44319,#6418);
#5007=LINE('',#44320,#6419);
#5008=LINE('',#44323,#6420);
#5009=LINE('',#44324,#6421);
#5010=LINE('',#44326,#6422);
#5011=LINE('',#44330,#6423);
#5012=LINE('',#44332,#6424);
#5013=LINE('',#44333,#6425);
#5014=LINE('',#44336,#6426);
#5015=LINE('',#44337,#6427);
#5016=LINE('',#44340,#6428);
#5017=LINE('',#44341,#6429);
#5018=LINE('',#44344,#6430);
#5019=LINE('',#44345,#6431);
#5020=LINE('',#44348,#6432);
#5021=LINE('',#44349,#6433);
#5022=LINE('',#44352,#6434);
#5023=LINE('',#44353,#6435);
#5024=LINE('',#44356,#6436);
#5025=LINE('',#44357,#6437);
#5026=LINE('',#44360,#6438);
#5027=LINE('',#44361,#6439);
#5028=LINE('',#44364,#6440);
#5029=LINE('',#44365,#6441);
#5030=LINE('',#44368,#6442);
#5031=LINE('',#44369,#6443);
#5032=LINE('',#44372,#6444);
#5033=LINE('',#44373,#6445);
#5034=LINE('',#44376,#6446);
#5035=LINE('',#44377,#6447);
#5036=LINE('',#44380,#6448);
#5037=LINE('',#44381,#6449);
#5038=LINE('',#44383,#6450);
#5039=LINE('',#44387,#6451);
#5040=LINE('',#44389,#6452);
#5041=LINE('',#44390,#6453);
#5042=LINE('',#44393,#6454);
#5043=LINE('',#44394,#6455);
#5044=LINE('',#44397,#6456);
#5045=LINE('',#44398,#6457);
#5046=LINE('',#44401,#6458);
#5047=LINE('',#44402,#6459);
#5048=LINE('',#44405,#6460);
#5049=LINE('',#44406,#6461);
#5050=LINE('',#44409,#6462);
#5051=LINE('',#44410,#6463);
#5052=LINE('',#44413,#6464);
#5053=LINE('',#44414,#6465);
#5054=LINE('',#44417,#6466);
#5055=LINE('',#44418,#6467);
#5056=LINE('',#44421,#6468);
#5057=LINE('',#44422,#6469);
#5058=LINE('',#44425,#6470);
#5059=LINE('',#44426,#6471);
#5060=LINE('',#44429,#6472);
#5061=LINE('',#44430,#6473);
#5062=LINE('',#44433,#6474);
#5063=LINE('',#44434,#6475);
#5064=LINE('',#44437,#6476);
#5065=LINE('',#44438,#6477);
#5066=LINE('',#44440,#6478);
#5067=LINE('',#44444,#6479);
#5068=LINE('',#44446,#6480);
#5069=LINE('',#44447,#6481);
#5070=LINE('',#44450,#6482);
#5071=LINE('',#44451,#6483);
#5072=LINE('',#44454,#6484);
#5073=LINE('',#44455,#6485);
#5074=LINE('',#44458,#6486);
#5075=LINE('',#44459,#6487);
#5076=LINE('',#44462,#6488);
#5077=LINE('',#44463,#6489);
#5078=LINE('',#44466,#6490);
#5079=LINE('',#44467,#6491);
#5080=LINE('',#44470,#6492);
#5081=LINE('',#44471,#6493);
#5082=LINE('',#44474,#6494);
#5083=LINE('',#44475,#6495);
#5084=LINE('',#44478,#6496);
#5085=LINE('',#44479,#6497);
#5086=LINE('',#44482,#6498);
#5087=LINE('',#44483,#6499);
#5088=LINE('',#44486,#6500);
#5089=LINE('',#44487,#6501);
#5090=LINE('',#44490,#6502);
#5091=LINE('',#44491,#6503);
#5092=LINE('',#44494,#6504);
#5093=LINE('',#44495,#6505);
#5094=LINE('',#44497,#6506);
#5095=LINE('',#44501,#6507);
#5096=LINE('',#44503,#6508);
#5097=LINE('',#44504,#6509);
#5098=LINE('',#44507,#6510);
#5099=LINE('',#44508,#6511);
#5100=LINE('',#44511,#6512);
#5101=LINE('',#44512,#6513);
#5102=LINE('',#44515,#6514);
#5103=LINE('',#44516,#6515);
#5104=LINE('',#44519,#6516);
#5105=LINE('',#44520,#6517);
#5106=LINE('',#44523,#6518);
#5107=LINE('',#44524,#6519);
#5108=LINE('',#44527,#6520);
#5109=LINE('',#44528,#6521);
#5110=LINE('',#44531,#6522);
#5111=LINE('',#44532,#6523);
#5112=LINE('',#44535,#6524);
#5113=LINE('',#44536,#6525);
#5114=LINE('',#44539,#6526);
#5115=LINE('',#44540,#6527);
#5116=LINE('',#44543,#6528);
#5117=LINE('',#44544,#6529);
#5118=LINE('',#44547,#6530);
#5119=LINE('',#44548,#6531);
#5120=LINE('',#44551,#6532);
#5121=LINE('',#44552,#6533);
#5122=LINE('',#44554,#6534);
#5123=LINE('',#44558,#6535);
#5124=LINE('',#44560,#6536);
#5125=LINE('',#44561,#6537);
#5126=LINE('',#44564,#6538);
#5127=LINE('',#44565,#6539);
#5128=LINE('',#44568,#6540);
#5129=LINE('',#44569,#6541);
#5130=LINE('',#44572,#6542);
#5131=LINE('',#44573,#6543);
#5132=LINE('',#44576,#6544);
#5133=LINE('',#44577,#6545);
#5134=LINE('',#44580,#6546);
#5135=LINE('',#44581,#6547);
#5136=LINE('',#44584,#6548);
#5137=LINE('',#44585,#6549);
#5138=LINE('',#44588,#6550);
#5139=LINE('',#44589,#6551);
#5140=LINE('',#44592,#6552);
#5141=LINE('',#44593,#6553);
#5142=LINE('',#44596,#6554);
#5143=LINE('',#44597,#6555);
#5144=LINE('',#44600,#6556);
#5145=LINE('',#44601,#6557);
#5146=LINE('',#44604,#6558);
#5147=LINE('',#44605,#6559);
#5148=LINE('',#44608,#6560);
#5149=LINE('',#44609,#6561);
#5150=LINE('',#44611,#6562);
#5151=LINE('',#44615,#6563);
#5152=LINE('',#44617,#6564);
#5153=LINE('',#44618,#6565);
#5154=LINE('',#44621,#6566);
#5155=LINE('',#44622,#6567);
#5156=LINE('',#44625,#6568);
#5157=LINE('',#44626,#6569);
#5158=LINE('',#44629,#6570);
#5159=LINE('',#44630,#6571);
#5160=LINE('',#44633,#6572);
#5161=LINE('',#44634,#6573);
#5162=LINE('',#44637,#6574);
#5163=LINE('',#44638,#6575);
#5164=LINE('',#44641,#6576);
#5165=LINE('',#44642,#6577);
#5166=LINE('',#44645,#6578);
#5167=LINE('',#44646,#6579);
#5168=LINE('',#44649,#6580);
#5169=LINE('',#44650,#6581);
#5170=LINE('',#44653,#6582);
#5171=LINE('',#44654,#6583);
#5172=LINE('',#44657,#6584);
#5173=LINE('',#44658,#6585);
#5174=LINE('',#44661,#6586);
#5175=LINE('',#44662,#6587);
#5176=LINE('',#44665,#6588);
#5177=LINE('',#44666,#6589);
#5178=LINE('',#44668,#6590);
#5179=LINE('',#44672,#6591);
#5180=LINE('',#44674,#6592);
#5181=LINE('',#44675,#6593);
#5182=LINE('',#44678,#6594);
#5183=LINE('',#44679,#6595);
#5184=LINE('',#44682,#6596);
#5185=LINE('',#44683,#6597);
#5186=LINE('',#44686,#6598);
#5187=LINE('',#44687,#6599);
#5188=LINE('',#44690,#6600);
#5189=LINE('',#44691,#6601);
#5190=LINE('',#44694,#6602);
#5191=LINE('',#44695,#6603);
#5192=LINE('',#44698,#6604);
#5193=LINE('',#44699,#6605);
#5194=LINE('',#44702,#6606);
#5195=LINE('',#44703,#6607);
#5196=LINE('',#44706,#6608);
#5197=LINE('',#44707,#6609);
#5198=LINE('',#44710,#6610);
#5199=LINE('',#44711,#6611);
#5200=LINE('',#44714,#6612);
#5201=LINE('',#44715,#6613);
#5202=LINE('',#44718,#6614);
#5203=LINE('',#44719,#6615);
#5204=LINE('',#44722,#6616);
#5205=LINE('',#44723,#6617);
#5206=LINE('',#44725,#6618);
#5207=LINE('',#44729,#6619);
#5208=LINE('',#44731,#6620);
#5209=LINE('',#44732,#6621);
#5210=LINE('',#44735,#6622);
#5211=LINE('',#44736,#6623);
#5212=LINE('',#44739,#6624);
#5213=LINE('',#44740,#6625);
#5214=LINE('',#44743,#6626);
#5215=LINE('',#44744,#6627);
#5216=LINE('',#44747,#6628);
#5217=LINE('',#44748,#6629);
#5218=LINE('',#44751,#6630);
#5219=LINE('',#44752,#6631);
#5220=LINE('',#44755,#6632);
#5221=LINE('',#44756,#6633);
#5222=LINE('',#44759,#6634);
#5223=LINE('',#44760,#6635);
#5224=LINE('',#44763,#6636);
#5225=LINE('',#44764,#6637);
#5226=LINE('',#44767,#6638);
#5227=LINE('',#44768,#6639);
#5228=LINE('',#44771,#6640);
#5229=LINE('',#44772,#6641);
#5230=LINE('',#44775,#6642);
#5231=LINE('',#44776,#6643);
#5232=LINE('',#44779,#6644);
#5233=LINE('',#44780,#6645);
#5234=LINE('',#44782,#6646);
#5235=LINE('',#44786,#6647);
#5236=LINE('',#44788,#6648);
#5237=LINE('',#44789,#6649);
#5238=LINE('',#44792,#6650);
#5239=LINE('',#44793,#6651);
#5240=LINE('',#44796,#6652);
#5241=LINE('',#44797,#6653);
#5242=LINE('',#44800,#6654);
#5243=LINE('',#44801,#6655);
#5244=LINE('',#44804,#6656);
#5245=LINE('',#44805,#6657);
#5246=LINE('',#44808,#6658);
#5247=LINE('',#44809,#6659);
#5248=LINE('',#44812,#6660);
#5249=LINE('',#44813,#6661);
#5250=LINE('',#44816,#6662);
#5251=LINE('',#44817,#6663);
#5252=LINE('',#44820,#6664);
#5253=LINE('',#44821,#6665);
#5254=LINE('',#44824,#6666);
#5255=LINE('',#44825,#6667);
#5256=LINE('',#44828,#6668);
#5257=LINE('',#44829,#6669);
#5258=LINE('',#44832,#6670);
#5259=LINE('',#44833,#6671);
#5260=LINE('',#44836,#6672);
#5261=LINE('',#44837,#6673);
#5262=LINE('',#44839,#6674);
#5263=LINE('',#44843,#6675);
#5264=LINE('',#44845,#6676);
#5265=LINE('',#44846,#6677);
#5266=LINE('',#44849,#6678);
#5267=LINE('',#44850,#6679);
#5268=LINE('',#44853,#6680);
#5269=LINE('',#44854,#6681);
#5270=LINE('',#44857,#6682);
#5271=LINE('',#44858,#6683);
#5272=LINE('',#44861,#6684);
#5273=LINE('',#44862,#6685);
#5274=LINE('',#44865,#6686);
#5275=LINE('',#44866,#6687);
#5276=LINE('',#44869,#6688);
#5277=LINE('',#44870,#6689);
#5278=LINE('',#44873,#6690);
#5279=LINE('',#44874,#6691);
#5280=LINE('',#44877,#6692);
#5281=LINE('',#44878,#6693);
#5282=LINE('',#44881,#6694);
#5283=LINE('',#44882,#6695);
#5284=LINE('',#44885,#6696);
#5285=LINE('',#44886,#6697);
#5286=LINE('',#44889,#6698);
#5287=LINE('',#44890,#6699);
#5288=LINE('',#44893,#6700);
#5289=LINE('',#44894,#6701);
#5290=LINE('',#44896,#6702);
#5291=LINE('',#44900,#6703);
#5292=LINE('',#44902,#6704);
#5293=LINE('',#44903,#6705);
#5294=LINE('',#44906,#6706);
#5295=LINE('',#44907,#6707);
#5296=LINE('',#44910,#6708);
#5297=LINE('',#44911,#6709);
#5298=LINE('',#44914,#6710);
#5299=LINE('',#44915,#6711);
#5300=LINE('',#44918,#6712);
#5301=LINE('',#44919,#6713);
#5302=LINE('',#44922,#6714);
#5303=LINE('',#44923,#6715);
#5304=LINE('',#44926,#6716);
#5305=LINE('',#44927,#6717);
#5306=LINE('',#44930,#6718);
#5307=LINE('',#44931,#6719);
#5308=LINE('',#44934,#6720);
#5309=LINE('',#44935,#6721);
#5310=LINE('',#44938,#6722);
#5311=LINE('',#44939,#6723);
#5312=LINE('',#44942,#6724);
#5313=LINE('',#44943,#6725);
#5314=LINE('',#44946,#6726);
#5315=LINE('',#44947,#6727);
#5316=LINE('',#44950,#6728);
#5317=LINE('',#44951,#6729);
#5318=LINE('',#44953,#6730);
#5319=LINE('',#44956,#6731);
#5320=LINE('',#44957,#6732);
#6198=VECTOR('',#21008,10.);
#6199=VECTOR('',#21009,10.);
#6200=VECTOR('',#21010,10.);
#6201=VECTOR('',#21011,10.);
#6202=VECTOR('',#21014,10.);
#6203=VECTOR('',#21015,10.);
#6204=VECTOR('',#21016,10.);
#6205=VECTOR('',#21021,10.);
#6206=VECTOR('',#21022,10.);
#6207=VECTOR('',#21023,10.);
#6208=VECTOR('',#21026,10.);
#6209=VECTOR('',#21027,10.);
#6210=VECTOR('',#21036,10.);
#6211=VECTOR('',#21037,10.);
#6212=VECTOR('',#21038,10.);
#6213=VECTOR('',#21039,10.);
#6214=VECTOR('',#21040,10.);
#6215=VECTOR('',#21041,10.);
#6216=VECTOR('',#21042,10.);
#6217=VECTOR('',#21043,10.);
#6218=VECTOR('',#21044,10.);
#6219=VECTOR('',#21045,10.);
#6220=VECTOR('',#21046,10.);
#6221=VECTOR('',#21047,10.);
#6222=VECTOR('',#21048,10.);
#6223=VECTOR('',#21049,10.);
#6224=VECTOR('',#21050,10.);
#6225=VECTOR('',#21051,10.);
#6226=VECTOR('',#21052,10.);
#6227=VECTOR('',#21053,10.);
#6228=VECTOR('',#21054,10.);
#6229=VECTOR('',#21055,10.);
#6230=VECTOR('',#21056,10.);
#6231=VECTOR('',#21057,10.);
#6232=VECTOR('',#21058,10.);
#6233=VECTOR('',#21059,10.);
#6234=VECTOR('',#21060,10.);
#6235=VECTOR('',#21061,10.);
#6236=VECTOR('',#21062,10.);
#6237=VECTOR('',#21063,10.);
#6238=VECTOR('',#21064,10.);
#6239=VECTOR('',#21065,10.);
#6240=VECTOR('',#21066,10.);
#6241=VECTOR('',#21067,10.);
#6242=VECTOR('',#21068,10.);
#6243=VECTOR('',#21069,10.);
#6244=VECTOR('',#21070,10.);
#6245=VECTOR('',#21071,10.);
#6246=VECTOR('',#21072,10.);
#6247=VECTOR('',#21073,10.);
#6248=VECTOR('',#21074,10.);
#6249=VECTOR('',#21075,10.);
#6250=VECTOR('',#21076,10.);
#6251=VECTOR('',#21077,10.);
#6252=VECTOR('',#21078,10.);
#6253=VECTOR('',#21079,10.);
#6254=VECTOR('',#21080,10.);
#6255=VECTOR('',#21081,10.);
#6256=VECTOR('',#21082,10.);
#6257=VECTOR('',#21083,10.);
#6258=VECTOR('',#21084,10.);
#6259=VECTOR('',#21085,10.);
#6260=VECTOR('',#21086,10.);
#6261=VECTOR('',#21087,10.);
#6262=VECTOR('',#21088,10.);
#6263=VECTOR('',#21089,10.);
#6264=VECTOR('',#21090,10.);
#6265=VECTOR('',#21091,10.);
#6266=VECTOR('',#21092,10.);
#6267=VECTOR('',#21093,10.);
#6268=VECTOR('',#21094,10.);
#6269=VECTOR('',#21095,10.);
#6270=VECTOR('',#21096,10.);
#6271=VECTOR('',#21097,10.);
#6272=VECTOR('',#21098,10.);
#6273=VECTOR('',#21099,10.);
#6274=VECTOR('',#21100,10.);
#6275=VECTOR('',#21101,10.);
#6276=VECTOR('',#21102,10.);
#6277=VECTOR('',#21103,10.);
#6278=VECTOR('',#21104,10.);
#6279=VECTOR('',#21105,10.);
#6280=VECTOR('',#21106,10.);
#6281=VECTOR('',#21107,10.);
#6282=VECTOR('',#21108,10.);
#6283=VECTOR('',#21109,10.);
#6284=VECTOR('',#21110,10.);
#6285=VECTOR('',#21111,10.);
#6286=VECTOR('',#21112,10.);
#6287=VECTOR('',#21113,10.);
#6288=VECTOR('',#21114,10.);
#6289=VECTOR('',#21115,10.);
#6290=VECTOR('',#21116,10.);
#6291=VECTOR('',#21117,10.);
#6292=VECTOR('',#21118,10.);
#6293=VECTOR('',#21119,10.);
#6294=VECTOR('',#21128,10.);
#6295=VECTOR('',#21129,10.);
#6296=VECTOR('',#21138,10.);
#6297=VECTOR('',#21139,10.);
#6298=VECTOR('',#21142,10.);
#6299=VECTOR('',#21145,10.);
#6300=VECTOR('',#21152,10.);
#6301=VECTOR('',#21153,10.);
#6302=VECTOR('',#21154,10.);
#6303=VECTOR('',#21155,10.);
#6304=VECTOR('',#21156,10.);
#6305=VECTOR('',#21157,10.);
#6306=VECTOR('',#21158,10.);
#6307=VECTOR('',#21159,10.);
#6308=VECTOR('',#21160,10.);
#6309=VECTOR('',#21161,10.);
#6310=VECTOR('',#21162,10.);
#6311=VECTOR('',#21163,10.);
#6312=VECTOR('',#21164,10.);
#6313=VECTOR('',#21165,10.);
#6314=VECTOR('',#21166,10.);
#6315=VECTOR('',#21167,10.);
#6316=VECTOR('',#21168,10.);
#6317=VECTOR('',#21169,10.);
#6318=VECTOR('',#21170,10.);
#6319=VECTOR('',#21171,10.);
#6320=VECTOR('',#21172,10.);
#6321=VECTOR('',#21173,10.);
#6322=VECTOR('',#21174,10.);
#6323=VECTOR('',#21175,10.);
#6324=VECTOR('',#21176,10.);
#6325=VECTOR('',#21177,10.);
#6326=VECTOR('',#21178,10.);
#6327=VECTOR('',#21179,10.);
#6328=VECTOR('',#21180,10.);
#6329=VECTOR('',#21181,10.);
#6330=VECTOR('',#21182,10.);
#6331=VECTOR('',#21183,10.);
#6332=VECTOR('',#21184,10.);
#6333=VECTOR('',#21185,10.);
#6334=VECTOR('',#21186,10.);
#6335=VECTOR('',#21187,10.);
#6336=VECTOR('',#21188,10.);
#6337=VECTOR('',#21189,10.);
#6338=VECTOR('',#21190,10.);
#6339=VECTOR('',#21191,10.);
#6340=VECTOR('',#21192,10.);
#6341=VECTOR('',#21193,10.);
#6342=VECTOR('',#21194,10.);
#6343=VECTOR('',#21195,10.);
#6344=VECTOR('',#21196,10.);
#6345=VECTOR('',#21197,10.);
#6346=VECTOR('',#21198,10.);
#6347=VECTOR('',#21199,10.);
#6348=VECTOR('',#21200,10.);
#6349=VECTOR('',#21201,10.);
#6350=VECTOR('',#21202,10.);
#6351=VECTOR('',#21203,10.);
#6352=VECTOR('',#21204,10.);
#6353=VECTOR('',#21205,10.);
#6354=VECTOR('',#21206,10.);
#6355=VECTOR('',#21207,10.);
#6356=VECTOR('',#21208,10.);
#6357=VECTOR('',#21209,10.);
#6358=VECTOR('',#21210,10.);
#6359=VECTOR('',#21211,10.);
#6360=VECTOR('',#21212,10.);
#6361=VECTOR('',#21213,10.);
#6362=VECTOR('',#21214,10.);
#6363=VECTOR('',#21215,10.);
#6364=VECTOR('',#21216,10.);
#6365=VECTOR('',#21217,10.);
#6366=VECTOR('',#21218,10.);
#6367=VECTOR('',#21219,10.);
#6368=VECTOR('',#21220,10.);
#6369=VECTOR('',#21221,10.);
#6370=VECTOR('',#21222,10.);
#6371=VECTOR('',#21223,10.);
#6372=VECTOR('',#21224,10.);
#6373=VECTOR('',#21225,10.);
#6374=VECTOR('',#21226,10.);
#6375=VECTOR('',#21227,10.);
#6376=VECTOR('',#21228,10.);
#6377=VECTOR('',#21229,10.);
#6378=VECTOR('',#21230,10.);
#6379=VECTOR('',#21231,10.);
#6380=VECTOR('',#21232,10.);
#6381=VECTOR('',#21233,10.);
#6382=VECTOR('',#21234,10.);
#6383=VECTOR('',#21235,10.);
#6384=VECTOR('',#21242,2.75);
#6385=VECTOR('',#21247,2.65);
#6386=VECTOR('',#21252,2.75);
#6387=VECTOR('',#21255,2.75);
#6388=VECTOR('',#21260,2.65);
#6389=VECTOR('',#21265,2.75);
#6390=VECTOR('',#21268,2.75);
#6391=VECTOR('',#21273,2.65);
#6392=VECTOR('',#21278,2.75);
#6393=VECTOR('',#21281,1.1);
#6394=VECTOR('',#21286,1.);
#6395=VECTOR('',#21289,10.);
#6396=VECTOR('',#21290,10.);
#6397=VECTOR('',#21291,10.);
#6398=VECTOR('',#21294,10.);
#6399=VECTOR('',#21295,10.);
#6400=VECTOR('',#21298,10.);
#6401=VECTOR('',#21299,10.);
#6402=VECTOR('',#21302,10.);
#6403=VECTOR('',#21303,10.);
#6404=VECTOR('',#21306,10.);
#6405=VECTOR('',#21307,10.);
#6406=VECTOR('',#21310,10.);
#6407=VECTOR('',#21311,10.);
#6408=VECTOR('',#21314,10.);
#6409=VECTOR('',#21315,10.);
#6410=VECTOR('',#21318,10.);
#6411=VECTOR('',#21319,10.);
#6412=VECTOR('',#21322,10.);
#6413=VECTOR('',#21323,10.);
#6414=VECTOR('',#21326,10.);
#6415=VECTOR('',#21327,10.);
#6416=VECTOR('',#21330,10.);
#6417=VECTOR('',#21331,10.);
#6418=VECTOR('',#21334,10.);
#6419=VECTOR('',#21335,10.);
#6420=VECTOR('',#21338,10.);
#6421=VECTOR('',#21339,10.);
#6422=VECTOR('',#21342,10.);
#6423=VECTOR('',#21347,10.);
#6424=VECTOR('',#21348,10.);
#6425=VECTOR('',#21349,10.);
#6426=VECTOR('',#21352,10.);
#6427=VECTOR('',#21353,10.);
#6428=VECTOR('',#21356,10.);
#6429=VECTOR('',#21357,10.);
#6430=VECTOR('',#21360,10.);
#6431=VECTOR('',#21361,10.);
#6432=VECTOR('',#21364,10.);
#6433=VECTOR('',#21365,10.);
#6434=VECTOR('',#21368,10.);
#6435=VECTOR('',#21369,10.);
#6436=VECTOR('',#21372,10.);
#6437=VECTOR('',#21373,10.);
#6438=VECTOR('',#21376,10.);
#6439=VECTOR('',#21377,10.);
#6440=VECTOR('',#21380,10.);
#6441=VECTOR('',#21381,10.);
#6442=VECTOR('',#21384,10.);
#6443=VECTOR('',#21385,10.);
#6444=VECTOR('',#21388,10.);
#6445=VECTOR('',#21389,10.);
#6446=VECTOR('',#21392,10.);
#6447=VECTOR('',#21393,10.);
#6448=VECTOR('',#21396,10.);
#6449=VECTOR('',#21397,10.);
#6450=VECTOR('',#21400,10.);
#6451=VECTOR('',#21405,10.);
#6452=VECTOR('',#21406,10.);
#6453=VECTOR('',#21407,10.);
#6454=VECTOR('',#21410,10.);
#6455=VECTOR('',#21411,10.);
#6456=VECTOR('',#21414,10.);
#6457=VECTOR('',#21415,10.);
#6458=VECTOR('',#21418,10.);
#6459=VECTOR('',#21419,10.);
#6460=VECTOR('',#21422,10.);
#6461=VECTOR('',#21423,10.);
#6462=VECTOR('',#21426,10.);
#6463=VECTOR('',#21427,10.);
#6464=VECTOR('',#21430,10.);
#6465=VECTOR('',#21431,10.);
#6466=VECTOR('',#21434,10.);
#6467=VECTOR('',#21435,10.);
#6468=VECTOR('',#21438,10.);
#6469=VECTOR('',#21439,10.);
#6470=VECTOR('',#21442,10.);
#6471=VECTOR('',#21443,10.);
#6472=VECTOR('',#21446,10.);
#6473=VECTOR('',#21447,10.);
#6474=VECTOR('',#21450,10.);
#6475=VECTOR('',#21451,10.);
#6476=VECTOR('',#21454,10.);
#6477=VECTOR('',#21455,10.);
#6478=VECTOR('',#21458,10.);
#6479=VECTOR('',#21463,10.);
#6480=VECTOR('',#21464,10.);
#6481=VECTOR('',#21465,10.);
#6482=VECTOR('',#21468,10.);
#6483=VECTOR('',#21469,10.);
#6484=VECTOR('',#21472,10.);
#6485=VECTOR('',#21473,10.);
#6486=VECTOR('',#21476,10.);
#6487=VECTOR('',#21477,10.);
#6488=VECTOR('',#21480,10.);
#6489=VECTOR('',#21481,10.);
#6490=VECTOR('',#21484,10.);
#6491=VECTOR('',#21485,10.);
#6492=VECTOR('',#21488,10.);
#6493=VECTOR('',#21489,10.);
#6494=VECTOR('',#21492,10.);
#6495=VECTOR('',#21493,10.);
#6496=VECTOR('',#21496,10.);
#6497=VECTOR('',#21497,10.);
#6498=VECTOR('',#21500,10.);
#6499=VECTOR('',#21501,10.);
#6500=VECTOR('',#21504,10.);
#6501=VECTOR('',#21505,10.);
#6502=VECTOR('',#21508,10.);
#6503=VECTOR('',#21509,10.);
#6504=VECTOR('',#21512,10.);
#6505=VECTOR('',#21513,10.);
#6506=VECTOR('',#21516,10.);
#6507=VECTOR('',#21521,10.);
#6508=VECTOR('',#21522,10.);
#6509=VECTOR('',#21523,10.);
#6510=VECTOR('',#21526,10.);
#6511=VECTOR('',#21527,10.);
#6512=VECTOR('',#21530,10.);
#6513=VECTOR('',#21531,10.);
#6514=VECTOR('',#21534,10.);
#6515=VECTOR('',#21535,10.);
#6516=VECTOR('',#21538,10.);
#6517=VECTOR('',#21539,10.);
#6518=VECTOR('',#21542,10.);
#6519=VECTOR('',#21543,10.);
#6520=VECTOR('',#21546,10.);
#6521=VECTOR('',#21547,10.);
#6522=VECTOR('',#21550,10.);
#6523=VECTOR('',#21551,10.);
#6524=VECTOR('',#21554,10.);
#6525=VECTOR('',#21555,10.);
#6526=VECTOR('',#21558,10.);
#6527=VECTOR('',#21559,10.);
#6528=VECTOR('',#21562,10.);
#6529=VECTOR('',#21563,10.);
#6530=VECTOR('',#21566,10.);
#6531=VECTOR('',#21567,10.);
#6532=VECTOR('',#21570,10.);
#6533=VECTOR('',#21571,10.);
#6534=VECTOR('',#21574,10.);
#6535=VECTOR('',#21579,10.);
#6536=VECTOR('',#21580,10.);
#6537=VECTOR('',#21581,10.);
#6538=VECTOR('',#21584,10.);
#6539=VECTOR('',#21585,10.);
#6540=VECTOR('',#21588,10.);
#6541=VECTOR('',#21589,10.);
#6542=VECTOR('',#21592,10.);
#6543=VECTOR('',#21593,10.);
#6544=VECTOR('',#21596,10.);
#6545=VECTOR('',#21597,10.);
#6546=VECTOR('',#21600,10.);
#6547=VECTOR('',#21601,10.);
#6548=VECTOR('',#21604,10.);
#6549=VECTOR('',#21605,10.);
#6550=VECTOR('',#21608,10.);
#6551=VECTOR('',#21609,10.);
#6552=VECTOR('',#21612,10.);
#6553=VECTOR('',#21613,10.);
#6554=VECTOR('',#21616,10.);
#6555=VECTOR('',#21617,10.);
#6556=VECTOR('',#21620,10.);
#6557=VECTOR('',#21621,10.);
#6558=VECTOR('',#21624,10.);
#6559=VECTOR('',#21625,10.);
#6560=VECTOR('',#21628,10.);
#6561=VECTOR('',#21629,10.);
#6562=VECTOR('',#21632,10.);
#6563=VECTOR('',#21637,10.);
#6564=VECTOR('',#21638,10.);
#6565=VECTOR('',#21639,10.);
#6566=VECTOR('',#21642,10.);
#6567=VECTOR('',#21643,10.);
#6568=VECTOR('',#21646,10.);
#6569=VECTOR('',#21647,10.);
#6570=VECTOR('',#21650,10.);
#6571=VECTOR('',#21651,10.);
#6572=VECTOR('',#21654,10.);
#6573=VECTOR('',#21655,10.);
#6574=VECTOR('',#21658,10.);
#6575=VECTOR('',#21659,10.);
#6576=VECTOR('',#21662,10.);
#6577=VECTOR('',#21663,10.);
#6578=VECTOR('',#21666,10.);
#6579=VECTOR('',#21667,10.);
#6580=VECTOR('',#21670,10.);
#6581=VECTOR('',#21671,10.);
#6582=VECTOR('',#21674,10.);
#6583=VECTOR('',#21675,10.);
#6584=VECTOR('',#21678,10.);
#6585=VECTOR('',#21679,10.);
#6586=VECTOR('',#21682,10.);
#6587=VECTOR('',#21683,10.);
#6588=VECTOR('',#21686,10.);
#6589=VECTOR('',#21687,10.);
#6590=VECTOR('',#21690,10.);
#6591=VECTOR('',#21695,10.);
#6592=VECTOR('',#21696,10.);
#6593=VECTOR('',#21697,10.);
#6594=VECTOR('',#21700,10.);
#6595=VECTOR('',#21701,10.);
#6596=VECTOR('',#21704,10.);
#6597=VECTOR('',#21705,10.);
#6598=VECTOR('',#21708,10.);
#6599=VECTOR('',#21709,10.);
#6600=VECTOR('',#21712,10.);
#6601=VECTOR('',#21713,10.);
#6602=VECTOR('',#21716,10.);
#6603=VECTOR('',#21717,10.);
#6604=VECTOR('',#21720,10.);
#6605=VECTOR('',#21721,10.);
#6606=VECTOR('',#21724,10.);
#6607=VECTOR('',#21725,10.);
#6608=VECTOR('',#21728,10.);
#6609=VECTOR('',#21729,10.);
#6610=VECTOR('',#21732,10.);
#6611=VECTOR('',#21733,10.);
#6612=VECTOR('',#21736,10.);
#6613=VECTOR('',#21737,10.);
#6614=VECTOR('',#21740,10.);
#6615=VECTOR('',#21741,10.);
#6616=VECTOR('',#21744,10.);
#6617=VECTOR('',#21745,10.);
#6618=VECTOR('',#21748,10.);
#6619=VECTOR('',#21753,10.);
#6620=VECTOR('',#21754,10.);
#6621=VECTOR('',#21755,10.);
#6622=VECTOR('',#21758,10.);
#6623=VECTOR('',#21759,10.);
#6624=VECTOR('',#21762,10.);
#6625=VECTOR('',#21763,10.);
#6626=VECTOR('',#21766,10.);
#6627=VECTOR('',#21767,10.);
#6628=VECTOR('',#21770,10.);
#6629=VECTOR('',#21771,10.);
#6630=VECTOR('',#21774,10.);
#6631=VECTOR('',#21775,10.);
#6632=VECTOR('',#21778,10.);
#6633=VECTOR('',#21779,10.);
#6634=VECTOR('',#21782,10.);
#6635=VECTOR('',#21783,10.);
#6636=VECTOR('',#21786,10.);
#6637=VECTOR('',#21787,10.);
#6638=VECTOR('',#21790,10.);
#6639=VECTOR('',#21791,10.);
#6640=VECTOR('',#21794,10.);
#6641=VECTOR('',#21795,10.);
#6642=VECTOR('',#21798,10.);
#6643=VECTOR('',#21799,10.);
#6644=VECTOR('',#21802,10.);
#6645=VECTOR('',#21803,10.);
#6646=VECTOR('',#21806,10.);
#6647=VECTOR('',#21811,10.);
#6648=VECTOR('',#21812,10.);
#6649=VECTOR('',#21813,10.);
#6650=VECTOR('',#21816,10.);
#6651=VECTOR('',#21817,10.);
#6652=VECTOR('',#21820,10.);
#6653=VECTOR('',#21821,10.);
#6654=VECTOR('',#21824,10.);
#6655=VECTOR('',#21825,10.);
#6656=VECTOR('',#21828,10.);
#6657=VECTOR('',#21829,10.);
#6658=VECTOR('',#21832,10.);
#6659=VECTOR('',#21833,10.);
#6660=VECTOR('',#21836,10.);
#6661=VECTOR('',#21837,10.);
#6662=VECTOR('',#21840,10.);
#6663=VECTOR('',#21841,10.);
#6664=VECTOR('',#21844,10.);
#6665=VECTOR('',#21845,10.);
#6666=VECTOR('',#21848,10.);
#6667=VECTOR('',#21849,10.);
#6668=VECTOR('',#21852,10.);
#6669=VECTOR('',#21853,10.);
#6670=VECTOR('',#21856,10.);
#6671=VECTOR('',#21857,10.);
#6672=VECTOR('',#21860,10.);
#6673=VECTOR('',#21861,10.);
#6674=VECTOR('',#21864,10.);
#6675=VECTOR('',#21869,10.);
#6676=VECTOR('',#21870,10.);
#6677=VECTOR('',#21871,10.);
#6678=VECTOR('',#21874,10.);
#6679=VECTOR('',#21875,10.);
#6680=VECTOR('',#21878,10.);
#6681=VECTOR('',#21879,10.);
#6682=VECTOR('',#21882,10.);
#6683=VECTOR('',#21883,10.);
#6684=VECTOR('',#21886,10.);
#6685=VECTOR('',#21887,10.);
#6686=VECTOR('',#21890,10.);
#6687=VECTOR('',#21891,10.);
#6688=VECTOR('',#21894,10.);
#6689=VECTOR('',#21895,10.);
#6690=VECTOR('',#21898,10.);
#6691=VECTOR('',#21899,10.);
#6692=VECTOR('',#21902,10.);
#6693=VECTOR('',#21903,10.);
#6694=VECTOR('',#21906,10.);
#6695=VECTOR('',#21907,10.);
#6696=VECTOR('',#21910,10.);
#6697=VECTOR('',#21911,10.);
#6698=VECTOR('',#21914,10.);
#6699=VECTOR('',#21915,10.);
#6700=VECTOR('',#21918,10.);
#6701=VECTOR('',#21919,10.);
#6702=VECTOR('',#21922,10.);
#6703=VECTOR('',#21927,10.);
#6704=VECTOR('',#21928,10.);
#6705=VECTOR('',#21929,10.);
#6706=VECTOR('',#21932,10.);
#6707=VECTOR('',#21933,10.);
#6708=VECTOR('',#21936,10.);
#6709=VECTOR('',#21937,10.);
#6710=VECTOR('',#21940,10.);
#6711=VECTOR('',#21941,10.);
#6712=VECTOR('',#21944,10.);
#6713=VECTOR('',#21945,10.);
#6714=VECTOR('',#21948,10.);
#6715=VECTOR('',#21949,10.);
#6716=VECTOR('',#21952,10.);
#6717=VECTOR('',#21953,10.);
#6718=VECTOR('',#21956,10.);
#6719=VECTOR('',#21957,10.);
#6720=VECTOR('',#21960,10.);
#6721=VECTOR('',#21961,10.);
#6722=VECTOR('',#21964,10.);
#6723=VECTOR('',#21965,10.);
#6724=VECTOR('',#21968,10.);
#6725=VECTOR('',#21969,10.);
#6726=VECTOR('',#21972,10.);
#6727=VECTOR('',#21973,10.);
#6728=VECTOR('',#21976,10.);
#6729=VECTOR('',#21977,10.);
#6730=VECTOR('',#21980,10.);
#6731=VECTOR('',#21985,5.85);
#6732=VECTOR('',#21986,5.85);
#7962=VERTEX_POINT('',#43760);
#7963=VERTEX_POINT('',#43761);
#7964=VERTEX_POINT('',#43763);
#7965=VERTEX_POINT('',#43765);
#7966=VERTEX_POINT('',#43769);
#7967=VERTEX_POINT('',#43771);
#7968=VERTEX_POINT('',#43774);
#7969=VERTEX_POINT('',#43777);
#7970=VERTEX_POINT('',#43779);
#7971=VERTEX_POINT('',#43783);
#7972=VERTEX_POINT('',#43785);
#7973=VERTEX_POINT('',#43788);
#7974=VERTEX_POINT('',#43790);
#7975=VERTEX_POINT('',#43792);
#7976=VERTEX_POINT('',#43794);
#7977=VERTEX_POINT('',#43795);
#7978=VERTEX_POINT('',#43797);
#7979=VERTEX_POINT('',#43799);
#7980=VERTEX_POINT('',#43801);
#7981=VERTEX_POINT('',#43803);
#7982=VERTEX_POINT('',#43805);
#7983=VERTEX_POINT('',#43807);
#7984=VERTEX_POINT('',#43809);
#7985=VERTEX_POINT('',#43811);
#7986=VERTEX_POINT('',#43813);
#7987=VERTEX_POINT('',#43815);
#7988=VERTEX_POINT('',#43817);
#7989=VERTEX_POINT('',#43819);
#7990=VERTEX_POINT('',#43822);
#7991=VERTEX_POINT('',#43823);
#7992=VERTEX_POINT('',#43825);
#7993=VERTEX_POINT('',#43827);
#7994=VERTEX_POINT('',#43829);
#7995=VERTEX_POINT('',#43831);
#7996=VERTEX_POINT('',#43833);
#7997=VERTEX_POINT('',#43835);
#7998=VERTEX_POINT('',#43837);
#7999=VERTEX_POINT('',#43839);
#8000=VERTEX_POINT('',#43841);
#8001=VERTEX_POINT('',#43843);
#8002=VERTEX_POINT('',#43845);
#8003=VERTEX_POINT('',#43847);
#8004=VERTEX_POINT('',#43850);
#8005=VERTEX_POINT('',#43851);
#8006=VERTEX_POINT('',#43853);
#8007=VERTEX_POINT('',#43855);
#8008=VERTEX_POINT('',#43857);
#8009=VERTEX_POINT('',#43859);
#8010=VERTEX_POINT('',#43861);
#8011=VERTEX_POINT('',#43863);
#8012=VERTEX_POINT('',#43865);
#8013=VERTEX_POINT('',#43867);
#8014=VERTEX_POINT('',#43869);
#8015=VERTEX_POINT('',#43871);
#8016=VERTEX_POINT('',#43873);
#8017=VERTEX_POINT('',#43875);
#8018=VERTEX_POINT('',#43878);
#8019=VERTEX_POINT('',#43879);
#8020=VERTEX_POINT('',#43881);
#8021=VERTEX_POINT('',#43883);
#8022=VERTEX_POINT('',#43885);
#8023=VERTEX_POINT('',#43887);
#8024=VERTEX_POINT('',#43889);
#8025=VERTEX_POINT('',#43891);
#8026=VERTEX_POINT('',#43893);
#8027=VERTEX_POINT('',#43895);
#8028=VERTEX_POINT('',#43897);
#8029=VERTEX_POINT('',#43899);
#8030=VERTEX_POINT('',#43901);
#8031=VERTEX_POINT('',#43903);
#8032=VERTEX_POINT('',#43906);
#8033=VERTEX_POINT('',#43907);
#8034=VERTEX_POINT('',#43909);
#8035=VERTEX_POINT('',#43911);
#8036=VERTEX_POINT('',#43913);
#8037=VERTEX_POINT('',#43915);
#8038=VERTEX_POINT('',#43917);
#8039=VERTEX_POINT('',#43919);
#8040=VERTEX_POINT('',#43921);
#8041=VERTEX_POINT('',#43923);
#8042=VERTEX_POINT('',#43925);
#8043=VERTEX_POINT('',#43927);
#8044=VERTEX_POINT('',#43929);
#8045=VERTEX_POINT('',#43931);
#8046=VERTEX_POINT('',#43934);
#8047=VERTEX_POINT('',#43935);
#8048=VERTEX_POINT('',#43937);
#8049=VERTEX_POINT('',#43939);
#8050=VERTEX_POINT('',#43941);
#8051=VERTEX_POINT('',#43943);
#8052=VERTEX_POINT('',#43945);
#8053=VERTEX_POINT('',#43947);
#8054=VERTEX_POINT('',#43949);
#8055=VERTEX_POINT('',#43951);
#8056=VERTEX_POINT('',#43953);
#8057=VERTEX_POINT('',#43955);
#8058=VERTEX_POINT('',#43957);
#8059=VERTEX_POINT('',#43959);
#8060=VERTEX_POINT('',#43962);
#8061=VERTEX_POINT('',#43965);
#8062=VERTEX_POINT('',#43969);
#8063=VERTEX_POINT('',#43974);
#8064=VERTEX_POINT('',#43976);
#8065=VERTEX_POINT('',#43985);
#8066=VERTEX_POINT('',#43987);
#8067=VERTEX_POINT('',#43994);
#8068=VERTEX_POINT('',#43996);
#8069=VERTEX_POINT('',#44000);
#8070=VERTEX_POINT('',#44002);
#8071=VERTEX_POINT('',#44017);
#8072=VERTEX_POINT('',#44019);
#8073=VERTEX_POINT('',#44021);
#8074=VERTEX_POINT('',#44023);
#8075=VERTEX_POINT('',#44024);
#8076=VERTEX_POINT('',#44026);
#8077=VERTEX_POINT('',#44028);
#8078=VERTEX_POINT('',#44030);
#8079=VERTEX_POINT('',#44032);
#8080=VERTEX_POINT('',#44034);
#8081=VERTEX_POINT('',#44036);
#8082=VERTEX_POINT('',#44038);
#8083=VERTEX_POINT('',#44040);
#8084=VERTEX_POINT('',#44042);
#8085=VERTEX_POINT('',#44044);
#8086=VERTEX_POINT('',#44046);
#8087=VERTEX_POINT('',#44048);
#8088=VERTEX_POINT('',#44051);
#8089=VERTEX_POINT('',#44052);
#8090=VERTEX_POINT('',#44054);
#8091=VERTEX_POINT('',#44056);
#8092=VERTEX_POINT('',#44058);
#8093=VERTEX_POINT('',#44060);
#8094=VERTEX_POINT('',#44062);
#8095=VERTEX_POINT('',#44064);
#8096=VERTEX_POINT('',#44066);
#8097=VERTEX_POINT('',#44068);
#8098=VERTEX_POINT('',#44070);
#8099=VERTEX_POINT('',#44072);
#8100=VERTEX_POINT('',#44074);
#8101=VERTEX_POINT('',#44076);
#8102=VERTEX_POINT('',#44079);
#8103=VERTEX_POINT('',#44080);
#8104=VERTEX_POINT('',#44082);
#8105=VERTEX_POINT('',#44084);
#8106=VERTEX_POINT('',#44086);
#8107=VERTEX_POINT('',#44088);
#8108=VERTEX_POINT('',#44090);
#8109=VERTEX_POINT('',#44092);
#8110=VERTEX_POINT('',#44094);
#8111=VERTEX_POINT('',#44096);
#8112=VERTEX_POINT('',#44098);
#8113=VERTEX_POINT('',#44100);
#8114=VERTEX_POINT('',#44102);
#8115=VERTEX_POINT('',#44104);
#8116=VERTEX_POINT('',#44107);
#8117=VERTEX_POINT('',#44108);
#8118=VERTEX_POINT('',#44110);
#8119=VERTEX_POINT('',#44112);
#8120=VERTEX_POINT('',#44114);
#8121=VERTEX_POINT('',#44116);
#8122=VERTEX_POINT('',#44118);
#8123=VERTEX_POINT('',#44120);
#8124=VERTEX_POINT('',#44122);
#8125=VERTEX_POINT('',#44124);
#8126=VERTEX_POINT('',#44126);
#8127=VERTEX_POINT('',#44128);
#8128=VERTEX_POINT('',#44130);
#8129=VERTEX_POINT('',#44132);
#8130=VERTEX_POINT('',#44135);
#8131=VERTEX_POINT('',#44136);
#8132=VERTEX_POINT('',#44138);
#8133=VERTEX_POINT('',#44140);
#8134=VERTEX_POINT('',#44142);
#8135=VERTEX_POINT('',#44144);
#8136=VERTEX_POINT('',#44146);
#8137=VERTEX_POINT('',#44148);
#8138=VERTEX_POINT('',#44150);
#8139=VERTEX_POINT('',#44152);
#8140=VERTEX_POINT('',#44154);
#8141=VERTEX_POINT('',#44156);
#8142=VERTEX_POINT('',#44158);
#8143=VERTEX_POINT('',#44160);
#8144=VERTEX_POINT('',#44163);
#8145=VERTEX_POINT('',#44164);
#8146=VERTEX_POINT('',#44166);
#8147=VERTEX_POINT('',#44168);
#8148=VERTEX_POINT('',#44170);
#8149=VERTEX_POINT('',#44172);
#8150=VERTEX_POINT('',#44174);
#8151=VERTEX_POINT('',#44176);
#8152=VERTEX_POINT('',#44178);
#8153=VERTEX_POINT('',#44180);
#8154=VERTEX_POINT('',#44182);
#8155=VERTEX_POINT('',#44184);
#8156=VERTEX_POINT('',#44186);
#8157=VERTEX_POINT('',#44188);
#8158=VERTEX_POINT('',#44191);
#8159=VERTEX_POINT('',#44195);
#8160=VERTEX_POINT('',#44199);
#8161=VERTEX_POINT('',#44205);
#8162=VERTEX_POINT('',#44209);
#8163=VERTEX_POINT('',#44215);
#8164=VERTEX_POINT('',#44219);
#8165=VERTEX_POINT('',#44225);
#8166=VERTEX_POINT('',#44229);
#8167=VERTEX_POINT('',#44231);
#8168=VERTEX_POINT('',#44242);
#8169=VERTEX_POINT('',#44272);
#8170=VERTEX_POINT('',#44274);
#8171=VERTEX_POINT('',#44278);
#8172=VERTEX_POINT('',#44282);
#8173=VERTEX_POINT('',#44286);
#8174=VERTEX_POINT('',#44290);
#8175=VERTEX_POINT('',#44294);
#8176=VERTEX_POINT('',#44298);
#8177=VERTEX_POINT('',#44302);
#8178=VERTEX_POINT('',#44306);
#8179=VERTEX_POINT('',#44310);
#8180=VERTEX_POINT('',#44314);
#8181=VERTEX_POINT('',#44318);
#8182=VERTEX_POINT('',#44322);
#8183=VERTEX_POINT('',#44329);
#8184=VERTEX_POINT('',#44331);
#8185=VERTEX_POINT('',#44335);
#8186=VERTEX_POINT('',#44339);
#8187=VERTEX_POINT('',#44343);
#8188=VERTEX_POINT('',#44347);
#8189=VERTEX_POINT('',#44351);
#8190=VERTEX_POINT('',#44355);
#8191=VERTEX_POINT('',#44359);
#8192=VERTEX_POINT('',#44363);
#8193=VERTEX_POINT('',#44367);
#8194=VERTEX_POINT('',#44371);
#8195=VERTEX_POINT('',#44375);
#8196=VERTEX_POINT('',#44379);
#8197=VERTEX_POINT('',#44386);
#8198=VERTEX_POINT('',#44388);
#8199=VERTEX_POINT('',#44392);
#8200=VERTEX_POINT('',#44396);
#8201=VERTEX_POINT('',#44400);
#8202=VERTEX_POINT('',#44404);
#8203=VERTEX_POINT('',#44408);
#8204=VERTEX_POINT('',#44412);
#8205=VERTEX_POINT('',#44416);
#8206=VERTEX_POINT('',#44420);
#8207=VERTEX_POINT('',#44424);
#8208=VERTEX_POINT('',#44428);
#8209=VERTEX_POINT('',#44432);
#8210=VERTEX_POINT('',#44436);
#8211=VERTEX_POINT('',#44443);
#8212=VERTEX_POINT('',#44445);
#8213=VERTEX_POINT('',#44449);
#8214=VERTEX_POINT('',#44453);
#8215=VERTEX_POINT('',#44457);
#8216=VERTEX_POINT('',#44461);
#8217=VERTEX_POINT('',#44465);
#8218=VERTEX_POINT('',#44469);
#8219=VERTEX_POINT('',#44473);
#8220=VERTEX_POINT('',#44477);
#8221=VERTEX_POINT('',#44481);
#8222=VERTEX_POINT('',#44485);
#8223=VERTEX_POINT('',#44489);
#8224=VERTEX_POINT('',#44493);
#8225=VERTEX_POINT('',#44500);
#8226=VERTEX_POINT('',#44502);
#8227=VERTEX_POINT('',#44506);
#8228=VERTEX_POINT('',#44510);
#8229=VERTEX_POINT('',#44514);
#8230=VERTEX_POINT('',#44518);
#8231=VERTEX_POINT('',#44522);
#8232=VERTEX_POINT('',#44526);
#8233=VERTEX_POINT('',#44530);
#8234=VERTEX_POINT('',#44534);
#8235=VERTEX_POINT('',#44538);
#8236=VERTEX_POINT('',#44542);
#8237=VERTEX_POINT('',#44546);
#8238=VERTEX_POINT('',#44550);
#8239=VERTEX_POINT('',#44557);
#8240=VERTEX_POINT('',#44559);
#8241=VERTEX_POINT('',#44563);
#8242=VERTEX_POINT('',#44567);
#8243=VERTEX_POINT('',#44571);
#8244=VERTEX_POINT('',#44575);
#8245=VERTEX_POINT('',#44579);
#8246=VERTEX_POINT('',#44583);
#8247=VERTEX_POINT('',#44587);
#8248=VERTEX_POINT('',#44591);
#8249=VERTEX_POINT('',#44595);
#8250=VERTEX_POINT('',#44599);
#8251=VERTEX_POINT('',#44603);
#8252=VERTEX_POINT('',#44607);
#8253=VERTEX_POINT('',#44614);
#8254=VERTEX_POINT('',#44616);
#8255=VERTEX_POINT('',#44620);
#8256=VERTEX_POINT('',#44624);
#8257=VERTEX_POINT('',#44628);
#8258=VERTEX_POINT('',#44632);
#8259=VERTEX_POINT('',#44636);
#8260=VERTEX_POINT('',#44640);
#8261=VERTEX_POINT('',#44644);
#8262=VERTEX_POINT('',#44648);
#8263=VERTEX_POINT('',#44652);
#8264=VERTEX_POINT('',#44656);
#8265=VERTEX_POINT('',#44660);
#8266=VERTEX_POINT('',#44664);
#8267=VERTEX_POINT('',#44671);
#8268=VERTEX_POINT('',#44673);
#8269=VERTEX_POINT('',#44677);
#8270=VERTEX_POINT('',#44681);
#8271=VERTEX_POINT('',#44685);
#8272=VERTEX_POINT('',#44689);
#8273=VERTEX_POINT('',#44693);
#8274=VERTEX_POINT('',#44697);
#8275=VERTEX_POINT('',#44701);
#8276=VERTEX_POINT('',#44705);
#8277=VERTEX_POINT('',#44709);
#8278=VERTEX_POINT('',#44713);
#8279=VERTEX_POINT('',#44717);
#8280=VERTEX_POINT('',#44721);
#8281=VERTEX_POINT('',#44728);
#8282=VERTEX_POINT('',#44730);
#8283=VERTEX_POINT('',#44734);
#8284=VERTEX_POINT('',#44738);
#8285=VERTEX_POINT('',#44742);
#8286=VERTEX_POINT('',#44746);
#8287=VERTEX_POINT('',#44750);
#8288=VERTEX_POINT('',#44754);
#8289=VERTEX_POINT('',#44758);
#8290=VERTEX_POINT('',#44762);
#8291=VERTEX_POINT('',#44766);
#8292=VERTEX_POINT('',#44770);
#8293=VERTEX_POINT('',#44774);
#8294=VERTEX_POINT('',#44778);
#8295=VERTEX_POINT('',#44785);
#8296=VERTEX_POINT('',#44787);
#8297=VERTEX_POINT('',#44791);
#8298=VERTEX_POINT('',#44795);
#8299=VERTEX_POINT('',#44799);
#8300=VERTEX_POINT('',#44803);
#8301=VERTEX_POINT('',#44807);
#8302=VERTEX_POINT('',#44811);
#8303=VERTEX_POINT('',#44815);
#8304=VERTEX_POINT('',#44819);
#8305=VERTEX_POINT('',#44823);
#8306=VERTEX_POINT('',#44827);
#8307=VERTEX_POINT('',#44831);
#8308=VERTEX_POINT('',#44835);
#8309=VERTEX_POINT('',#44842);
#8310=VERTEX_POINT('',#44844);
#8311=VERTEX_POINT('',#44848);
#8312=VERTEX_POINT('',#44852);
#8313=VERTEX_POINT('',#44856);
#8314=VERTEX_POINT('',#44860);
#8315=VERTEX_POINT('',#44864);
#8316=VERTEX_POINT('',#44868);
#8317=VERTEX_POINT('',#44872);
#8318=VERTEX_POINT('',#44876);
#8319=VERTEX_POINT('',#44880);
#8320=VERTEX_POINT('',#44884);
#8321=VERTEX_POINT('',#44888);
#8322=VERTEX_POINT('',#44892);
#8323=VERTEX_POINT('',#44899);
#8324=VERTEX_POINT('',#44901);
#8325=VERTEX_POINT('',#44905);
#8326=VERTEX_POINT('',#44909);
#8327=VERTEX_POINT('',#44913);
#8328=VERTEX_POINT('',#44917);
#8329=VERTEX_POINT('',#44921);
#8330=VERTEX_POINT('',#44925);
#8331=VERTEX_POINT('',#44929);
#8332=VERTEX_POINT('',#44933);
#8333=VERTEX_POINT('',#44937);
#8334=VERTEX_POINT('',#44941);
#8335=VERTEX_POINT('',#44945);
#8336=VERTEX_POINT('',#44949);
#10083=EDGE_CURVE('',#7962,#7963,#4786,.F.);
#10084=EDGE_CURVE('',#7963,#7964,#4787,.T.);
#10085=EDGE_CURVE('',#7964,#7965,#4788,.F.);
#10086=EDGE_CURVE('',#7965,#7962,#4789,.T.);
#10087=EDGE_CURVE('',#7966,#7963,#4790,.T.);
#10088=EDGE_CURVE('',#7967,#7966,#4791,.T.);
#10089=EDGE_CURVE('',#7967,#7964,#4792,.T.);
#10090=EDGE_CURVE('',#7968,#7968,#3517,.T.);
#10091=EDGE_CURVE('',#7966,#7969,#4793,.F.);
#10092=EDGE_CURVE('',#7969,#7970,#4794,.T.);
#10093=EDGE_CURVE('',#7970,#7967,#4795,.F.);
#10094=EDGE_CURVE('',#7970,#7971,#4796,.T.);
#10095=EDGE_CURVE('',#7972,#7969,#4797,.T.);
#10096=EDGE_CURVE('',#7971,#7972,#3518,.T.);
#10097=EDGE_CURVE('',#7973,#7973,#3519,.T.);
#10098=EDGE_CURVE('',#7974,#7974,#3520,.T.);
#10099=EDGE_CURVE('',#7975,#7975,#3521,.T.);
#10100=EDGE_CURVE('',#7976,#7977,#4798,.T.);
#10101=EDGE_CURVE('',#7977,#7978,#4799,.T.);
#10102=EDGE_CURVE('',#7978,#7979,#4800,.T.);
#10103=EDGE_CURVE('',#7979,#7980,#4801,.T.);
#10104=EDGE_CURVE('',#7980,#7981,#4802,.T.);
#10105=EDGE_CURVE('',#7981,#7982,#4803,.T.);
#10106=EDGE_CURVE('',#7982,#7983,#4804,.T.);
#10107=EDGE_CURVE('',#7983,#7984,#4805,.T.);
#10108=EDGE_CURVE('',#7984,#7985,#4806,.T.);
#10109=EDGE_CURVE('',#7985,#7986,#4807,.T.);
#10110=EDGE_CURVE('',#7986,#7987,#4808,.T.);
#10111=EDGE_CURVE('',#7987,#7988,#4809,.T.);
#10112=EDGE_CURVE('',#7988,#7989,#4810,.T.);
#10113=EDGE_CURVE('',#7989,#7976,#4811,.T.);
#10114=EDGE_CURVE('',#7990,#7991,#4812,.T.);
#10115=EDGE_CURVE('',#7991,#7992,#4813,.T.);
#10116=EDGE_CURVE('',#7992,#7993,#4814,.T.);
#10117=EDGE_CURVE('',#7993,#7994,#4815,.T.);
#10118=EDGE_CURVE('',#7994,#7995,#4816,.T.);
#10119=EDGE_CURVE('',#7995,#7996,#4817,.T.);
#10120=EDGE_CURVE('',#7996,#7997,#4818,.T.);
#10121=EDGE_CURVE('',#7997,#7998,#4819,.T.);
#10122=EDGE_CURVE('',#7998,#7999,#4820,.T.);
#10123=EDGE_CURVE('',#7999,#8000,#4821,.T.);
#10124=EDGE_CURVE('',#8000,#8001,#4822,.T.);
#10125=EDGE_CURVE('',#8001,#8002,#4823,.T.);
#10126=EDGE_CURVE('',#8002,#8003,#4824,.T.);
#10127=EDGE_CURVE('',#8003,#7990,#4825,.T.);
#10128=EDGE_CURVE('',#8004,#8005,#4826,.T.);
#10129=EDGE_CURVE('',#8005,#8006,#4827,.T.);
#10130=EDGE_CURVE('',#8006,#8007,#4828,.T.);
#10131=EDGE_CURVE('',#8007,#8008,#4829,.T.);
#10132=EDGE_CURVE('',#8008,#8009,#4830,.T.);
#10133=EDGE_CURVE('',#8009,#8010,#4831,.T.);
#10134=EDGE_CURVE('',#8010,#8011,#4832,.T.);
#10135=EDGE_CURVE('',#8011,#8012,#4833,.T.);
#10136=EDGE_CURVE('',#8012,#8013,#4834,.T.);
#10137=EDGE_CURVE('',#8013,#8014,#4835,.T.);
#10138=EDGE_CURVE('',#8014,#8015,#4836,.T.);
#10139=EDGE_CURVE('',#8015,#8016,#4837,.T.);
#10140=EDGE_CURVE('',#8016,#8017,#4838,.T.);
#10141=EDGE_CURVE('',#8017,#8004,#4839,.T.);
#10142=EDGE_CURVE('',#8018,#8019,#4840,.T.);
#10143=EDGE_CURVE('',#8019,#8020,#4841,.T.);
#10144=EDGE_CURVE('',#8020,#8021,#4842,.T.);
#10145=EDGE_CURVE('',#8021,#8022,#4843,.T.);
#10146=EDGE_CURVE('',#8022,#8023,#4844,.T.);
#10147=EDGE_CURVE('',#8023,#8024,#4845,.T.);
#10148=EDGE_CURVE('',#8024,#8025,#4846,.T.);
#10149=EDGE_CURVE('',#8025,#8026,#4847,.T.);
#10150=EDGE_CURVE('',#8026,#8027,#4848,.T.);
#10151=EDGE_CURVE('',#8027,#8028,#4849,.T.);
#10152=EDGE_CURVE('',#8028,#8029,#4850,.T.);
#10153=EDGE_CURVE('',#8029,#8030,#4851,.T.);
#10154=EDGE_CURVE('',#8030,#8031,#4852,.T.);
#10155=EDGE_CURVE('',#8031,#8018,#4853,.T.);
#10156=EDGE_CURVE('',#8032,#8033,#4854,.T.);
#10157=EDGE_CURVE('',#8033,#8034,#4855,.T.);
#10158=EDGE_CURVE('',#8034,#8035,#4856,.T.);
#10159=EDGE_CURVE('',#8035,#8036,#4857,.T.);
#10160=EDGE_CURVE('',#8036,#8037,#4858,.T.);
#10161=EDGE_CURVE('',#8037,#8038,#4859,.T.);
#10162=EDGE_CURVE('',#8038,#8039,#4860,.T.);
#10163=EDGE_CURVE('',#8039,#8040,#4861,.T.);
#10164=EDGE_CURVE('',#8040,#8041,#4862,.T.);
#10165=EDGE_CURVE('',#8041,#8042,#4863,.T.);
#10166=EDGE_CURVE('',#8042,#8043,#4864,.T.);
#10167=EDGE_CURVE('',#8043,#8044,#4865,.T.);
#10168=EDGE_CURVE('',#8044,#8045,#4866,.T.);
#10169=EDGE_CURVE('',#8045,#8032,#4867,.T.);
#10170=EDGE_CURVE('',#8046,#8047,#4868,.T.);
#10171=EDGE_CURVE('',#8047,#8048,#4869,.T.);
#10172=EDGE_CURVE('',#8048,#8049,#4870,.T.);
#10173=EDGE_CURVE('',#8049,#8050,#4871,.T.);
#10174=EDGE_CURVE('',#8050,#8051,#4872,.T.);
#10175=EDGE_CURVE('',#8051,#8052,#4873,.T.);
#10176=EDGE_CURVE('',#8052,#8053,#4874,.T.);
#10177=EDGE_CURVE('',#8053,#8054,#4875,.T.);
#10178=EDGE_CURVE('',#8054,#8055,#4876,.T.);
#10179=EDGE_CURVE('',#8055,#8056,#4877,.T.);
#10180=EDGE_CURVE('',#8056,#8057,#4878,.T.);
#10181=EDGE_CURVE('',#8057,#8058,#4879,.T.);
#10182=EDGE_CURVE('',#8058,#8059,#4880,.T.);
#10183=EDGE_CURVE('',#8059,#8046,#4881,.T.);
#10184=EDGE_CURVE('',#8060,#8060,#3522,.T.);
#10185=EDGE_CURVE('',#7972,#8061,#1050,.T.);
#10186=EDGE_CURVE('',#8061,#8062,#4096,.T.);
#10187=EDGE_CURVE('',#8062,#8063,#3523,.T.);
#10188=EDGE_CURVE('',#8063,#8064,#4097,.T.);
#10189=EDGE_CURVE('',#8064,#7971,#1051,.T.);
#10190=EDGE_CURVE('',#8065,#8062,#4882,.T.);
#10191=EDGE_CURVE('',#8061,#8066,#4883,.T.);
#10192=EDGE_CURVE('',#8066,#8065,#4098,.T.);
#10193=EDGE_CURVE('',#8067,#8065,#3524,.T.);
#10194=EDGE_CURVE('',#8066,#8068,#1052,.T.);
#10195=EDGE_CURVE('',#8068,#8069,#3525,.T.);
#10196=EDGE_CURVE('',#8069,#8070,#1053,.T.);
#10197=EDGE_CURVE('',#8067,#8070,#4099,.T.);
#10198=EDGE_CURVE('',#8070,#8064,#4884,.T.);
#10199=EDGE_CURVE('',#8063,#8067,#4885,.T.);
#10200=EDGE_CURVE('',#7965,#8069,#4886,.T.);
#10201=EDGE_CURVE('',#8068,#7962,#4887,.T.);
#10202=EDGE_CURVE('',#8071,#8071,#3526,.T.);
#10203=EDGE_CURVE('',#8072,#8072,#3527,.T.);
#10204=EDGE_CURVE('',#8073,#8073,#3528,.T.);
#10205=EDGE_CURVE('',#8074,#8075,#4888,.T.);
#10206=EDGE_CURVE('',#8075,#8076,#4889,.T.);
#10207=EDGE_CURVE('',#8076,#8077,#4890,.T.);
#10208=EDGE_CURVE('',#8077,#8078,#4891,.T.);
#10209=EDGE_CURVE('',#8078,#8079,#4892,.T.);
#10210=EDGE_CURVE('',#8079,#8080,#4893,.T.);
#10211=EDGE_CURVE('',#8080,#8081,#4894,.T.);
#10212=EDGE_CURVE('',#8081,#8082,#4895,.T.);
#10213=EDGE_CURVE('',#8082,#8083,#4896,.T.);
#10214=EDGE_CURVE('',#8083,#8084,#4897,.T.);
#10215=EDGE_CURVE('',#8084,#8085,#4898,.T.);
#10216=EDGE_CURVE('',#8085,#8086,#4899,.T.);
#10217=EDGE_CURVE('',#8086,#8087,#4900,.T.);
#10218=EDGE_CURVE('',#8087,#8074,#4901,.T.);
#10219=EDGE_CURVE('',#8088,#8089,#4902,.T.);
#10220=EDGE_CURVE('',#8089,#8090,#4903,.T.);
#10221=EDGE_CURVE('',#8090,#8091,#4904,.T.);
#10222=EDGE_CURVE('',#8091,#8092,#4905,.T.);
#10223=EDGE_CURVE('',#8092,#8093,#4906,.T.);
#10224=EDGE_CURVE('',#8093,#8094,#4907,.T.);
#10225=EDGE_CURVE('',#8094,#8095,#4908,.T.);
#10226=EDGE_CURVE('',#8095,#8096,#4909,.T.);
#10227=EDGE_CURVE('',#8096,#8097,#4910,.T.);
#10228=EDGE_CURVE('',#8097,#8098,#4911,.T.);
#10229=EDGE_CURVE('',#8098,#8099,#4912,.T.);
#10230=EDGE_CURVE('',#8099,#8100,#4913,.T.);
#10231=EDGE_CURVE('',#8100,#8101,#4914,.T.);
#10232=EDGE_CURVE('',#8101,#8088,#4915,.T.);
#10233=EDGE_CURVE('',#8102,#8103,#4916,.T.);
#10234=EDGE_CURVE('',#8103,#8104,#4917,.T.);
#10235=EDGE_CURVE('',#8104,#8105,#4918,.T.);
#10236=EDGE_CURVE('',#8105,#8106,#4919,.T.);
#10237=EDGE_CURVE('',#8106,#8107,#4920,.T.);
#10238=EDGE_CURVE('',#8107,#8108,#4921,.T.);
#10239=EDGE_CURVE('',#8108,#8109,#4922,.T.);
#10240=EDGE_CURVE('',#8109,#8110,#4923,.T.);
#10241=EDGE_CURVE('',#8110,#8111,#4924,.T.);
#10242=EDGE_CURVE('',#8111,#8112,#4925,.T.);
#10243=EDGE_CURVE('',#8112,#8113,#4926,.T.);
#10244=EDGE_CURVE('',#8113,#8114,#4927,.T.);
#10245=EDGE_CURVE('',#8114,#8115,#4928,.T.);
#10246=EDGE_CURVE('',#8115,#8102,#4929,.T.);
#10247=EDGE_CURVE('',#8116,#8117,#4930,.T.);
#10248=EDGE_CURVE('',#8117,#8118,#4931,.T.);
#10249=EDGE_CURVE('',#8118,#8119,#4932,.T.);
#10250=EDGE_CURVE('',#8119,#8120,#4933,.T.);
#10251=EDGE_CURVE('',#8120,#8121,#4934,.T.);
#10252=EDGE_CURVE('',#8121,#8122,#4935,.T.);
#10253=EDGE_CURVE('',#8122,#8123,#4936,.T.);
#10254=EDGE_CURVE('',#8123,#8124,#4937,.T.);
#10255=EDGE_CURVE('',#8124,#8125,#4938,.T.);
#10256=EDGE_CURVE('',#8125,#8126,#4939,.T.);
#10257=EDGE_CURVE('',#8126,#8127,#4940,.T.);
#10258=EDGE_CURVE('',#8127,#8128,#4941,.T.);
#10259=EDGE_CURVE('',#8128,#8129,#4942,.T.);
#10260=EDGE_CURVE('',#8129,#8116,#4943,.T.);
#10261=EDGE_CURVE('',#8130,#8131,#4944,.T.);
#10262=EDGE_CURVE('',#8131,#8132,#4945,.T.);
#10263=EDGE_CURVE('',#8132,#8133,#4946,.T.);
#10264=EDGE_CURVE('',#8133,#8134,#4947,.T.);
#10265=EDGE_CURVE('',#8134,#8135,#4948,.T.);
#10266=EDGE_CURVE('',#8135,#8136,#4949,.T.);
#10267=EDGE_CURVE('',#8136,#8137,#4950,.T.);
#10268=EDGE_CURVE('',#8137,#8138,#4951,.T.);
#10269=EDGE_CURVE('',#8138,#8139,#4952,.T.);
#10270=EDGE_CURVE('',#8139,#8140,#4953,.T.);
#10271=EDGE_CURVE('',#8140,#8141,#4954,.T.);
#10272=EDGE_CURVE('',#8141,#8142,#4955,.T.);
#10273=EDGE_CURVE('',#8142,#8143,#4956,.T.);
#10274=EDGE_CURVE('',#8143,#8130,#4957,.T.);
#10275=EDGE_CURVE('',#8144,#8145,#4958,.T.);
#10276=EDGE_CURVE('',#8145,#8146,#4959,.T.);
#10277=EDGE_CURVE('',#8146,#8147,#4960,.T.);
#10278=EDGE_CURVE('',#8147,#8148,#4961,.T.);
#10279=EDGE_CURVE('',#8148,#8149,#4962,.T.);
#10280=EDGE_CURVE('',#8149,#8150,#4963,.T.);
#10281=EDGE_CURVE('',#8150,#8151,#4964,.T.);
#10282=EDGE_CURVE('',#8151,#8152,#4965,.T.);
#10283=EDGE_CURVE('',#8152,#8153,#4966,.T.);
#10284=EDGE_CURVE('',#8153,#8154,#4967,.T.);
#10285=EDGE_CURVE('',#8154,#8155,#4968,.T.);
#10286=EDGE_CURVE('',#8155,#8156,#4969,.T.);
#10287=EDGE_CURVE('',#8156,#8157,#4970,.T.);
#10288=EDGE_CURVE('',#8157,#8144,#4971,.T.);
#10289=EDGE_CURVE('',#8158,#8158,#3529,.T.);
#10290=EDGE_CURVE('',#7973,#8159,#4972,.T.);
#10291=EDGE_CURVE('',#8159,#8159,#3530,.T.);
#10292=EDGE_CURVE('',#8159,#8160,#4973,.T.);
#10293=EDGE_CURVE('',#8160,#8160,#3531,.T.);
#10294=EDGE_CURVE('',#8071,#8160,#4974,.T.);
#10295=EDGE_CURVE('',#8060,#8161,#4975,.T.);
#10296=EDGE_CURVE('',#8161,#8161,#3532,.T.);
#10297=EDGE_CURVE('',#8161,#8162,#4976,.T.);
#10298=EDGE_CURVE('',#8162,#8162,#3533,.T.);
#10299=EDGE_CURVE('',#8158,#8162,#4977,.T.);
#10300=EDGE_CURVE('',#7974,#8163,#4978,.T.);
#10301=EDGE_CURVE('',#8163,#8163,#3534,.T.);
#10302=EDGE_CURVE('',#8163,#8164,#4979,.T.);
#10303=EDGE_CURVE('',#8164,#8164,#3535,.T.);
#10304=EDGE_CURVE('',#8072,#8164,#4980,.T.);
#10305=EDGE_CURVE('',#7968,#8165,#4981,.T.);
#10306=EDGE_CURVE('',#8165,#8165,#3536,.T.);
#10307=EDGE_CURVE('',#8165,#8166,#4982,.T.);
#10308=EDGE_CURVE('',#8167,#8166,#4100,.T.);
#10309=EDGE_CURVE('',#8168,#8167,#4101,.T.);
#10310=EDGE_CURVE('',#8166,#8168,#4102,.T.);
#10311=EDGE_CURVE('',#8144,#8169,#4983,.T.);
#10312=EDGE_CURVE('',#8169,#8170,#4984,.T.);
#10313=EDGE_CURVE('',#8145,#8170,#4985,.T.);
#10314=EDGE_CURVE('',#8157,#8171,#4986,.T.);
#10315=EDGE_CURVE('',#8171,#8169,#4987,.T.);
#10316=EDGE_CURVE('',#8156,#8172,#4988,.T.);
#10317=EDGE_CURVE('',#8172,#8171,#4989,.T.);
#10318=EDGE_CURVE('',#8155,#8173,#4990,.T.);
#10319=EDGE_CURVE('',#8173,#8172,#4991,.T.);
#10320=EDGE_CURVE('',#8154,#8174,#4992,.T.);
#10321=EDGE_CURVE('',#8174,#8173,#4993,.T.);
#10322=EDGE_CURVE('',#8153,#8175,#4994,.T.);
#10323=EDGE_CURVE('',#8175,#8174,#4995,.T.);
#10324=EDGE_CURVE('',#8152,#8176,#4996,.T.);
#10325=EDGE_CURVE('',#8176,#8175,#4997,.T.);
#10326=EDGE_CURVE('',#8151,#8177,#4998,.T.);
#10327=EDGE_CURVE('',#8177,#8176,#4999,.T.);
#10328=EDGE_CURVE('',#8150,#8178,#5000,.T.);
#10329=EDGE_CURVE('',#8178,#8177,#5001,.T.);
#10330=EDGE_CURVE('',#8149,#8179,#5002,.T.);
#10331=EDGE_CURVE('',#8179,#8178,#5003,.T.);
#10332=EDGE_CURVE('',#8148,#8180,#5004,.T.);
#10333=EDGE_CURVE('',#8180,#8179,#5005,.T.);
#10334=EDGE_CURVE('',#8147,#8181,#5006,.T.);
#10335=EDGE_CURVE('',#8181,#8180,#5007,.T.);
#10336=EDGE_CURVE('',#8146,#8182,#5008,.T.);
#10337=EDGE_CURVE('',#8182,#8181,#5009,.T.);
#10338=EDGE_CURVE('',#8170,#8182,#5010,.T.);
#10339=EDGE_CURVE('',#8130,#8183,#5011,.T.);
#10340=EDGE_CURVE('',#8183,#8184,#5012,.T.);
#10341=EDGE_CURVE('',#8131,#8184,#5013,.T.);
#10342=EDGE_CURVE('',#8143,#8185,#5014,.T.);
#10343=EDGE_CURVE('',#8185,#8183,#5015,.T.);
#10344=EDGE_CURVE('',#8142,#8186,#5016,.T.);
#10345=EDGE_CURVE('',#8186,#8185,#5017,.T.);
#10346=EDGE_CURVE('',#8141,#8187,#5018,.T.);
#10347=EDGE_CURVE('',#8187,#8186,#5019,.T.);
#10348=EDGE_CURVE('',#8140,#8188,#5020,.T.);
#10349=EDGE_CURVE('',#8188,#8187,#5021,.T.);
#10350=EDGE_CURVE('',#8139,#8189,#5022,.T.);
#10351=EDGE_CURVE('',#8189,#8188,#5023,.T.);
#10352=EDGE_CURVE('',#8138,#8190,#5024,.T.);
#10353=EDGE_CURVE('',#8190,#8189,#5025,.T.);
#10354=EDGE_CURVE('',#8137,#8191,#5026,.T.);
#10355=EDGE_CURVE('',#8191,#8190,#5027,.T.);
#10356=EDGE_CURVE('',#8136,#8192,#5028,.T.);
#10357=EDGE_CURVE('',#8192,#8191,#5029,.T.);
#10358=EDGE_CURVE('',#8135,#8193,#5030,.T.);
#10359=EDGE_CURVE('',#8193,#8192,#5031,.T.);
#10360=EDGE_CURVE('',#8134,#8194,#5032,.T.);
#10361=EDGE_CURVE('',#8194,#8193,#5033,.T.);
#10362=EDGE_CURVE('',#8133,#8195,#5034,.T.);
#10363=EDGE_CURVE('',#8195,#8194,#5035,.T.);
#10364=EDGE_CURVE('',#8132,#8196,#5036,.T.);
#10365=EDGE_CURVE('',#8196,#8195,#5037,.T.);
#10366=EDGE_CURVE('',#8184,#8196,#5038,.T.);
#10367=EDGE_CURVE('',#8116,#8197,#5039,.T.);
#10368=EDGE_CURVE('',#8197,#8198,#5040,.T.);
#10369=EDGE_CURVE('',#8117,#8198,#5041,.T.);
#10370=EDGE_CURVE('',#8129,#8199,#5042,.T.);
#10371=EDGE_CURVE('',#8199,#8197,#5043,.T.);
#10372=EDGE_CURVE('',#8128,#8200,#5044,.T.);
#10373=EDGE_CURVE('',#8200,#8199,#5045,.T.);
#10374=EDGE_CURVE('',#8127,#8201,#5046,.T.);
#10375=EDGE_CURVE('',#8201,#8200,#5047,.T.);
#10376=EDGE_CURVE('',#8126,#8202,#5048,.T.);
#10377=EDGE_CURVE('',#8202,#8201,#5049,.T.);
#10378=EDGE_CURVE('',#8125,#8203,#5050,.T.);
#10379=EDGE_CURVE('',#8203,#8202,#5051,.T.);
#10380=EDGE_CURVE('',#8124,#8204,#5052,.T.);
#10381=EDGE_CURVE('',#8204,#8203,#5053,.T.);
#10382=EDGE_CURVE('',#8123,#8205,#5054,.T.);
#10383=EDGE_CURVE('',#8205,#8204,#5055,.T.);
#10384=EDGE_CURVE('',#8122,#8206,#5056,.T.);
#10385=EDGE_CURVE('',#8206,#8205,#5057,.T.);
#10386=EDGE_CURVE('',#8121,#8207,#5058,.T.);
#10387=EDGE_CURVE('',#8207,#8206,#5059,.T.);
#10388=EDGE_CURVE('',#8120,#8208,#5060,.T.);
#10389=EDGE_CURVE('',#8208,#8207,#5061,.T.);
#10390=EDGE_CURVE('',#8119,#8209,#5062,.T.);
#10391=EDGE_CURVE('',#8209,#8208,#5063,.T.);
#10392=EDGE_CURVE('',#8118,#8210,#5064,.T.);
#10393=EDGE_CURVE('',#8210,#8209,#5065,.T.);
#10394=EDGE_CURVE('',#8198,#8210,#5066,.T.);
#10395=EDGE_CURVE('',#8102,#8211,#5067,.T.);
#10396=EDGE_CURVE('',#8211,#8212,#5068,.T.);
#10397=EDGE_CURVE('',#8103,#8212,#5069,.T.);
#10398=EDGE_CURVE('',#8115,#8213,#5070,.T.);
#10399=EDGE_CURVE('',#8213,#8211,#5071,.T.);
#10400=EDGE_CURVE('',#8114,#8214,#5072,.T.);
#10401=EDGE_CURVE('',#8214,#8213,#5073,.T.);
#10402=EDGE_CURVE('',#8113,#8215,#5074,.T.);
#10403=EDGE_CURVE('',#8215,#8214,#5075,.T.);
#10404=EDGE_CURVE('',#8112,#8216,#5076,.T.);
#10405=EDGE_CURVE('',#8216,#8215,#5077,.T.);
#10406=EDGE_CURVE('',#8111,#8217,#5078,.T.);
#10407=EDGE_CURVE('',#8217,#8216,#5079,.T.);
#10408=EDGE_CURVE('',#8110,#8218,#5080,.T.);
#10409=EDGE_CURVE('',#8218,#8217,#5081,.T.);
#10410=EDGE_CURVE('',#8109,#8219,#5082,.T.);
#10411=EDGE_CURVE('',#8219,#8218,#5083,.T.);
#10412=EDGE_CURVE('',#8108,#8220,#5084,.T.);
#10413=EDGE_CURVE('',#8220,#8219,#5085,.T.);
#10414=EDGE_CURVE('',#8107,#8221,#5086,.T.);
#10415=EDGE_CURVE('',#8221,#8220,#5087,.T.);
#10416=EDGE_CURVE('',#8106,#8222,#5088,.T.);
#10417=EDGE_CURVE('',#8222,#8221,#5089,.T.);
#10418=EDGE_CURVE('',#8105,#8223,#5090,.T.);
#10419=EDGE_CURVE('',#8223,#8222,#5091,.T.);
#10420=EDGE_CURVE('',#8104,#8224,#5092,.T.);
#10421=EDGE_CURVE('',#8224,#8223,#5093,.T.);
#10422=EDGE_CURVE('',#8212,#8224,#5094,.T.);
#10423=EDGE_CURVE('',#8088,#8225,#5095,.T.);
#10424=EDGE_CURVE('',#8225,#8226,#5096,.T.);
#10425=EDGE_CURVE('',#8089,#8226,#5097,.T.);
#10426=EDGE_CURVE('',#8101,#8227,#5098,.T.);
#10427=EDGE_CURVE('',#8227,#8225,#5099,.T.);
#10428=EDGE_CURVE('',#8100,#8228,#5100,.T.);
#10429=EDGE_CURVE('',#8228,#8227,#5101,.T.);
#10430=EDGE_CURVE('',#8099,#8229,#5102,.T.);
#10431=EDGE_CURVE('',#8229,#8228,#5103,.T.);
#10432=EDGE_CURVE('',#8098,#8230,#5104,.T.);
#10433=EDGE_CURVE('',#8230,#8229,#5105,.T.);
#10434=EDGE_CURVE('',#8097,#8231,#5106,.T.);
#10435=EDGE_CURVE('',#8231,#8230,#5107,.T.);
#10436=EDGE_CURVE('',#8096,#8232,#5108,.T.);
#10437=EDGE_CURVE('',#8232,#8231,#5109,.T.);
#10438=EDGE_CURVE('',#8095,#8233,#5110,.T.);
#10439=EDGE_CURVE('',#8233,#8232,#5111,.T.);
#10440=EDGE_CURVE('',#8094,#8234,#5112,.T.);
#10441=EDGE_CURVE('',#8234,#8233,#5113,.T.);
#10442=EDGE_CURVE('',#8093,#8235,#5114,.T.);
#10443=EDGE_CURVE('',#8235,#8234,#5115,.T.);
#10444=EDGE_CURVE('',#8092,#8236,#5116,.T.);
#10445=EDGE_CURVE('',#8236,#8235,#5117,.T.);
#10446=EDGE_CURVE('',#8091,#8237,#5118,.T.);
#10447=EDGE_CURVE('',#8237,#8236,#5119,.T.);
#10448=EDGE_CURVE('',#8090,#8238,#5120,.T.);
#10449=EDGE_CURVE('',#8238,#8237,#5121,.T.);
#10450=EDGE_CURVE('',#8226,#8238,#5122,.T.);
#10451=EDGE_CURVE('',#8074,#8239,#5123,.T.);
#10452=EDGE_CURVE('',#8239,#8240,#5124,.T.);
#10453=EDGE_CURVE('',#8075,#8240,#5125,.T.);
#10454=EDGE_CURVE('',#8087,#8241,#5126,.T.);
#10455=EDGE_CURVE('',#8241,#8239,#5127,.T.);
#10456=EDGE_CURVE('',#8086,#8242,#5128,.T.);
#10457=EDGE_CURVE('',#8242,#8241,#5129,.T.);
#10458=EDGE_CURVE('',#8085,#8243,#5130,.T.);
#10459=EDGE_CURVE('',#8243,#8242,#5131,.T.);
#10460=EDGE_CURVE('',#8084,#8244,#5132,.T.);
#10461=EDGE_CURVE('',#8244,#8243,#5133,.T.);
#10462=EDGE_CURVE('',#8083,#8245,#5134,.T.);
#10463=EDGE_CURVE('',#8245,#8244,#5135,.T.);
#10464=EDGE_CURVE('',#8082,#8246,#5136,.T.);
#10465=EDGE_CURVE('',#8246,#8245,#5137,.T.);
#10466=EDGE_CURVE('',#8081,#8247,#5138,.T.);
#10467=EDGE_CURVE('',#8247,#8246,#5139,.T.);
#10468=EDGE_CURVE('',#8080,#8248,#5140,.T.);
#10469=EDGE_CURVE('',#8248,#8247,#5141,.T.);
#10470=EDGE_CURVE('',#8079,#8249,#5142,.T.);
#10471=EDGE_CURVE('',#8249,#8248,#5143,.T.);
#10472=EDGE_CURVE('',#8078,#8250,#5144,.T.);
#10473=EDGE_CURVE('',#8250,#8249,#5145,.T.);
#10474=EDGE_CURVE('',#8077,#8251,#5146,.T.);
#10475=EDGE_CURVE('',#8251,#8250,#5147,.T.);
#10476=EDGE_CURVE('',#8076,#8252,#5148,.T.);
#10477=EDGE_CURVE('',#8252,#8251,#5149,.T.);
#10478=EDGE_CURVE('',#8240,#8252,#5150,.T.);
#10479=EDGE_CURVE('',#8046,#8253,#5151,.T.);
#10480=EDGE_CURVE('',#8253,#8254,#5152,.T.);
#10481=EDGE_CURVE('',#8047,#8254,#5153,.T.);
#10482=EDGE_CURVE('',#8059,#8255,#5154,.T.);
#10483=EDGE_CURVE('',#8255,#8253,#5155,.T.);
#10484=EDGE_CURVE('',#8058,#8256,#5156,.T.);
#10485=EDGE_CURVE('',#8256,#8255,#5157,.T.);
#10486=EDGE_CURVE('',#8057,#8257,#5158,.T.);
#10487=EDGE_CURVE('',#8257,#8256,#5159,.T.);
#10488=EDGE_CURVE('',#8056,#8258,#5160,.T.);
#10489=EDGE_CURVE('',#8258,#8257,#5161,.T.);
#10490=EDGE_CURVE('',#8055,#8259,#5162,.T.);
#10491=EDGE_CURVE('',#8259,#8258,#5163,.T.);
#10492=EDGE_CURVE('',#8054,#8260,#5164,.T.);
#10493=EDGE_CURVE('',#8260,#8259,#5165,.T.);
#10494=EDGE_CURVE('',#8053,#8261,#5166,.T.);
#10495=EDGE_CURVE('',#8261,#8260,#5167,.T.);
#10496=EDGE_CURVE('',#8052,#8262,#5168,.T.);
#10497=EDGE_CURVE('',#8262,#8261,#5169,.T.);
#10498=EDGE_CURVE('',#8051,#8263,#5170,.T.);
#10499=EDGE_CURVE('',#8263,#8262,#5171,.T.);
#10500=EDGE_CURVE('',#8050,#8264,#5172,.T.);
#10501=EDGE_CURVE('',#8264,#8263,#5173,.T.);
#10502=EDGE_CURVE('',#8049,#8265,#5174,.T.);
#10503=EDGE_CURVE('',#8265,#8264,#5175,.T.);
#10504=EDGE_CURVE('',#8048,#8266,#5176,.T.);
#10505=EDGE_CURVE('',#8266,#8265,#5177,.T.);
#10506=EDGE_CURVE('',#8254,#8266,#5178,.T.);
#10507=EDGE_CURVE('',#8032,#8267,#5179,.T.);
#10508=EDGE_CURVE('',#8267,#8268,#5180,.T.);
#10509=EDGE_CURVE('',#8033,#8268,#5181,.T.);
#10510=EDGE_CURVE('',#8045,#8269,#5182,.T.);
#10511=EDGE_CURVE('',#8269,#8267,#5183,.T.);
#10512=EDGE_CURVE('',#8044,#8270,#5184,.T.);
#10513=EDGE_CURVE('',#8270,#8269,#5185,.T.);
#10514=EDGE_CURVE('',#8043,#8271,#5186,.T.);
#10515=EDGE_CURVE('',#8271,#8270,#5187,.T.);
#10516=EDGE_CURVE('',#8042,#8272,#5188,.T.);
#10517=EDGE_CURVE('',#8272,#8271,#5189,.T.);
#10518=EDGE_CURVE('',#8041,#8273,#5190,.T.);
#10519=EDGE_CURVE('',#8273,#8272,#5191,.T.);
#10520=EDGE_CURVE('',#8040,#8274,#5192,.T.);
#10521=EDGE_CURVE('',#8274,#8273,#5193,.T.);
#10522=EDGE_CURVE('',#8039,#8275,#5194,.T.);
#10523=EDGE_CURVE('',#8275,#8274,#5195,.T.);
#10524=EDGE_CURVE('',#8038,#8276,#5196,.T.);
#10525=EDGE_CURVE('',#8276,#8275,#5197,.T.);
#10526=EDGE_CURVE('',#8037,#8277,#5198,.T.);
#10527=EDGE_CURVE('',#8277,#8276,#5199,.T.);
#10528=EDGE_CURVE('',#8036,#8278,#5200,.T.);
#10529=EDGE_CURVE('',#8278,#8277,#5201,.T.);
#10530=EDGE_CURVE('',#8035,#8279,#5202,.T.);
#10531=EDGE_CURVE('',#8279,#8278,#5203,.T.);
#10532=EDGE_CURVE('',#8034,#8280,#5204,.T.);
#10533=EDGE_CURVE('',#8280,#8279,#5205,.T.);
#10534=EDGE_CURVE('',#8268,#8280,#5206,.T.);
#10535=EDGE_CURVE('',#8018,#8281,#5207,.T.);
#10536=EDGE_CURVE('',#8281,#8282,#5208,.T.);
#10537=EDGE_CURVE('',#8019,#8282,#5209,.T.);
#10538=EDGE_CURVE('',#8031,#8283,#5210,.T.);
#10539=EDGE_CURVE('',#8283,#8281,#5211,.T.);
#10540=EDGE_CURVE('',#8030,#8284,#5212,.T.);
#10541=EDGE_CURVE('',#8284,#8283,#5213,.T.);
#10542=EDGE_CURVE('',#8029,#8285,#5214,.T.);
#10543=EDGE_CURVE('',#8285,#8284,#5215,.T.);
#10544=EDGE_CURVE('',#8028,#8286,#5216,.T.);
#10545=EDGE_CURVE('',#8286,#8285,#5217,.T.);
#10546=EDGE_CURVE('',#8027,#8287,#5218,.T.);
#10547=EDGE_CURVE('',#8287,#8286,#5219,.T.);
#10548=EDGE_CURVE('',#8026,#8288,#5220,.T.);
#10549=EDGE_CURVE('',#8288,#8287,#5221,.T.);
#10550=EDGE_CURVE('',#8025,#8289,#5222,.T.);
#10551=EDGE_CURVE('',#8289,#8288,#5223,.T.);
#10552=EDGE_CURVE('',#8024,#8290,#5224,.T.);
#10553=EDGE_CURVE('',#8290,#8289,#5225,.T.);
#10554=EDGE_CURVE('',#8023,#8291,#5226,.T.);
#10555=EDGE_CURVE('',#8291,#8290,#5227,.T.);
#10556=EDGE_CURVE('',#8022,#8292,#5228,.T.);
#10557=EDGE_CURVE('',#8292,#8291,#5229,.T.);
#10558=EDGE_CURVE('',#8021,#8293,#5230,.T.);
#10559=EDGE_CURVE('',#8293,#8292,#5231,.T.);
#10560=EDGE_CURVE('',#8020,#8294,#5232,.T.);
#10561=EDGE_CURVE('',#8294,#8293,#5233,.T.);
#10562=EDGE_CURVE('',#8282,#8294,#5234,.T.);
#10563=EDGE_CURVE('',#8004,#8295,#5235,.T.);
#10564=EDGE_CURVE('',#8295,#8296,#5236,.T.);
#10565=EDGE_CURVE('',#8005,#8296,#5237,.T.);
#10566=EDGE_CURVE('',#8017,#8297,#5238,.T.);
#10567=EDGE_CURVE('',#8297,#8295,#5239,.T.);
#10568=EDGE_CURVE('',#8016,#8298,#5240,.T.);
#10569=EDGE_CURVE('',#8298,#8297,#5241,.T.);
#10570=EDGE_CURVE('',#8015,#8299,#5242,.T.);
#10571=EDGE_CURVE('',#8299,#8298,#5243,.T.);
#10572=EDGE_CURVE('',#8014,#8300,#5244,.T.);
#10573=EDGE_CURVE('',#8300,#8299,#5245,.T.);
#10574=EDGE_CURVE('',#8013,#8301,#5246,.T.);
#10575=EDGE_CURVE('',#8301,#8300,#5247,.T.);
#10576=EDGE_CURVE('',#8012,#8302,#5248,.T.);
#10577=EDGE_CURVE('',#8302,#8301,#5249,.T.);
#10578=EDGE_CURVE('',#8011,#8303,#5250,.T.);
#10579=EDGE_CURVE('',#8303,#8302,#5251,.T.);
#10580=EDGE_CURVE('',#8010,#8304,#5252,.T.);
#10581=EDGE_CURVE('',#8304,#8303,#5253,.T.);
#10582=EDGE_CURVE('',#8009,#8305,#5254,.T.);
#10583=EDGE_CURVE('',#8305,#8304,#5255,.T.);
#10584=EDGE_CURVE('',#8008,#8306,#5256,.T.);
#10585=EDGE_CURVE('',#8306,#8305,#5257,.T.);
#10586=EDGE_CURVE('',#8007,#8307,#5258,.T.);
#10587=EDGE_CURVE('',#8307,#8306,#5259,.T.);
#10588=EDGE_CURVE('',#8006,#8308,#5260,.T.);
#10589=EDGE_CURVE('',#8308,#8307,#5261,.T.);
#10590=EDGE_CURVE('',#8296,#8308,#5262,.T.);
#10591=EDGE_CURVE('',#7990,#8309,#5263,.T.);
#10592=EDGE_CURVE('',#8309,#8310,#5264,.T.);
#10593=EDGE_CURVE('',#7991,#8310,#5265,.T.);
#10594=EDGE_CURVE('',#8003,#8311,#5266,.T.);
#10595=EDGE_CURVE('',#8311,#8309,#5267,.T.);
#10596=EDGE_CURVE('',#8002,#8312,#5268,.T.);
#10597=EDGE_CURVE('',#8312,#8311,#5269,.T.);
#10598=EDGE_CURVE('',#8001,#8313,#5270,.T.);
#10599=EDGE_CURVE('',#8313,#8312,#5271,.T.);
#10600=EDGE_CURVE('',#8000,#8314,#5272,.T.);
#10601=EDGE_CURVE('',#8314,#8313,#5273,.T.);
#10602=EDGE_CURVE('',#7999,#8315,#5274,.T.);
#10603=EDGE_CURVE('',#8315,#8314,#5275,.T.);
#10604=EDGE_CURVE('',#7998,#8316,#5276,.T.);
#10605=EDGE_CURVE('',#8316,#8315,#5277,.T.);
#10606=EDGE_CURVE('',#7997,#8317,#5278,.T.);
#10607=EDGE_CURVE('',#8317,#8316,#5279,.T.);
#10608=EDGE_CURVE('',#7996,#8318,#5280,.T.);
#10609=EDGE_CURVE('',#8318,#8317,#5281,.T.);
#10610=EDGE_CURVE('',#7995,#8319,#5282,.T.);
#10611=EDGE_CURVE('',#8319,#8318,#5283,.T.);
#10612=EDGE_CURVE('',#7994,#8320,#5284,.T.);
#10613=EDGE_CURVE('',#8320,#8319,#5285,.T.);
#10614=EDGE_CURVE('',#7993,#8321,#5286,.T.);
#10615=EDGE_CURVE('',#8321,#8320,#5287,.T.);
#10616=EDGE_CURVE('',#7992,#8322,#5288,.T.);
#10617=EDGE_CURVE('',#8322,#8321,#5289,.T.);
#10618=EDGE_CURVE('',#8310,#8322,#5290,.T.);
#10619=EDGE_CURVE('',#7976,#8323,#5291,.T.);
#10620=EDGE_CURVE('',#8323,#8324,#5292,.T.);
#10621=EDGE_CURVE('',#7977,#8324,#5293,.T.);
#10622=EDGE_CURVE('',#7989,#8325,#5294,.T.);
#10623=EDGE_CURVE('',#8325,#8323,#5295,.T.);
#10624=EDGE_CURVE('',#7988,#8326,#5296,.T.);
#10625=EDGE_CURVE('',#8326,#8325,#5297,.T.);
#10626=EDGE_CURVE('',#7987,#8327,#5298,.T.);
#10627=EDGE_CURVE('',#8327,#8326,#5299,.T.);
#10628=EDGE_CURVE('',#7986,#8328,#5300,.T.);
#10629=EDGE_CURVE('',#8328,#8327,#5301,.T.);
#10630=EDGE_CURVE('',#7985,#8329,#5302,.T.);
#10631=EDGE_CURVE('',#8329,#8328,#5303,.T.);
#10632=EDGE_CURVE('',#7984,#8330,#5304,.T.);
#10633=EDGE_CURVE('',#8330,#8329,#5305,.T.);
#10634=EDGE_CURVE('',#7983,#8331,#5306,.T.);
#10635=EDGE_CURVE('',#8331,#8330,#5307,.T.);
#10636=EDGE_CURVE('',#7982,#8332,#5308,.T.);
#10637=EDGE_CURVE('',#8332,#8331,#5309,.T.);
#10638=EDGE_CURVE('',#7981,#8333,#5310,.T.);
#10639=EDGE_CURVE('',#8333,#8332,#5311,.T.);
#10640=EDGE_CURVE('',#7980,#8334,#5312,.T.);
#10641=EDGE_CURVE('',#8334,#8333,#5313,.T.);
#10642=EDGE_CURVE('',#7979,#8335,#5314,.T.);
#10643=EDGE_CURVE('',#8335,#8334,#5315,.T.);
#10644=EDGE_CURVE('',#7978,#8336,#5316,.T.);
#10645=EDGE_CURVE('',#8336,#8335,#5317,.T.);
#10646=EDGE_CURVE('',#8324,#8336,#5318,.T.);
#10647=EDGE_CURVE('',#8073,#8168,#5319,.T.);
#10648=EDGE_CURVE('',#8166,#7975,#5320,.T.);
#13751=ORIENTED_EDGE('',*,*,#10083,.T.);
#13752=ORIENTED_EDGE('',*,*,#10084,.T.);
#13753=ORIENTED_EDGE('',*,*,#10085,.T.);
#13754=ORIENTED_EDGE('',*,*,#10086,.T.);
#13755=ORIENTED_EDGE('',*,*,#10084,.F.);
#13756=ORIENTED_EDGE('',*,*,#10087,.F.);
#13757=ORIENTED_EDGE('',*,*,#10088,.F.);
#13758=ORIENTED_EDGE('',*,*,#10089,.T.);
#13759=ORIENTED_EDGE('',*,*,#10090,.F.);
#13760=ORIENTED_EDGE('',*,*,#10091,.T.);
#13761=ORIENTED_EDGE('',*,*,#10092,.T.);
#13762=ORIENTED_EDGE('',*,*,#10093,.T.);
#13763=ORIENTED_EDGE('',*,*,#10088,.T.);
#13764=ORIENTED_EDGE('',*,*,#10094,.F.);
#13765=ORIENTED_EDGE('',*,*,#10092,.F.);
#13766=ORIENTED_EDGE('',*,*,#10095,.F.);
#13767=ORIENTED_EDGE('',*,*,#10096,.F.);
#13768=ORIENTED_EDGE('',*,*,#10097,.F.);
#13769=ORIENTED_EDGE('',*,*,#10098,.F.);
#13770=ORIENTED_EDGE('',*,*,#10099,.F.);
#13771=ORIENTED_EDGE('',*,*,#10100,.T.);
#13772=ORIENTED_EDGE('',*,*,#10101,.T.);
#13773=ORIENTED_EDGE('',*,*,#10102,.T.);
#13774=ORIENTED_EDGE('',*,*,#10103,.T.);
#13775=ORIENTED_EDGE('',*,*,#10104,.T.);
#13776=ORIENTED_EDGE('',*,*,#10105,.T.);
#13777=ORIENTED_EDGE('',*,*,#10106,.T.);
#13778=ORIENTED_EDGE('',*,*,#10107,.T.);
#13779=ORIENTED_EDGE('',*,*,#10108,.T.);
#13780=ORIENTED_EDGE('',*,*,#10109,.T.);
#13781=ORIENTED_EDGE('',*,*,#10110,.T.);
#13782=ORIENTED_EDGE('',*,*,#10111,.T.);
#13783=ORIENTED_EDGE('',*,*,#10112,.T.);
#13784=ORIENTED_EDGE('',*,*,#10113,.T.);
#13785=ORIENTED_EDGE('',*,*,#10114,.T.);
#13786=ORIENTED_EDGE('',*,*,#10115,.T.);
#13787=ORIENTED_EDGE('',*,*,#10116,.T.);
#13788=ORIENTED_EDGE('',*,*,#10117,.T.);
#13789=ORIENTED_EDGE('',*,*,#10118,.T.);
#13790=ORIENTED_EDGE('',*,*,#10119,.T.);
#13791=ORIENTED_EDGE('',*,*,#10120,.T.);
#13792=ORIENTED_EDGE('',*,*,#10121,.T.);
#13793=ORIENTED_EDGE('',*,*,#10122,.T.);
#13794=ORIENTED_EDGE('',*,*,#10123,.T.);
#13795=ORIENTED_EDGE('',*,*,#10124,.T.);
#13796=ORIENTED_EDGE('',*,*,#10125,.T.);
#13797=ORIENTED_EDGE('',*,*,#10126,.T.);
#13798=ORIENTED_EDGE('',*,*,#10127,.T.);
#13799=ORIENTED_EDGE('',*,*,#10128,.T.);
#13800=ORIENTED_EDGE('',*,*,#10129,.T.);
#13801=ORIENTED_EDGE('',*,*,#10130,.T.);
#13802=ORIENTED_EDGE('',*,*,#10131,.T.);
#13803=ORIENTED_EDGE('',*,*,#10132,.T.);
#13804=ORIENTED_EDGE('',*,*,#10133,.T.);
#13805=ORIENTED_EDGE('',*,*,#10134,.T.);
#13806=ORIENTED_EDGE('',*,*,#10135,.T.);
#13807=ORIENTED_EDGE('',*,*,#10136,.T.);
#13808=ORIENTED_EDGE('',*,*,#10137,.T.);
#13809=ORIENTED_EDGE('',*,*,#10138,.T.);
#13810=ORIENTED_EDGE('',*,*,#10139,.T.);
#13811=ORIENTED_EDGE('',*,*,#10140,.T.);
#13812=ORIENTED_EDGE('',*,*,#10141,.T.);
#13813=ORIENTED_EDGE('',*,*,#10142,.T.);
#13814=ORIENTED_EDGE('',*,*,#10143,.T.);
#13815=ORIENTED_EDGE('',*,*,#10144,.T.);
#13816=ORIENTED_EDGE('',*,*,#10145,.T.);
#13817=ORIENTED_EDGE('',*,*,#10146,.T.);
#13818=ORIENTED_EDGE('',*,*,#10147,.T.);
#13819=ORIENTED_EDGE('',*,*,#10148,.T.);
#13820=ORIENTED_EDGE('',*,*,#10149,.T.);
#13821=ORIENTED_EDGE('',*,*,#10150,.T.);
#13822=ORIENTED_EDGE('',*,*,#10151,.T.);
#13823=ORIENTED_EDGE('',*,*,#10152,.T.);
#13824=ORIENTED_EDGE('',*,*,#10153,.T.);
#13825=ORIENTED_EDGE('',*,*,#10154,.T.);
#13826=ORIENTED_EDGE('',*,*,#10155,.T.);
#13827=ORIENTED_EDGE('',*,*,#10156,.T.);
#13828=ORIENTED_EDGE('',*,*,#10157,.T.);
#13829=ORIENTED_EDGE('',*,*,#10158,.T.);
#13830=ORIENTED_EDGE('',*,*,#10159,.T.);
#13831=ORIENTED_EDGE('',*,*,#10160,.T.);
#13832=ORIENTED_EDGE('',*,*,#10161,.T.);
#13833=ORIENTED_EDGE('',*,*,#10162,.T.);
#13834=ORIENTED_EDGE('',*,*,#10163,.T.);
#13835=ORIENTED_EDGE('',*,*,#10164,.T.);
#13836=ORIENTED_EDGE('',*,*,#10165,.T.);
#13837=ORIENTED_EDGE('',*,*,#10166,.T.);
#13838=ORIENTED_EDGE('',*,*,#10167,.T.);
#13839=ORIENTED_EDGE('',*,*,#10168,.T.);
#13840=ORIENTED_EDGE('',*,*,#10169,.T.);
#13841=ORIENTED_EDGE('',*,*,#10170,.T.);
#13842=ORIENTED_EDGE('',*,*,#10171,.T.);
#13843=ORIENTED_EDGE('',*,*,#10172,.T.);
#13844=ORIENTED_EDGE('',*,*,#10173,.T.);
#13845=ORIENTED_EDGE('',*,*,#10174,.T.);
#13846=ORIENTED_EDGE('',*,*,#10175,.T.);
#13847=ORIENTED_EDGE('',*,*,#10176,.T.);
#13848=ORIENTED_EDGE('',*,*,#10177,.T.);
#13849=ORIENTED_EDGE('',*,*,#10178,.T.);
#13850=ORIENTED_EDGE('',*,*,#10179,.T.);
#13851=ORIENTED_EDGE('',*,*,#10180,.T.);
#13852=ORIENTED_EDGE('',*,*,#10181,.T.);
#13853=ORIENTED_EDGE('',*,*,#10182,.T.);
#13854=ORIENTED_EDGE('',*,*,#10183,.T.);
#13855=ORIENTED_EDGE('',*,*,#10184,.F.);
#13856=ORIENTED_EDGE('',*,*,#10096,.T.);
#13857=ORIENTED_EDGE('',*,*,#10185,.T.);
#13858=ORIENTED_EDGE('',*,*,#10186,.T.);
#13859=ORIENTED_EDGE('',*,*,#10187,.T.);
#13860=ORIENTED_EDGE('',*,*,#10188,.T.);
#13861=ORIENTED_EDGE('',*,*,#10189,.T.);
#13862=ORIENTED_EDGE('',*,*,#10190,.T.);
#13863=ORIENTED_EDGE('',*,*,#10186,.F.);
#13864=ORIENTED_EDGE('',*,*,#10191,.T.);
#13865=ORIENTED_EDGE('',*,*,#10192,.T.);
#13866=ORIENTED_EDGE('',*,*,#10193,.T.);
#13867=ORIENTED_EDGE('',*,*,#10192,.F.);
#13868=ORIENTED_EDGE('',*,*,#10194,.T.);
#13869=ORIENTED_EDGE('',*,*,#10195,.T.);
#13870=ORIENTED_EDGE('',*,*,#10196,.T.);
#13871=ORIENTED_EDGE('',*,*,#10197,.F.);
#13872=ORIENTED_EDGE('',*,*,#10198,.T.);
#13873=ORIENTED_EDGE('',*,*,#10188,.F.);
#13874=ORIENTED_EDGE('',*,*,#10199,.T.);
#13875=ORIENTED_EDGE('',*,*,#10197,.T.);
#13876=ORIENTED_EDGE('',*,*,#10189,.F.);
#13877=ORIENTED_EDGE('',*,*,#10198,.F.);
#13878=ORIENTED_EDGE('',*,*,#10196,.F.);
#13879=ORIENTED_EDGE('',*,*,#10200,.F.);
#13880=ORIENTED_EDGE('',*,*,#10085,.F.);
#13881=ORIENTED_EDGE('',*,*,#10089,.F.);
#13882=ORIENTED_EDGE('',*,*,#10093,.F.);
#13883=ORIENTED_EDGE('',*,*,#10094,.T.);
#13884=ORIENTED_EDGE('',*,*,#10200,.T.);
#13885=ORIENTED_EDGE('',*,*,#10195,.F.);
#13886=ORIENTED_EDGE('',*,*,#10201,.T.);
#13887=ORIENTED_EDGE('',*,*,#10086,.F.);
#13888=ORIENTED_EDGE('',*,*,#10202,.F.);
#13889=ORIENTED_EDGE('',*,*,#10203,.F.);
#13890=ORIENTED_EDGE('',*,*,#10204,.T.);
#13891=ORIENTED_EDGE('',*,*,#10205,.T.);
#13892=ORIENTED_EDGE('',*,*,#10206,.T.);
#13893=ORIENTED_EDGE('',*,*,#10207,.T.);
#13894=ORIENTED_EDGE('',*,*,#10208,.T.);
#13895=ORIENTED_EDGE('',*,*,#10209,.T.);
#13896=ORIENTED_EDGE('',*,*,#10210,.T.);
#13897=ORIENTED_EDGE('',*,*,#10211,.T.);
#13898=ORIENTED_EDGE('',*,*,#10212,.T.);
#13899=ORIENTED_EDGE('',*,*,#10213,.T.);
#13900=ORIENTED_EDGE('',*,*,#10214,.T.);
#13901=ORIENTED_EDGE('',*,*,#10215,.T.);
#13902=ORIENTED_EDGE('',*,*,#10216,.T.);
#13903=ORIENTED_EDGE('',*,*,#10217,.T.);
#13904=ORIENTED_EDGE('',*,*,#10218,.T.);
#13905=ORIENTED_EDGE('',*,*,#10219,.T.);
#13906=ORIENTED_EDGE('',*,*,#10220,.T.);
#13907=ORIENTED_EDGE('',*,*,#10221,.T.);
#13908=ORIENTED_EDGE('',*,*,#10222,.T.);
#13909=ORIENTED_EDGE('',*,*,#10223,.T.);
#13910=ORIENTED_EDGE('',*,*,#10224,.T.);
#13911=ORIENTED_EDGE('',*,*,#10225,.T.);
#13912=ORIENTED_EDGE('',*,*,#10226,.T.);
#13913=ORIENTED_EDGE('',*,*,#10227,.T.);
#13914=ORIENTED_EDGE('',*,*,#10228,.T.);
#13915=ORIENTED_EDGE('',*,*,#10229,.T.);
#13916=ORIENTED_EDGE('',*,*,#10230,.T.);
#13917=ORIENTED_EDGE('',*,*,#10231,.T.);
#13918=ORIENTED_EDGE('',*,*,#10232,.T.);
#13919=ORIENTED_EDGE('',*,*,#10233,.T.);
#13920=ORIENTED_EDGE('',*,*,#10234,.T.);
#13921=ORIENTED_EDGE('',*,*,#10235,.T.);
#13922=ORIENTED_EDGE('',*,*,#10236,.T.);
#13923=ORIENTED_EDGE('',*,*,#10237,.T.);
#13924=ORIENTED_EDGE('',*,*,#10238,.T.);
#13925=ORIENTED_EDGE('',*,*,#10239,.T.);
#13926=ORIENTED_EDGE('',*,*,#10240,.T.);
#13927=ORIENTED_EDGE('',*,*,#10241,.T.);
#13928=ORIENTED_EDGE('',*,*,#10242,.T.);
#13929=ORIENTED_EDGE('',*,*,#10243,.T.);
#13930=ORIENTED_EDGE('',*,*,#10244,.T.);
#13931=ORIENTED_EDGE('',*,*,#10245,.T.);
#13932=ORIENTED_EDGE('',*,*,#10246,.T.);
#13933=ORIENTED_EDGE('',*,*,#10247,.T.);
#13934=ORIENTED_EDGE('',*,*,#10248,.T.);
#13935=ORIENTED_EDGE('',*,*,#10249,.T.);
#13936=ORIENTED_EDGE('',*,*,#10250,.T.);
#13937=ORIENTED_EDGE('',*,*,#10251,.T.);
#13938=ORIENTED_EDGE('',*,*,#10252,.T.);
#13939=ORIENTED_EDGE('',*,*,#10253,.T.);
#13940=ORIENTED_EDGE('',*,*,#10254,.T.);
#13941=ORIENTED_EDGE('',*,*,#10255,.T.);
#13942=ORIENTED_EDGE('',*,*,#10256,.T.);
#13943=ORIENTED_EDGE('',*,*,#10257,.T.);
#13944=ORIENTED_EDGE('',*,*,#10258,.T.);
#13945=ORIENTED_EDGE('',*,*,#10259,.T.);
#13946=ORIENTED_EDGE('',*,*,#10260,.T.);
#13947=ORIENTED_EDGE('',*,*,#10261,.T.);
#13948=ORIENTED_EDGE('',*,*,#10262,.T.);
#13949=ORIENTED_EDGE('',*,*,#10263,.T.);
#13950=ORIENTED_EDGE('',*,*,#10264,.T.);
#13951=ORIENTED_EDGE('',*,*,#10265,.T.);
#13952=ORIENTED_EDGE('',*,*,#10266,.T.);
#13953=ORIENTED_EDGE('',*,*,#10267,.T.);
#13954=ORIENTED_EDGE('',*,*,#10268,.T.);
#13955=ORIENTED_EDGE('',*,*,#10269,.T.);
#13956=ORIENTED_EDGE('',*,*,#10270,.T.);
#13957=ORIENTED_EDGE('',*,*,#10271,.T.);
#13958=ORIENTED_EDGE('',*,*,#10272,.T.);
#13959=ORIENTED_EDGE('',*,*,#10273,.T.);
#13960=ORIENTED_EDGE('',*,*,#10274,.T.);
#13961=ORIENTED_EDGE('',*,*,#10275,.T.);
#13962=ORIENTED_EDGE('',*,*,#10276,.T.);
#13963=ORIENTED_EDGE('',*,*,#10277,.T.);
#13964=ORIENTED_EDGE('',*,*,#10278,.T.);
#13965=ORIENTED_EDGE('',*,*,#10279,.T.);
#13966=ORIENTED_EDGE('',*,*,#10280,.T.);
#13967=ORIENTED_EDGE('',*,*,#10281,.T.);
#13968=ORIENTED_EDGE('',*,*,#10282,.T.);
#13969=ORIENTED_EDGE('',*,*,#10283,.T.);
#13970=ORIENTED_EDGE('',*,*,#10284,.T.);
#13971=ORIENTED_EDGE('',*,*,#10285,.T.);
#13972=ORIENTED_EDGE('',*,*,#10286,.T.);
#13973=ORIENTED_EDGE('',*,*,#10287,.T.);
#13974=ORIENTED_EDGE('',*,*,#10288,.T.);
#13975=ORIENTED_EDGE('',*,*,#10289,.F.);
#13976=ORIENTED_EDGE('',*,*,#10187,.F.);
#13977=ORIENTED_EDGE('',*,*,#10190,.F.);
#13978=ORIENTED_EDGE('',*,*,#10193,.F.);
#13979=ORIENTED_EDGE('',*,*,#10199,.F.);
#13980=ORIENTED_EDGE('',*,*,#10097,.T.);
#13981=ORIENTED_EDGE('',*,*,#10290,.T.);
#13982=ORIENTED_EDGE('',*,*,#10291,.T.);
#13983=ORIENTED_EDGE('',*,*,#10290,.F.);
#13984=ORIENTED_EDGE('',*,*,#10291,.F.);
#13985=ORIENTED_EDGE('',*,*,#10292,.T.);
#13986=ORIENTED_EDGE('',*,*,#10293,.F.);
#13987=ORIENTED_EDGE('',*,*,#10292,.F.);
#13988=ORIENTED_EDGE('',*,*,#10202,.T.);
#13989=ORIENTED_EDGE('',*,*,#10294,.T.);
#13990=ORIENTED_EDGE('',*,*,#10293,.T.);
#13991=ORIENTED_EDGE('',*,*,#10294,.F.);
#13992=ORIENTED_EDGE('',*,*,#10184,.T.);
#13993=ORIENTED_EDGE('',*,*,#10295,.T.);
#13994=ORIENTED_EDGE('',*,*,#10296,.T.);
#13995=ORIENTED_EDGE('',*,*,#10295,.F.);
#13996=ORIENTED_EDGE('',*,*,#10296,.F.);
#13997=ORIENTED_EDGE('',*,*,#10297,.T.);
#13998=ORIENTED_EDGE('',*,*,#10298,.F.);
#13999=ORIENTED_EDGE('',*,*,#10297,.F.);
#14000=ORIENTED_EDGE('',*,*,#10289,.T.);
#14001=ORIENTED_EDGE('',*,*,#10299,.T.);
#14002=ORIENTED_EDGE('',*,*,#10298,.T.);
#14003=ORIENTED_EDGE('',*,*,#10299,.F.);
#14004=ORIENTED_EDGE('',*,*,#10098,.T.);
#14005=ORIENTED_EDGE('',*,*,#10300,.T.);
#14006=ORIENTED_EDGE('',*,*,#10301,.T.);
#14007=ORIENTED_EDGE('',*,*,#10300,.F.);
#14008=ORIENTED_EDGE('',*,*,#10301,.F.);
#14009=ORIENTED_EDGE('',*,*,#10302,.T.);
#14010=ORIENTED_EDGE('',*,*,#10303,.F.);
#14011=ORIENTED_EDGE('',*,*,#10302,.F.);
#14012=ORIENTED_EDGE('',*,*,#10203,.T.);
#14013=ORIENTED_EDGE('',*,*,#10304,.T.);
#14014=ORIENTED_EDGE('',*,*,#10303,.T.);
#14015=ORIENTED_EDGE('',*,*,#10304,.F.);
#14016=ORIENTED_EDGE('',*,*,#10090,.T.);
#14017=ORIENTED_EDGE('',*,*,#10305,.T.);
#14018=ORIENTED_EDGE('',*,*,#10306,.T.);
#14019=ORIENTED_EDGE('',*,*,#10305,.F.);
#14020=ORIENTED_EDGE('',*,*,#10306,.F.);
#14021=ORIENTED_EDGE('',*,*,#10307,.T.);
#14022=ORIENTED_EDGE('',*,*,#10308,.F.);
#14023=ORIENTED_EDGE('',*,*,#10309,.F.);
#14024=ORIENTED_EDGE('',*,*,#10310,.F.);
#14025=ORIENTED_EDGE('',*,*,#10307,.F.);
#14026=ORIENTED_EDGE('',*,*,#10275,.F.);
#14027=ORIENTED_EDGE('',*,*,#10311,.T.);
#14028=ORIENTED_EDGE('',*,*,#10312,.T.);
#14029=ORIENTED_EDGE('',*,*,#10313,.F.);
#14030=ORIENTED_EDGE('',*,*,#10288,.F.);
#14031=ORIENTED_EDGE('',*,*,#10314,.T.);
#14032=ORIENTED_EDGE('',*,*,#10315,.T.);
#14033=ORIENTED_EDGE('',*,*,#10311,.F.);
#14034=ORIENTED_EDGE('',*,*,#10287,.F.);
#14035=ORIENTED_EDGE('',*,*,#10316,.T.);
#14036=ORIENTED_EDGE('',*,*,#10317,.T.);
#14037=ORIENTED_EDGE('',*,*,#10314,.F.);
#14038=ORIENTED_EDGE('',*,*,#10286,.F.);
#14039=ORIENTED_EDGE('',*,*,#10318,.T.);
#14040=ORIENTED_EDGE('',*,*,#10319,.T.);
#14041=ORIENTED_EDGE('',*,*,#10316,.F.);
#14042=ORIENTED_EDGE('',*,*,#10285,.F.);
#14043=ORIENTED_EDGE('',*,*,#10320,.T.);
#14044=ORIENTED_EDGE('',*,*,#10321,.T.);
#14045=ORIENTED_EDGE('',*,*,#10318,.F.);
#14046=ORIENTED_EDGE('',*,*,#10284,.F.);
#14047=ORIENTED_EDGE('',*,*,#10322,.T.);
#14048=ORIENTED_EDGE('',*,*,#10323,.T.);
#14049=ORIENTED_EDGE('',*,*,#10320,.F.);
#14050=ORIENTED_EDGE('',*,*,#10283,.F.);
#14051=ORIENTED_EDGE('',*,*,#10324,.T.);
#14052=ORIENTED_EDGE('',*,*,#10325,.T.);
#14053=ORIENTED_EDGE('',*,*,#10322,.F.);
#14054=ORIENTED_EDGE('',*,*,#10282,.F.);
#14055=ORIENTED_EDGE('',*,*,#10326,.T.);
#14056=ORIENTED_EDGE('',*,*,#10327,.T.);
#14057=ORIENTED_EDGE('',*,*,#10324,.F.);
#14058=ORIENTED_EDGE('',*,*,#10281,.F.);
#14059=ORIENTED_EDGE('',*,*,#10328,.T.);
#14060=ORIENTED_EDGE('',*,*,#10329,.T.);
#14061=ORIENTED_EDGE('',*,*,#10326,.F.);
#14062=ORIENTED_EDGE('',*,*,#10280,.F.);
#14063=ORIENTED_EDGE('',*,*,#10330,.T.);
#14064=ORIENTED_EDGE('',*,*,#10331,.T.);
#14065=ORIENTED_EDGE('',*,*,#10328,.F.);
#14066=ORIENTED_EDGE('',*,*,#10279,.F.);
#14067=ORIENTED_EDGE('',*,*,#10332,.T.);
#14068=ORIENTED_EDGE('',*,*,#10333,.T.);
#14069=ORIENTED_EDGE('',*,*,#10330,.F.);
#14070=ORIENTED_EDGE('',*,*,#10278,.F.);
#14071=ORIENTED_EDGE('',*,*,#10334,.T.);
#14072=ORIENTED_EDGE('',*,*,#10335,.T.);
#14073=ORIENTED_EDGE('',*,*,#10332,.F.);
#14074=ORIENTED_EDGE('',*,*,#10277,.F.);
#14075=ORIENTED_EDGE('',*,*,#10336,.T.);
#14076=ORIENTED_EDGE('',*,*,#10337,.T.);
#14077=ORIENTED_EDGE('',*,*,#10334,.F.);
#14078=ORIENTED_EDGE('',*,*,#10276,.F.);
#14079=ORIENTED_EDGE('',*,*,#10313,.T.);
#14080=ORIENTED_EDGE('',*,*,#10338,.T.);
#14081=ORIENTED_EDGE('',*,*,#10336,.F.);
#14082=ORIENTED_EDGE('',*,*,#10338,.F.);
#14083=ORIENTED_EDGE('',*,*,#10312,.F.);
#14084=ORIENTED_EDGE('',*,*,#10315,.F.);
#14085=ORIENTED_EDGE('',*,*,#10317,.F.);
#14086=ORIENTED_EDGE('',*,*,#10319,.F.);
#14087=ORIENTED_EDGE('',*,*,#10321,.F.);
#14088=ORIENTED_EDGE('',*,*,#10323,.F.);
#14089=ORIENTED_EDGE('',*,*,#10325,.F.);
#14090=ORIENTED_EDGE('',*,*,#10327,.F.);
#14091=ORIENTED_EDGE('',*,*,#10329,.F.);
#14092=ORIENTED_EDGE('',*,*,#10331,.F.);
#14093=ORIENTED_EDGE('',*,*,#10333,.F.);
#14094=ORIENTED_EDGE('',*,*,#10335,.F.);
#14095=ORIENTED_EDGE('',*,*,#10337,.F.);
#14096=ORIENTED_EDGE('',*,*,#10261,.F.);
#14097=ORIENTED_EDGE('',*,*,#10339,.T.);
#14098=ORIENTED_EDGE('',*,*,#10340,.T.);
#14099=ORIENTED_EDGE('',*,*,#10341,.F.);
#14100=ORIENTED_EDGE('',*,*,#10274,.F.);
#14101=ORIENTED_EDGE('',*,*,#10342,.T.);
#14102=ORIENTED_EDGE('',*,*,#10343,.T.);
#14103=ORIENTED_EDGE('',*,*,#10339,.F.);
#14104=ORIENTED_EDGE('',*,*,#10273,.F.);
#14105=ORIENTED_EDGE('',*,*,#10344,.T.);
#14106=ORIENTED_EDGE('',*,*,#10345,.T.);
#14107=ORIENTED_EDGE('',*,*,#10342,.F.);
#14108=ORIENTED_EDGE('',*,*,#10272,.F.);
#14109=ORIENTED_EDGE('',*,*,#10346,.T.);
#14110=ORIENTED_EDGE('',*,*,#10347,.T.);
#14111=ORIENTED_EDGE('',*,*,#10344,.F.);
#14112=ORIENTED_EDGE('',*,*,#10271,.F.);
#14113=ORIENTED_EDGE('',*,*,#10348,.T.);
#14114=ORIENTED_EDGE('',*,*,#10349,.T.);
#14115=ORIENTED_EDGE('',*,*,#10346,.F.);
#14116=ORIENTED_EDGE('',*,*,#10270,.F.);
#14117=ORIENTED_EDGE('',*,*,#10350,.T.);
#14118=ORIENTED_EDGE('',*,*,#10351,.T.);
#14119=ORIENTED_EDGE('',*,*,#10348,.F.);
#14120=ORIENTED_EDGE('',*,*,#10269,.F.);
#14121=ORIENTED_EDGE('',*,*,#10352,.T.);
#14122=ORIENTED_EDGE('',*,*,#10353,.T.);
#14123=ORIENTED_EDGE('',*,*,#10350,.F.);
#14124=ORIENTED_EDGE('',*,*,#10268,.F.);
#14125=ORIENTED_EDGE('',*,*,#10354,.T.);
#14126=ORIENTED_EDGE('',*,*,#10355,.T.);
#14127=ORIENTED_EDGE('',*,*,#10352,.F.);
#14128=ORIENTED_EDGE('',*,*,#10267,.F.);
#14129=ORIENTED_EDGE('',*,*,#10356,.T.);
#14130=ORIENTED_EDGE('',*,*,#10357,.T.);
#14131=ORIENTED_EDGE('',*,*,#10354,.F.);
#14132=ORIENTED_EDGE('',*,*,#10266,.F.);
#14133=ORIENTED_EDGE('',*,*,#10358,.T.);
#14134=ORIENTED_EDGE('',*,*,#10359,.T.);
#14135=ORIENTED_EDGE('',*,*,#10356,.F.);
#14136=ORIENTED_EDGE('',*,*,#10265,.F.);
#14137=ORIENTED_EDGE('',*,*,#10360,.T.);
#14138=ORIENTED_EDGE('',*,*,#10361,.T.);
#14139=ORIENTED_EDGE('',*,*,#10358,.F.);
#14140=ORIENTED_EDGE('',*,*,#10264,.F.);
#14141=ORIENTED_EDGE('',*,*,#10362,.T.);
#14142=ORIENTED_EDGE('',*,*,#10363,.T.);
#14143=ORIENTED_EDGE('',*,*,#10360,.F.);
#14144=ORIENTED_EDGE('',*,*,#10263,.F.);
#14145=ORIENTED_EDGE('',*,*,#10364,.T.);
#14146=ORIENTED_EDGE('',*,*,#10365,.T.);
#14147=ORIENTED_EDGE('',*,*,#10362,.F.);
#14148=ORIENTED_EDGE('',*,*,#10262,.F.);
#14149=ORIENTED_EDGE('',*,*,#10341,.T.);
#14150=ORIENTED_EDGE('',*,*,#10366,.T.);
#14151=ORIENTED_EDGE('',*,*,#10364,.F.);
#14152=ORIENTED_EDGE('',*,*,#10366,.F.);
#14153=ORIENTED_EDGE('',*,*,#10340,.F.);
#14154=ORIENTED_EDGE('',*,*,#10343,.F.);
#14155=ORIENTED_EDGE('',*,*,#10345,.F.);
#14156=ORIENTED_EDGE('',*,*,#10347,.F.);
#14157=ORIENTED_EDGE('',*,*,#10349,.F.);
#14158=ORIENTED_EDGE('',*,*,#10351,.F.);
#14159=ORIENTED_EDGE('',*,*,#10353,.F.);
#14160=ORIENTED_EDGE('',*,*,#10355,.F.);
#14161=ORIENTED_EDGE('',*,*,#10357,.F.);
#14162=ORIENTED_EDGE('',*,*,#10359,.F.);
#14163=ORIENTED_EDGE('',*,*,#10361,.F.);
#14164=ORIENTED_EDGE('',*,*,#10363,.F.);
#14165=ORIENTED_EDGE('',*,*,#10365,.F.);
#14166=ORIENTED_EDGE('',*,*,#10247,.F.);
#14167=ORIENTED_EDGE('',*,*,#10367,.T.);
#14168=ORIENTED_EDGE('',*,*,#10368,.T.);
#14169=ORIENTED_EDGE('',*,*,#10369,.F.);
#14170=ORIENTED_EDGE('',*,*,#10260,.F.);
#14171=ORIENTED_EDGE('',*,*,#10370,.T.);
#14172=ORIENTED_EDGE('',*,*,#10371,.T.);
#14173=ORIENTED_EDGE('',*,*,#10367,.F.);
#14174=ORIENTED_EDGE('',*,*,#10259,.F.);
#14175=ORIENTED_EDGE('',*,*,#10372,.T.);
#14176=ORIENTED_EDGE('',*,*,#10373,.T.);
#14177=ORIENTED_EDGE('',*,*,#10370,.F.);
#14178=ORIENTED_EDGE('',*,*,#10258,.F.);
#14179=ORIENTED_EDGE('',*,*,#10374,.T.);
#14180=ORIENTED_EDGE('',*,*,#10375,.T.);
#14181=ORIENTED_EDGE('',*,*,#10372,.F.);
#14182=ORIENTED_EDGE('',*,*,#10257,.F.);
#14183=ORIENTED_EDGE('',*,*,#10376,.T.);
#14184=ORIENTED_EDGE('',*,*,#10377,.T.);
#14185=ORIENTED_EDGE('',*,*,#10374,.F.);
#14186=ORIENTED_EDGE('',*,*,#10256,.F.);
#14187=ORIENTED_EDGE('',*,*,#10378,.T.);
#14188=ORIENTED_EDGE('',*,*,#10379,.T.);
#14189=ORIENTED_EDGE('',*,*,#10376,.F.);
#14190=ORIENTED_EDGE('',*,*,#10255,.F.);
#14191=ORIENTED_EDGE('',*,*,#10380,.T.);
#14192=ORIENTED_EDGE('',*,*,#10381,.T.);
#14193=ORIENTED_EDGE('',*,*,#10378,.F.);
#14194=ORIENTED_EDGE('',*,*,#10254,.F.);
#14195=ORIENTED_EDGE('',*,*,#10382,.T.);
#14196=ORIENTED_EDGE('',*,*,#10383,.T.);
#14197=ORIENTED_EDGE('',*,*,#10380,.F.);
#14198=ORIENTED_EDGE('',*,*,#10253,.F.);
#14199=ORIENTED_EDGE('',*,*,#10384,.T.);
#14200=ORIENTED_EDGE('',*,*,#10385,.T.);
#14201=ORIENTED_EDGE('',*,*,#10382,.F.);
#14202=ORIENTED_EDGE('',*,*,#10252,.F.);
#14203=ORIENTED_EDGE('',*,*,#10386,.T.);
#14204=ORIENTED_EDGE('',*,*,#10387,.T.);
#14205=ORIENTED_EDGE('',*,*,#10384,.F.);
#14206=ORIENTED_EDGE('',*,*,#10251,.F.);
#14207=ORIENTED_EDGE('',*,*,#10388,.T.);
#14208=ORIENTED_EDGE('',*,*,#10389,.T.);
#14209=ORIENTED_EDGE('',*,*,#10386,.F.);
#14210=ORIENTED_EDGE('',*,*,#10250,.F.);
#14211=ORIENTED_EDGE('',*,*,#10390,.T.);
#14212=ORIENTED_EDGE('',*,*,#10391,.T.);
#14213=ORIENTED_EDGE('',*,*,#10388,.F.);
#14214=ORIENTED_EDGE('',*,*,#10249,.F.);
#14215=ORIENTED_EDGE('',*,*,#10392,.T.);
#14216=ORIENTED_EDGE('',*,*,#10393,.T.);
#14217=ORIENTED_EDGE('',*,*,#10390,.F.);
#14218=ORIENTED_EDGE('',*,*,#10248,.F.);
#14219=ORIENTED_EDGE('',*,*,#10369,.T.);
#14220=ORIENTED_EDGE('',*,*,#10394,.T.);
#14221=ORIENTED_EDGE('',*,*,#10392,.F.);
#14222=ORIENTED_EDGE('',*,*,#10394,.F.);
#14223=ORIENTED_EDGE('',*,*,#10368,.F.);
#14224=ORIENTED_EDGE('',*,*,#10371,.F.);
#14225=ORIENTED_EDGE('',*,*,#10373,.F.);
#14226=ORIENTED_EDGE('',*,*,#10375,.F.);
#14227=ORIENTED_EDGE('',*,*,#10377,.F.);
#14228=ORIENTED_EDGE('',*,*,#10379,.F.);
#14229=ORIENTED_EDGE('',*,*,#10381,.F.);
#14230=ORIENTED_EDGE('',*,*,#10383,.F.);
#14231=ORIENTED_EDGE('',*,*,#10385,.F.);
#14232=ORIENTED_EDGE('',*,*,#10387,.F.);
#14233=ORIENTED_EDGE('',*,*,#10389,.F.);
#14234=ORIENTED_EDGE('',*,*,#10391,.F.);
#14235=ORIENTED_EDGE('',*,*,#10393,.F.);
#14236=ORIENTED_EDGE('',*,*,#10233,.F.);
#14237=ORIENTED_EDGE('',*,*,#10395,.T.);
#14238=ORIENTED_EDGE('',*,*,#10396,.T.);
#14239=ORIENTED_EDGE('',*,*,#10397,.F.);
#14240=ORIENTED_EDGE('',*,*,#10246,.F.);
#14241=ORIENTED_EDGE('',*,*,#10398,.T.);
#14242=ORIENTED_EDGE('',*,*,#10399,.T.);
#14243=ORIENTED_EDGE('',*,*,#10395,.F.);
#14244=ORIENTED_EDGE('',*,*,#10245,.F.);
#14245=ORIENTED_EDGE('',*,*,#10400,.T.);
#14246=ORIENTED_EDGE('',*,*,#10401,.T.);
#14247=ORIENTED_EDGE('',*,*,#10398,.F.);
#14248=ORIENTED_EDGE('',*,*,#10244,.F.);
#14249=ORIENTED_EDGE('',*,*,#10402,.T.);
#14250=ORIENTED_EDGE('',*,*,#10403,.T.);
#14251=ORIENTED_EDGE('',*,*,#10400,.F.);
#14252=ORIENTED_EDGE('',*,*,#10243,.F.);
#14253=ORIENTED_EDGE('',*,*,#10404,.T.);
#14254=ORIENTED_EDGE('',*,*,#10405,.T.);
#14255=ORIENTED_EDGE('',*,*,#10402,.F.);
#14256=ORIENTED_EDGE('',*,*,#10242,.F.);
#14257=ORIENTED_EDGE('',*,*,#10406,.T.);
#14258=ORIENTED_EDGE('',*,*,#10407,.T.);
#14259=ORIENTED_EDGE('',*,*,#10404,.F.);
#14260=ORIENTED_EDGE('',*,*,#10241,.F.);
#14261=ORIENTED_EDGE('',*,*,#10408,.T.);
#14262=ORIENTED_EDGE('',*,*,#10409,.T.);
#14263=ORIENTED_EDGE('',*,*,#10406,.F.);
#14264=ORIENTED_EDGE('',*,*,#10240,.F.);
#14265=ORIENTED_EDGE('',*,*,#10410,.T.);
#14266=ORIENTED_EDGE('',*,*,#10411,.T.);
#14267=ORIENTED_EDGE('',*,*,#10408,.F.);
#14268=ORIENTED_EDGE('',*,*,#10239,.F.);
#14269=ORIENTED_EDGE('',*,*,#10412,.T.);
#14270=ORIENTED_EDGE('',*,*,#10413,.T.);
#14271=ORIENTED_EDGE('',*,*,#10410,.F.);
#14272=ORIENTED_EDGE('',*,*,#10238,.F.);
#14273=ORIENTED_EDGE('',*,*,#10414,.T.);
#14274=ORIENTED_EDGE('',*,*,#10415,.T.);
#14275=ORIENTED_EDGE('',*,*,#10412,.F.);
#14276=ORIENTED_EDGE('',*,*,#10237,.F.);
#14277=ORIENTED_EDGE('',*,*,#10416,.T.);
#14278=ORIENTED_EDGE('',*,*,#10417,.T.);
#14279=ORIENTED_EDGE('',*,*,#10414,.F.);
#14280=ORIENTED_EDGE('',*,*,#10236,.F.);
#14281=ORIENTED_EDGE('',*,*,#10418,.T.);
#14282=ORIENTED_EDGE('',*,*,#10419,.T.);
#14283=ORIENTED_EDGE('',*,*,#10416,.F.);
#14284=ORIENTED_EDGE('',*,*,#10235,.F.);
#14285=ORIENTED_EDGE('',*,*,#10420,.T.);
#14286=ORIENTED_EDGE('',*,*,#10421,.T.);
#14287=ORIENTED_EDGE('',*,*,#10418,.F.);
#14288=ORIENTED_EDGE('',*,*,#10234,.F.);
#14289=ORIENTED_EDGE('',*,*,#10397,.T.);
#14290=ORIENTED_EDGE('',*,*,#10422,.T.);
#14291=ORIENTED_EDGE('',*,*,#10420,.F.);
#14292=ORIENTED_EDGE('',*,*,#10422,.F.);
#14293=ORIENTED_EDGE('',*,*,#10396,.F.);
#14294=ORIENTED_EDGE('',*,*,#10399,.F.);
#14295=ORIENTED_EDGE('',*,*,#10401,.F.);
#14296=ORIENTED_EDGE('',*,*,#10403,.F.);
#14297=ORIENTED_EDGE('',*,*,#10405,.F.);
#14298=ORIENTED_EDGE('',*,*,#10407,.F.);
#14299=ORIENTED_EDGE('',*,*,#10409,.F.);
#14300=ORIENTED_EDGE('',*,*,#10411,.F.);
#14301=ORIENTED_EDGE('',*,*,#10413,.F.);
#14302=ORIENTED_EDGE('',*,*,#10415,.F.);
#14303=ORIENTED_EDGE('',*,*,#10417,.F.);
#14304=ORIENTED_EDGE('',*,*,#10419,.F.);
#14305=ORIENTED_EDGE('',*,*,#10421,.F.);
#14306=ORIENTED_EDGE('',*,*,#10219,.F.);
#14307=ORIENTED_EDGE('',*,*,#10423,.T.);
#14308=ORIENTED_EDGE('',*,*,#10424,.T.);
#14309=ORIENTED_EDGE('',*,*,#10425,.F.);
#14310=ORIENTED_EDGE('',*,*,#10232,.F.);
#14311=ORIENTED_EDGE('',*,*,#10426,.T.);
#14312=ORIENTED_EDGE('',*,*,#10427,.T.);
#14313=ORIENTED_EDGE('',*,*,#10423,.F.);
#14314=ORIENTED_EDGE('',*,*,#10231,.F.);
#14315=ORIENTED_EDGE('',*,*,#10428,.T.);
#14316=ORIENTED_EDGE('',*,*,#10429,.T.);
#14317=ORIENTED_EDGE('',*,*,#10426,.F.);
#14318=ORIENTED_EDGE('',*,*,#10230,.F.);
#14319=ORIENTED_EDGE('',*,*,#10430,.T.);
#14320=ORIENTED_EDGE('',*,*,#10431,.T.);
#14321=ORIENTED_EDGE('',*,*,#10428,.F.);
#14322=ORIENTED_EDGE('',*,*,#10229,.F.);
#14323=ORIENTED_EDGE('',*,*,#10432,.T.);
#14324=ORIENTED_EDGE('',*,*,#10433,.T.);
#14325=ORIENTED_EDGE('',*,*,#10430,.F.);
#14326=ORIENTED_EDGE('',*,*,#10228,.F.);
#14327=ORIENTED_EDGE('',*,*,#10434,.T.);
#14328=ORIENTED_EDGE('',*,*,#10435,.T.);
#14329=ORIENTED_EDGE('',*,*,#10432,.F.);
#14330=ORIENTED_EDGE('',*,*,#10227,.F.);
#14331=ORIENTED_EDGE('',*,*,#10436,.T.);
#14332=ORIENTED_EDGE('',*,*,#10437,.T.);
#14333=ORIENTED_EDGE('',*,*,#10434,.F.);
#14334=ORIENTED_EDGE('',*,*,#10226,.F.);
#14335=ORIENTED_EDGE('',*,*,#10438,.T.);
#14336=ORIENTED_EDGE('',*,*,#10439,.T.);
#14337=ORIENTED_EDGE('',*,*,#10436,.F.);
#14338=ORIENTED_EDGE('',*,*,#10225,.F.);
#14339=ORIENTED_EDGE('',*,*,#10440,.T.);
#14340=ORIENTED_EDGE('',*,*,#10441,.T.);
#14341=ORIENTED_EDGE('',*,*,#10438,.F.);
#14342=ORIENTED_EDGE('',*,*,#10224,.F.);
#14343=ORIENTED_EDGE('',*,*,#10442,.T.);
#14344=ORIENTED_EDGE('',*,*,#10443,.T.);
#14345=ORIENTED_EDGE('',*,*,#10440,.F.);
#14346=ORIENTED_EDGE('',*,*,#10223,.F.);
#14347=ORIENTED_EDGE('',*,*,#10444,.T.);
#14348=ORIENTED_EDGE('',*,*,#10445,.T.);
#14349=ORIENTED_EDGE('',*,*,#10442,.F.);
#14350=ORIENTED_EDGE('',*,*,#10222,.F.);
#14351=ORIENTED_EDGE('',*,*,#10446,.T.);
#14352=ORIENTED_EDGE('',*,*,#10447,.T.);
#14353=ORIENTED_EDGE('',*,*,#10444,.F.);
#14354=ORIENTED_EDGE('',*,*,#10221,.F.);
#14355=ORIENTED_EDGE('',*,*,#10448,.T.);
#14356=ORIENTED_EDGE('',*,*,#10449,.T.);
#14357=ORIENTED_EDGE('',*,*,#10446,.F.);
#14358=ORIENTED_EDGE('',*,*,#10220,.F.);
#14359=ORIENTED_EDGE('',*,*,#10425,.T.);
#14360=ORIENTED_EDGE('',*,*,#10450,.T.);
#14361=ORIENTED_EDGE('',*,*,#10448,.F.);
#14362=ORIENTED_EDGE('',*,*,#10450,.F.);
#14363=ORIENTED_EDGE('',*,*,#10424,.F.);
#14364=ORIENTED_EDGE('',*,*,#10427,.F.);
#14365=ORIENTED_EDGE('',*,*,#10429,.F.);
#14366=ORIENTED_EDGE('',*,*,#10431,.F.);
#14367=ORIENTED_EDGE('',*,*,#10433,.F.);
#14368=ORIENTED_EDGE('',*,*,#10435,.F.);
#14369=ORIENTED_EDGE('',*,*,#10437,.F.);
#14370=ORIENTED_EDGE('',*,*,#10439,.F.);
#14371=ORIENTED_EDGE('',*,*,#10441,.F.);
#14372=ORIENTED_EDGE('',*,*,#10443,.F.);
#14373=ORIENTED_EDGE('',*,*,#10445,.F.);
#14374=ORIENTED_EDGE('',*,*,#10447,.F.);
#14375=ORIENTED_EDGE('',*,*,#10449,.F.);
#14376=ORIENTED_EDGE('',*,*,#10205,.F.);
#14377=ORIENTED_EDGE('',*,*,#10451,.T.);
#14378=ORIENTED_EDGE('',*,*,#10452,.T.);
#14379=ORIENTED_EDGE('',*,*,#10453,.F.);
#14380=ORIENTED_EDGE('',*,*,#10218,.F.);
#14381=ORIENTED_EDGE('',*,*,#10454,.T.);
#14382=ORIENTED_EDGE('',*,*,#10455,.T.);
#14383=ORIENTED_EDGE('',*,*,#10451,.F.);
#14384=ORIENTED_EDGE('',*,*,#10217,.F.);
#14385=ORIENTED_EDGE('',*,*,#10456,.T.);
#14386=ORIENTED_EDGE('',*,*,#10457,.T.);
#14387=ORIENTED_EDGE('',*,*,#10454,.F.);
#14388=ORIENTED_EDGE('',*,*,#10216,.F.);
#14389=ORIENTED_EDGE('',*,*,#10458,.T.);
#14390=ORIENTED_EDGE('',*,*,#10459,.T.);
#14391=ORIENTED_EDGE('',*,*,#10456,.F.);
#14392=ORIENTED_EDGE('',*,*,#10215,.F.);
#14393=ORIENTED_EDGE('',*,*,#10460,.T.);
#14394=ORIENTED_EDGE('',*,*,#10461,.T.);
#14395=ORIENTED_EDGE('',*,*,#10458,.F.);
#14396=ORIENTED_EDGE('',*,*,#10214,.F.);
#14397=ORIENTED_EDGE('',*,*,#10462,.T.);
#14398=ORIENTED_EDGE('',*,*,#10463,.T.);
#14399=ORIENTED_EDGE('',*,*,#10460,.F.);
#14400=ORIENTED_EDGE('',*,*,#10213,.F.);
#14401=ORIENTED_EDGE('',*,*,#10464,.T.);
#14402=ORIENTED_EDGE('',*,*,#10465,.T.);
#14403=ORIENTED_EDGE('',*,*,#10462,.F.);
#14404=ORIENTED_EDGE('',*,*,#10212,.F.);
#14405=ORIENTED_EDGE('',*,*,#10466,.T.);
#14406=ORIENTED_EDGE('',*,*,#10467,.T.);
#14407=ORIENTED_EDGE('',*,*,#10464,.F.);
#14408=ORIENTED_EDGE('',*,*,#10211,.F.);
#14409=ORIENTED_EDGE('',*,*,#10468,.T.);
#14410=ORIENTED_EDGE('',*,*,#10469,.T.);
#14411=ORIENTED_EDGE('',*,*,#10466,.F.);
#14412=ORIENTED_EDGE('',*,*,#10210,.F.);
#14413=ORIENTED_EDGE('',*,*,#10470,.T.);
#14414=ORIENTED_EDGE('',*,*,#10471,.T.);
#14415=ORIENTED_EDGE('',*,*,#10468,.F.);
#14416=ORIENTED_EDGE('',*,*,#10209,.F.);
#14417=ORIENTED_EDGE('',*,*,#10472,.T.);
#14418=ORIENTED_EDGE('',*,*,#10473,.T.);
#14419=ORIENTED_EDGE('',*,*,#10470,.F.);
#14420=ORIENTED_EDGE('',*,*,#10208,.F.);
#14421=ORIENTED_EDGE('',*,*,#10474,.T.);
#14422=ORIENTED_EDGE('',*,*,#10475,.T.);
#14423=ORIENTED_EDGE('',*,*,#10472,.F.);
#14424=ORIENTED_EDGE('',*,*,#10207,.F.);
#14425=ORIENTED_EDGE('',*,*,#10476,.T.);
#14426=ORIENTED_EDGE('',*,*,#10477,.T.);
#14427=ORIENTED_EDGE('',*,*,#10474,.F.);
#14428=ORIENTED_EDGE('',*,*,#10206,.F.);
#14429=ORIENTED_EDGE('',*,*,#10453,.T.);
#14430=ORIENTED_EDGE('',*,*,#10478,.T.);
#14431=ORIENTED_EDGE('',*,*,#10476,.F.);
#14432=ORIENTED_EDGE('',*,*,#10478,.F.);
#14433=ORIENTED_EDGE('',*,*,#10452,.F.);
#14434=ORIENTED_EDGE('',*,*,#10455,.F.);
#14435=ORIENTED_EDGE('',*,*,#10457,.F.);
#14436=ORIENTED_EDGE('',*,*,#10459,.F.);
#14437=ORIENTED_EDGE('',*,*,#10461,.F.);
#14438=ORIENTED_EDGE('',*,*,#10463,.F.);
#14439=ORIENTED_EDGE('',*,*,#10465,.F.);
#14440=ORIENTED_EDGE('',*,*,#10467,.F.);
#14441=ORIENTED_EDGE('',*,*,#10469,.F.);
#14442=ORIENTED_EDGE('',*,*,#10471,.F.);
#14443=ORIENTED_EDGE('',*,*,#10473,.F.);
#14444=ORIENTED_EDGE('',*,*,#10475,.F.);
#14445=ORIENTED_EDGE('',*,*,#10477,.F.);
#14446=ORIENTED_EDGE('',*,*,#10170,.F.);
#14447=ORIENTED_EDGE('',*,*,#10479,.T.);
#14448=ORIENTED_EDGE('',*,*,#10480,.T.);
#14449=ORIENTED_EDGE('',*,*,#10481,.F.);
#14450=ORIENTED_EDGE('',*,*,#10183,.F.);
#14451=ORIENTED_EDGE('',*,*,#10482,.T.);
#14452=ORIENTED_EDGE('',*,*,#10483,.T.);
#14453=ORIENTED_EDGE('',*,*,#10479,.F.);
#14454=ORIENTED_EDGE('',*,*,#10182,.F.);
#14455=ORIENTED_EDGE('',*,*,#10484,.T.);
#14456=ORIENTED_EDGE('',*,*,#10485,.T.);
#14457=ORIENTED_EDGE('',*,*,#10482,.F.);
#14458=ORIENTED_EDGE('',*,*,#10181,.F.);
#14459=ORIENTED_EDGE('',*,*,#10486,.T.);
#14460=ORIENTED_EDGE('',*,*,#10487,.T.);
#14461=ORIENTED_EDGE('',*,*,#10484,.F.);
#14462=ORIENTED_EDGE('',*,*,#10180,.F.);
#14463=ORIENTED_EDGE('',*,*,#10488,.T.);
#14464=ORIENTED_EDGE('',*,*,#10489,.T.);
#14465=ORIENTED_EDGE('',*,*,#10486,.F.);
#14466=ORIENTED_EDGE('',*,*,#10179,.F.);
#14467=ORIENTED_EDGE('',*,*,#10490,.T.);
#14468=ORIENTED_EDGE('',*,*,#10491,.T.);
#14469=ORIENTED_EDGE('',*,*,#10488,.F.);
#14470=ORIENTED_EDGE('',*,*,#10178,.F.);
#14471=ORIENTED_EDGE('',*,*,#10492,.T.);
#14472=ORIENTED_EDGE('',*,*,#10493,.T.);
#14473=ORIENTED_EDGE('',*,*,#10490,.F.);
#14474=ORIENTED_EDGE('',*,*,#10177,.F.);
#14475=ORIENTED_EDGE('',*,*,#10494,.T.);
#14476=ORIENTED_EDGE('',*,*,#10495,.T.);
#14477=ORIENTED_EDGE('',*,*,#10492,.F.);
#14478=ORIENTED_EDGE('',*,*,#10176,.F.);
#14479=ORIENTED_EDGE('',*,*,#10496,.T.);
#14480=ORIENTED_EDGE('',*,*,#10497,.T.);
#14481=ORIENTED_EDGE('',*,*,#10494,.F.);
#14482=ORIENTED_EDGE('',*,*,#10175,.F.);
#14483=ORIENTED_EDGE('',*,*,#10498,.T.);
#14484=ORIENTED_EDGE('',*,*,#10499,.T.);
#14485=ORIENTED_EDGE('',*,*,#10496,.F.);
#14486=ORIENTED_EDGE('',*,*,#10174,.F.);
#14487=ORIENTED_EDGE('',*,*,#10500,.T.);
#14488=ORIENTED_EDGE('',*,*,#10501,.T.);
#14489=ORIENTED_EDGE('',*,*,#10498,.F.);
#14490=ORIENTED_EDGE('',*,*,#10173,.F.);
#14491=ORIENTED_EDGE('',*,*,#10502,.T.);
#14492=ORIENTED_EDGE('',*,*,#10503,.T.);
#14493=ORIENTED_EDGE('',*,*,#10500,.F.);
#14494=ORIENTED_EDGE('',*,*,#10172,.F.);
#14495=ORIENTED_EDGE('',*,*,#10504,.T.);
#14496=ORIENTED_EDGE('',*,*,#10505,.T.);
#14497=ORIENTED_EDGE('',*,*,#10502,.F.);
#14498=ORIENTED_EDGE('',*,*,#10171,.F.);
#14499=ORIENTED_EDGE('',*,*,#10481,.T.);
#14500=ORIENTED_EDGE('',*,*,#10506,.T.);
#14501=ORIENTED_EDGE('',*,*,#10504,.F.);
#14502=ORIENTED_EDGE('',*,*,#10506,.F.);
#14503=ORIENTED_EDGE('',*,*,#10480,.F.);
#14504=ORIENTED_EDGE('',*,*,#10483,.F.);
#14505=ORIENTED_EDGE('',*,*,#10485,.F.);
#14506=ORIENTED_EDGE('',*,*,#10487,.F.);
#14507=ORIENTED_EDGE('',*,*,#10489,.F.);
#14508=ORIENTED_EDGE('',*,*,#10491,.F.);
#14509=ORIENTED_EDGE('',*,*,#10493,.F.);
#14510=ORIENTED_EDGE('',*,*,#10495,.F.);
#14511=ORIENTED_EDGE('',*,*,#10497,.F.);
#14512=ORIENTED_EDGE('',*,*,#10499,.F.);
#14513=ORIENTED_EDGE('',*,*,#10501,.F.);
#14514=ORIENTED_EDGE('',*,*,#10503,.F.);
#14515=ORIENTED_EDGE('',*,*,#10505,.F.);
#14516=ORIENTED_EDGE('',*,*,#10156,.F.);
#14517=ORIENTED_EDGE('',*,*,#10507,.T.);
#14518=ORIENTED_EDGE('',*,*,#10508,.T.);
#14519=ORIENTED_EDGE('',*,*,#10509,.F.);
#14520=ORIENTED_EDGE('',*,*,#10169,.F.);
#14521=ORIENTED_EDGE('',*,*,#10510,.T.);
#14522=ORIENTED_EDGE('',*,*,#10511,.T.);
#14523=ORIENTED_EDGE('',*,*,#10507,.F.);
#14524=ORIENTED_EDGE('',*,*,#10168,.F.);
#14525=ORIENTED_EDGE('',*,*,#10512,.T.);
#14526=ORIENTED_EDGE('',*,*,#10513,.T.);
#14527=ORIENTED_EDGE('',*,*,#10510,.F.);
#14528=ORIENTED_EDGE('',*,*,#10167,.F.);
#14529=ORIENTED_EDGE('',*,*,#10514,.T.);
#14530=ORIENTED_EDGE('',*,*,#10515,.T.);
#14531=ORIENTED_EDGE('',*,*,#10512,.F.);
#14532=ORIENTED_EDGE('',*,*,#10166,.F.);
#14533=ORIENTED_EDGE('',*,*,#10516,.T.);
#14534=ORIENTED_EDGE('',*,*,#10517,.T.);
#14535=ORIENTED_EDGE('',*,*,#10514,.F.);
#14536=ORIENTED_EDGE('',*,*,#10165,.F.);
#14537=ORIENTED_EDGE('',*,*,#10518,.T.);
#14538=ORIENTED_EDGE('',*,*,#10519,.T.);
#14539=ORIENTED_EDGE('',*,*,#10516,.F.);
#14540=ORIENTED_EDGE('',*,*,#10164,.F.);
#14541=ORIENTED_EDGE('',*,*,#10520,.T.);
#14542=ORIENTED_EDGE('',*,*,#10521,.T.);
#14543=ORIENTED_EDGE('',*,*,#10518,.F.);
#14544=ORIENTED_EDGE('',*,*,#10163,.F.);
#14545=ORIENTED_EDGE('',*,*,#10522,.T.);
#14546=ORIENTED_EDGE('',*,*,#10523,.T.);
#14547=ORIENTED_EDGE('',*,*,#10520,.F.);
#14548=ORIENTED_EDGE('',*,*,#10162,.F.);
#14549=ORIENTED_EDGE('',*,*,#10524,.T.);
#14550=ORIENTED_EDGE('',*,*,#10525,.T.);
#14551=ORIENTED_EDGE('',*,*,#10522,.F.);
#14552=ORIENTED_EDGE('',*,*,#10161,.F.);
#14553=ORIENTED_EDGE('',*,*,#10526,.T.);
#14554=ORIENTED_EDGE('',*,*,#10527,.T.);
#14555=ORIENTED_EDGE('',*,*,#10524,.F.);
#14556=ORIENTED_EDGE('',*,*,#10160,.F.);
#14557=ORIENTED_EDGE('',*,*,#10528,.T.);
#14558=ORIENTED_EDGE('',*,*,#10529,.T.);
#14559=ORIENTED_EDGE('',*,*,#10526,.F.);
#14560=ORIENTED_EDGE('',*,*,#10159,.F.);
#14561=ORIENTED_EDGE('',*,*,#10530,.T.);
#14562=ORIENTED_EDGE('',*,*,#10531,.T.);
#14563=ORIENTED_EDGE('',*,*,#10528,.F.);
#14564=ORIENTED_EDGE('',*,*,#10158,.F.);
#14565=ORIENTED_EDGE('',*,*,#10532,.T.);
#14566=ORIENTED_EDGE('',*,*,#10533,.T.);
#14567=ORIENTED_EDGE('',*,*,#10530,.F.);
#14568=ORIENTED_EDGE('',*,*,#10157,.F.);
#14569=ORIENTED_EDGE('',*,*,#10509,.T.);
#14570=ORIENTED_EDGE('',*,*,#10534,.T.);
#14571=ORIENTED_EDGE('',*,*,#10532,.F.);
#14572=ORIENTED_EDGE('',*,*,#10534,.F.);
#14573=ORIENTED_EDGE('',*,*,#10508,.F.);
#14574=ORIENTED_EDGE('',*,*,#10511,.F.);
#14575=ORIENTED_EDGE('',*,*,#10513,.F.);
#14576=ORIENTED_EDGE('',*,*,#10515,.F.);
#14577=ORIENTED_EDGE('',*,*,#10517,.F.);
#14578=ORIENTED_EDGE('',*,*,#10519,.F.);
#14579=ORIENTED_EDGE('',*,*,#10521,.F.);
#14580=ORIENTED_EDGE('',*,*,#10523,.F.);
#14581=ORIENTED_EDGE('',*,*,#10525,.F.);
#14582=ORIENTED_EDGE('',*,*,#10527,.F.);
#14583=ORIENTED_EDGE('',*,*,#10529,.F.);
#14584=ORIENTED_EDGE('',*,*,#10531,.F.);
#14585=ORIENTED_EDGE('',*,*,#10533,.F.);
#14586=ORIENTED_EDGE('',*,*,#10142,.F.);
#14587=ORIENTED_EDGE('',*,*,#10535,.T.);
#14588=ORIENTED_EDGE('',*,*,#10536,.T.);
#14589=ORIENTED_EDGE('',*,*,#10537,.F.);
#14590=ORIENTED_EDGE('',*,*,#10155,.F.);
#14591=ORIENTED_EDGE('',*,*,#10538,.T.);
#14592=ORIENTED_EDGE('',*,*,#10539,.T.);
#14593=ORIENTED_EDGE('',*,*,#10535,.F.);
#14594=ORIENTED_EDGE('',*,*,#10154,.F.);
#14595=ORIENTED_EDGE('',*,*,#10540,.T.);
#14596=ORIENTED_EDGE('',*,*,#10541,.T.);
#14597=ORIENTED_EDGE('',*,*,#10538,.F.);
#14598=ORIENTED_EDGE('',*,*,#10153,.F.);
#14599=ORIENTED_EDGE('',*,*,#10542,.T.);
#14600=ORIENTED_EDGE('',*,*,#10543,.T.);
#14601=ORIENTED_EDGE('',*,*,#10540,.F.);
#14602=ORIENTED_EDGE('',*,*,#10152,.F.);
#14603=ORIENTED_EDGE('',*,*,#10544,.T.);
#14604=ORIENTED_EDGE('',*,*,#10545,.T.);
#14605=ORIENTED_EDGE('',*,*,#10542,.F.);
#14606=ORIENTED_EDGE('',*,*,#10151,.F.);
#14607=ORIENTED_EDGE('',*,*,#10546,.T.);
#14608=ORIENTED_EDGE('',*,*,#10547,.T.);
#14609=ORIENTED_EDGE('',*,*,#10544,.F.);
#14610=ORIENTED_EDGE('',*,*,#10150,.F.);
#14611=ORIENTED_EDGE('',*,*,#10548,.T.);
#14612=ORIENTED_EDGE('',*,*,#10549,.T.);
#14613=ORIENTED_EDGE('',*,*,#10546,.F.);
#14614=ORIENTED_EDGE('',*,*,#10149,.F.);
#14615=ORIENTED_EDGE('',*,*,#10550,.T.);
#14616=ORIENTED_EDGE('',*,*,#10551,.T.);
#14617=ORIENTED_EDGE('',*,*,#10548,.F.);
#14618=ORIENTED_EDGE('',*,*,#10148,.F.);
#14619=ORIENTED_EDGE('',*,*,#10552,.T.);
#14620=ORIENTED_EDGE('',*,*,#10553,.T.);
#14621=ORIENTED_EDGE('',*,*,#10550,.F.);
#14622=ORIENTED_EDGE('',*,*,#10147,.F.);
#14623=ORIENTED_EDGE('',*,*,#10554,.T.);
#14624=ORIENTED_EDGE('',*,*,#10555,.T.);
#14625=ORIENTED_EDGE('',*,*,#10552,.F.);
#14626=ORIENTED_EDGE('',*,*,#10146,.F.);
#14627=ORIENTED_EDGE('',*,*,#10556,.T.);
#14628=ORIENTED_EDGE('',*,*,#10557,.T.);
#14629=ORIENTED_EDGE('',*,*,#10554,.F.);
#14630=ORIENTED_EDGE('',*,*,#10145,.F.);
#14631=ORIENTED_EDGE('',*,*,#10558,.T.);
#14632=ORIENTED_EDGE('',*,*,#10559,.T.);
#14633=ORIENTED_EDGE('',*,*,#10556,.F.);
#14634=ORIENTED_EDGE('',*,*,#10144,.F.);
#14635=ORIENTED_EDGE('',*,*,#10560,.T.);
#14636=ORIENTED_EDGE('',*,*,#10561,.T.);
#14637=ORIENTED_EDGE('',*,*,#10558,.F.);
#14638=ORIENTED_EDGE('',*,*,#10143,.F.);
#14639=ORIENTED_EDGE('',*,*,#10537,.T.);
#14640=ORIENTED_EDGE('',*,*,#10562,.T.);
#14641=ORIENTED_EDGE('',*,*,#10560,.F.);
#14642=ORIENTED_EDGE('',*,*,#10562,.F.);
#14643=ORIENTED_EDGE('',*,*,#10536,.F.);
#14644=ORIENTED_EDGE('',*,*,#10539,.F.);
#14645=ORIENTED_EDGE('',*,*,#10541,.F.);
#14646=ORIENTED_EDGE('',*,*,#10543,.F.);
#14647=ORIENTED_EDGE('',*,*,#10545,.F.);
#14648=ORIENTED_EDGE('',*,*,#10547,.F.);
#14649=ORIENTED_EDGE('',*,*,#10549,.F.);
#14650=ORIENTED_EDGE('',*,*,#10551,.F.);
#14651=ORIENTED_EDGE('',*,*,#10553,.F.);
#14652=ORIENTED_EDGE('',*,*,#10555,.F.);
#14653=ORIENTED_EDGE('',*,*,#10557,.F.);
#14654=ORIENTED_EDGE('',*,*,#10559,.F.);
#14655=ORIENTED_EDGE('',*,*,#10561,.F.);
#14656=ORIENTED_EDGE('',*,*,#10128,.F.);
#14657=ORIENTED_EDGE('',*,*,#10563,.T.);
#14658=ORIENTED_EDGE('',*,*,#10564,.T.);
#14659=ORIENTED_EDGE('',*,*,#10565,.F.);
#14660=ORIENTED_EDGE('',*,*,#10141,.F.);
#14661=ORIENTED_EDGE('',*,*,#10566,.T.);
#14662=ORIENTED_EDGE('',*,*,#10567,.T.);
#14663=ORIENTED_EDGE('',*,*,#10563,.F.);
#14664=ORIENTED_EDGE('',*,*,#10140,.F.);
#14665=ORIENTED_EDGE('',*,*,#10568,.T.);
#14666=ORIENTED_EDGE('',*,*,#10569,.T.);
#14667=ORIENTED_EDGE('',*,*,#10566,.F.);
#14668=ORIENTED_EDGE('',*,*,#10139,.F.);
#14669=ORIENTED_EDGE('',*,*,#10570,.T.);
#14670=ORIENTED_EDGE('',*,*,#10571,.T.);
#14671=ORIENTED_EDGE('',*,*,#10568,.F.);
#14672=ORIENTED_EDGE('',*,*,#10138,.F.);
#14673=ORIENTED_EDGE('',*,*,#10572,.T.);
#14674=ORIENTED_EDGE('',*,*,#10573,.T.);
#14675=ORIENTED_EDGE('',*,*,#10570,.F.);
#14676=ORIENTED_EDGE('',*,*,#10137,.F.);
#14677=ORIENTED_EDGE('',*,*,#10574,.T.);
#14678=ORIENTED_EDGE('',*,*,#10575,.T.);
#14679=ORIENTED_EDGE('',*,*,#10572,.F.);
#14680=ORIENTED_EDGE('',*,*,#10136,.F.);
#14681=ORIENTED_EDGE('',*,*,#10576,.T.);
#14682=ORIENTED_EDGE('',*,*,#10577,.T.);
#14683=ORIENTED_EDGE('',*,*,#10574,.F.);
#14684=ORIENTED_EDGE('',*,*,#10135,.F.);
#14685=ORIENTED_EDGE('',*,*,#10578,.T.);
#14686=ORIENTED_EDGE('',*,*,#10579,.T.);
#14687=ORIENTED_EDGE('',*,*,#10576,.F.);
#14688=ORIENTED_EDGE('',*,*,#10134,.F.);
#14689=ORIENTED_EDGE('',*,*,#10580,.T.);
#14690=ORIENTED_EDGE('',*,*,#10581,.T.);
#14691=ORIENTED_EDGE('',*,*,#10578,.F.);
#14692=ORIENTED_EDGE('',*,*,#10133,.F.);
#14693=ORIENTED_EDGE('',*,*,#10582,.T.);
#14694=ORIENTED_EDGE('',*,*,#10583,.T.);
#14695=ORIENTED_EDGE('',*,*,#10580,.F.);
#14696=ORIENTED_EDGE('',*,*,#10132,.F.);
#14697=ORIENTED_EDGE('',*,*,#10584,.T.);
#14698=ORIENTED_EDGE('',*,*,#10585,.T.);
#14699=ORIENTED_EDGE('',*,*,#10582,.F.);
#14700=ORIENTED_EDGE('',*,*,#10131,.F.);
#14701=ORIENTED_EDGE('',*,*,#10586,.T.);
#14702=ORIENTED_EDGE('',*,*,#10587,.T.);
#14703=ORIENTED_EDGE('',*,*,#10584,.F.);
#14704=ORIENTED_EDGE('',*,*,#10130,.F.);
#14705=ORIENTED_EDGE('',*,*,#10588,.T.);
#14706=ORIENTED_EDGE('',*,*,#10589,.T.);
#14707=ORIENTED_EDGE('',*,*,#10586,.F.);
#14708=ORIENTED_EDGE('',*,*,#10129,.F.);
#14709=ORIENTED_EDGE('',*,*,#10565,.T.);
#14710=ORIENTED_EDGE('',*,*,#10590,.T.);
#14711=ORIENTED_EDGE('',*,*,#10588,.F.);
#14712=ORIENTED_EDGE('',*,*,#10590,.F.);
#14713=ORIENTED_EDGE('',*,*,#10564,.F.);
#14714=ORIENTED_EDGE('',*,*,#10567,.F.);
#14715=ORIENTED_EDGE('',*,*,#10569,.F.);
#14716=ORIENTED_EDGE('',*,*,#10571,.F.);
#14717=ORIENTED_EDGE('',*,*,#10573,.F.);
#14718=ORIENTED_EDGE('',*,*,#10575,.F.);
#14719=ORIENTED_EDGE('',*,*,#10577,.F.);
#14720=ORIENTED_EDGE('',*,*,#10579,.F.);
#14721=ORIENTED_EDGE('',*,*,#10581,.F.);
#14722=ORIENTED_EDGE('',*,*,#10583,.F.);
#14723=ORIENTED_EDGE('',*,*,#10585,.F.);
#14724=ORIENTED_EDGE('',*,*,#10587,.F.);
#14725=ORIENTED_EDGE('',*,*,#10589,.F.);
#14726=ORIENTED_EDGE('',*,*,#10114,.F.);
#14727=ORIENTED_EDGE('',*,*,#10591,.T.);
#14728=ORIENTED_EDGE('',*,*,#10592,.T.);
#14729=ORIENTED_EDGE('',*,*,#10593,.F.);
#14730=ORIENTED_EDGE('',*,*,#10127,.F.);
#14731=ORIENTED_EDGE('',*,*,#10594,.T.);
#14732=ORIENTED_EDGE('',*,*,#10595,.T.);
#14733=ORIENTED_EDGE('',*,*,#10591,.F.);
#14734=ORIENTED_EDGE('',*,*,#10126,.F.);
#14735=ORIENTED_EDGE('',*,*,#10596,.T.);
#14736=ORIENTED_EDGE('',*,*,#10597,.T.);
#14737=ORIENTED_EDGE('',*,*,#10594,.F.);
#14738=ORIENTED_EDGE('',*,*,#10125,.F.);
#14739=ORIENTED_EDGE('',*,*,#10598,.T.);
#14740=ORIENTED_EDGE('',*,*,#10599,.T.);
#14741=ORIENTED_EDGE('',*,*,#10596,.F.);
#14742=ORIENTED_EDGE('',*,*,#10124,.F.);
#14743=ORIENTED_EDGE('',*,*,#10600,.T.);
#14744=ORIENTED_EDGE('',*,*,#10601,.T.);
#14745=ORIENTED_EDGE('',*,*,#10598,.F.);
#14746=ORIENTED_EDGE('',*,*,#10123,.F.);
#14747=ORIENTED_EDGE('',*,*,#10602,.T.);
#14748=ORIENTED_EDGE('',*,*,#10603,.T.);
#14749=ORIENTED_EDGE('',*,*,#10600,.F.);
#14750=ORIENTED_EDGE('',*,*,#10122,.F.);
#14751=ORIENTED_EDGE('',*,*,#10604,.T.);
#14752=ORIENTED_EDGE('',*,*,#10605,.T.);
#14753=ORIENTED_EDGE('',*,*,#10602,.F.);
#14754=ORIENTED_EDGE('',*,*,#10121,.F.);
#14755=ORIENTED_EDGE('',*,*,#10606,.T.);
#14756=ORIENTED_EDGE('',*,*,#10607,.T.);
#14757=ORIENTED_EDGE('',*,*,#10604,.F.);
#14758=ORIENTED_EDGE('',*,*,#10120,.F.);
#14759=ORIENTED_EDGE('',*,*,#10608,.T.);
#14760=ORIENTED_EDGE('',*,*,#10609,.T.);
#14761=ORIENTED_EDGE('',*,*,#10606,.F.);
#14762=ORIENTED_EDGE('',*,*,#10119,.F.);
#14763=ORIENTED_EDGE('',*,*,#10610,.T.);
#14764=ORIENTED_EDGE('',*,*,#10611,.T.);
#14765=ORIENTED_EDGE('',*,*,#10608,.F.);
#14766=ORIENTED_EDGE('',*,*,#10118,.F.);
#14767=ORIENTED_EDGE('',*,*,#10612,.T.);
#14768=ORIENTED_EDGE('',*,*,#10613,.T.);
#14769=ORIENTED_EDGE('',*,*,#10610,.F.);
#14770=ORIENTED_EDGE('',*,*,#10117,.F.);
#14771=ORIENTED_EDGE('',*,*,#10614,.T.);
#14772=ORIENTED_EDGE('',*,*,#10615,.T.);
#14773=ORIENTED_EDGE('',*,*,#10612,.F.);
#14774=ORIENTED_EDGE('',*,*,#10116,.F.);
#14775=ORIENTED_EDGE('',*,*,#10616,.T.);
#14776=ORIENTED_EDGE('',*,*,#10617,.T.);
#14777=ORIENTED_EDGE('',*,*,#10614,.F.);
#14778=ORIENTED_EDGE('',*,*,#10115,.F.);
#14779=ORIENTED_EDGE('',*,*,#10593,.T.);
#14780=ORIENTED_EDGE('',*,*,#10618,.T.);
#14781=ORIENTED_EDGE('',*,*,#10616,.F.);
#14782=ORIENTED_EDGE('',*,*,#10618,.F.);
#14783=ORIENTED_EDGE('',*,*,#10592,.F.);
#14784=ORIENTED_EDGE('',*,*,#10595,.F.);
#14785=ORIENTED_EDGE('',*,*,#10597,.F.);
#14786=ORIENTED_EDGE('',*,*,#10599,.F.);
#14787=ORIENTED_EDGE('',*,*,#10601,.F.);
#14788=ORIENTED_EDGE('',*,*,#10603,.F.);
#14789=ORIENTED_EDGE('',*,*,#10605,.F.);
#14790=ORIENTED_EDGE('',*,*,#10607,.F.);
#14791=ORIENTED_EDGE('',*,*,#10609,.F.);
#14792=ORIENTED_EDGE('',*,*,#10611,.F.);
#14793=ORIENTED_EDGE('',*,*,#10613,.F.);
#14794=ORIENTED_EDGE('',*,*,#10615,.F.);
#14795=ORIENTED_EDGE('',*,*,#10617,.F.);
#14796=ORIENTED_EDGE('',*,*,#10100,.F.);
#14797=ORIENTED_EDGE('',*,*,#10619,.T.);
#14798=ORIENTED_EDGE('',*,*,#10620,.T.);
#14799=ORIENTED_EDGE('',*,*,#10621,.F.);
#14800=ORIENTED_EDGE('',*,*,#10113,.F.);
#14801=ORIENTED_EDGE('',*,*,#10622,.T.);
#14802=ORIENTED_EDGE('',*,*,#10623,.T.);
#14803=ORIENTED_EDGE('',*,*,#10619,.F.);
#14804=ORIENTED_EDGE('',*,*,#10112,.F.);
#14805=ORIENTED_EDGE('',*,*,#10624,.T.);
#14806=ORIENTED_EDGE('',*,*,#10625,.T.);
#14807=ORIENTED_EDGE('',*,*,#10622,.F.);
#14808=ORIENTED_EDGE('',*,*,#10111,.F.);
#14809=ORIENTED_EDGE('',*,*,#10626,.T.);
#14810=ORIENTED_EDGE('',*,*,#10627,.T.);
#14811=ORIENTED_EDGE('',*,*,#10624,.F.);
#14812=ORIENTED_EDGE('',*,*,#10110,.F.);
#14813=ORIENTED_EDGE('',*,*,#10628,.T.);
#14814=ORIENTED_EDGE('',*,*,#10629,.T.);
#14815=ORIENTED_EDGE('',*,*,#10626,.F.);
#14816=ORIENTED_EDGE('',*,*,#10109,.F.);
#14817=ORIENTED_EDGE('',*,*,#10630,.T.);
#14818=ORIENTED_EDGE('',*,*,#10631,.T.);
#14819=ORIENTED_EDGE('',*,*,#10628,.F.);
#14820=ORIENTED_EDGE('',*,*,#10108,.F.);
#14821=ORIENTED_EDGE('',*,*,#10632,.T.);
#14822=ORIENTED_EDGE('',*,*,#10633,.T.);
#14823=ORIENTED_EDGE('',*,*,#10630,.F.);
#14824=ORIENTED_EDGE('',*,*,#10107,.F.);
#14825=ORIENTED_EDGE('',*,*,#10634,.T.);
#14826=ORIENTED_EDGE('',*,*,#10635,.T.);
#14827=ORIENTED_EDGE('',*,*,#10632,.F.);
#14828=ORIENTED_EDGE('',*,*,#10106,.F.);
#14829=ORIENTED_EDGE('',*,*,#10636,.T.);
#14830=ORIENTED_EDGE('',*,*,#10637,.T.);
#14831=ORIENTED_EDGE('',*,*,#10634,.F.);
#14832=ORIENTED_EDGE('',*,*,#10105,.F.);
#14833=ORIENTED_EDGE('',*,*,#10638,.T.);
#14834=ORIENTED_EDGE('',*,*,#10639,.T.);
#14835=ORIENTED_EDGE('',*,*,#10636,.F.);
#14836=ORIENTED_EDGE('',*,*,#10104,.F.);
#14837=ORIENTED_EDGE('',*,*,#10640,.T.);
#14838=ORIENTED_EDGE('',*,*,#10641,.T.);
#14839=ORIENTED_EDGE('',*,*,#10638,.F.);
#14840=ORIENTED_EDGE('',*,*,#10103,.F.);
#14841=ORIENTED_EDGE('',*,*,#10642,.T.);
#14842=ORIENTED_EDGE('',*,*,#10643,.T.);
#14843=ORIENTED_EDGE('',*,*,#10640,.F.);
#14844=ORIENTED_EDGE('',*,*,#10102,.F.);
#14845=ORIENTED_EDGE('',*,*,#10644,.T.);
#14846=ORIENTED_EDGE('',*,*,#10645,.T.);
#14847=ORIENTED_EDGE('',*,*,#10642,.F.);
#14848=ORIENTED_EDGE('',*,*,#10101,.F.);
#14849=ORIENTED_EDGE('',*,*,#10621,.T.);
#14850=ORIENTED_EDGE('',*,*,#10646,.T.);
#14851=ORIENTED_EDGE('',*,*,#10644,.F.);
#14852=ORIENTED_EDGE('',*,*,#10646,.F.);
#14853=ORIENTED_EDGE('',*,*,#10620,.F.);
#14854=ORIENTED_EDGE('',*,*,#10623,.F.);
#14855=ORIENTED_EDGE('',*,*,#10625,.F.);
#14856=ORIENTED_EDGE('',*,*,#10627,.F.);
#14857=ORIENTED_EDGE('',*,*,#10629,.F.);
#14858=ORIENTED_EDGE('',*,*,#10631,.F.);
#14859=ORIENTED_EDGE('',*,*,#10633,.F.);
#14860=ORIENTED_EDGE('',*,*,#10635,.F.);
#14861=ORIENTED_EDGE('',*,*,#10637,.F.);
#14862=ORIENTED_EDGE('',*,*,#10639,.F.);
#14863=ORIENTED_EDGE('',*,*,#10641,.F.);
#14864=ORIENTED_EDGE('',*,*,#10643,.F.);
#14865=ORIENTED_EDGE('',*,*,#10645,.F.);
#14866=ORIENTED_EDGE('',*,*,#10204,.F.);
#14867=ORIENTED_EDGE('',*,*,#10647,.T.);
#14868=ORIENTED_EDGE('',*,*,#10309,.T.);
#14869=ORIENTED_EDGE('',*,*,#10308,.T.);
#14870=ORIENTED_EDGE('',*,*,#10648,.T.);
#14871=ORIENTED_EDGE('',*,*,#10099,.T.);
#14872=ORIENTED_EDGE('',*,*,#10648,.F.);
#14873=ORIENTED_EDGE('',*,*,#10310,.T.);
#14874=ORIENTED_EDGE('',*,*,#10647,.F.);
#14875=ORIENTED_EDGE('',*,*,#10185,.F.);
#14876=ORIENTED_EDGE('',*,*,#10095,.T.);
#14877=ORIENTED_EDGE('',*,*,#10091,.F.);
#14878=ORIENTED_EDGE('',*,*,#10087,.T.);
#14879=ORIENTED_EDGE('',*,*,#10083,.F.);
#14880=ORIENTED_EDGE('',*,*,#10201,.F.);
#14881=ORIENTED_EDGE('',*,*,#10194,.F.);
#14882=ORIENTED_EDGE('',*,*,#10191,.F.);
#17296=CYLINDRICAL_SURFACE('',#18962,17.);
#17297=CYLINDRICAL_SURFACE('',#18965,2.65);
#17298=CYLINDRICAL_SURFACE('',#18970,2.65);
#17299=CYLINDRICAL_SURFACE('',#18975,2.65);
#17300=CYLINDRICAL_SURFACE('',#18980,1.);
#17301=CYLINDRICAL_SURFACE('',#19161,5.85);
#17678=ADVANCED_FACE('',(#1650),#403,.T.);
#17679=ADVANCED_FACE('',(#1651,#208),#404,.T.);
#17680=ADVANCED_FACE('',(#1652),#405,.T.);
#17681=ADVANCED_FACE('',(#1653,#209,#210,#211,#212,#213,#214,#215,#216,
#217,#218),#406,.F.);
#17682=ADVANCED_FACE('',(#1654),#906,.T.);
#17683=ADVANCED_FACE('',(#1655),#407,.T.);
#17684=ADVANCED_FACE('',(#1656),#907,.T.);
#17685=ADVANCED_FACE('',(#1657),#408,.T.);
#17686=ADVANCED_FACE('',(#1658),#409,.T.);
#17687=ADVANCED_FACE('',(#1659,#219,#220,#221,#222,#223,#224,#225,#226,
#227,#228),#410,.T.);
#17688=ADVANCED_FACE('',(#1660),#17296,.T.);
#17689=ADVANCED_FACE('',(#1661),#908,.F.);
#17690=ADVANCED_FACE('',(#1662),#17297,.F.);
#17691=ADVANCED_FACE('',(#1663),#909,.F.);
#17692=ADVANCED_FACE('',(#1664),#910,.F.);
#17693=ADVANCED_FACE('',(#1665),#17298,.F.);
#17694=ADVANCED_FACE('',(#1666),#911,.F.);
#17695=ADVANCED_FACE('',(#1667),#912,.F.);
#17696=ADVANCED_FACE('',(#1668),#17299,.F.);
#17697=ADVANCED_FACE('',(#1669),#913,.F.);
#17698=ADVANCED_FACE('',(#1670),#914,.F.);
#17699=ADVANCED_FACE('',(#1671),#17300,.F.);
#17700=ADVANCED_FACE('',(#1672),#411,.F.);
#17701=ADVANCED_FACE('',(#1673),#412,.F.);
#17702=ADVANCED_FACE('',(#1674),#413,.F.);
#17703=ADVANCED_FACE('',(#1675),#414,.F.);
#17704=ADVANCED_FACE('',(#1676),#415,.F.);
#17705=ADVANCED_FACE('',(#1677),#416,.F.);
#17706=ADVANCED_FACE('',(#1678),#417,.F.);
#17707=ADVANCED_FACE('',(#1679),#418,.F.);
#17708=ADVANCED_FACE('',(#1680),#419,.F.);
#17709=ADVANCED_FACE('',(#1681),#420,.F.);
#17710=ADVANCED_FACE('',(#1682),#421,.F.);
#17711=ADVANCED_FACE('',(#1683),#422,.F.);
#17712=ADVANCED_FACE('',(#1684),#423,.F.);
#17713=ADVANCED_FACE('',(#1685),#424,.F.);
#17714=ADVANCED_FACE('',(#1686),#425,.F.);
#17715=ADVANCED_FACE('',(#1687),#426,.F.);
#17716=ADVANCED_FACE('',(#1688),#427,.F.);
#17717=ADVANCED_FACE('',(#1689),#428,.F.);
#17718=ADVANCED_FACE('',(#1690),#429,.F.);
#17719=ADVANCED_FACE('',(#1691),#430,.F.);
#17720=ADVANCED_FACE('',(#1692),#431,.F.);
#17721=ADVANCED_FACE('',(#1693),#432,.F.);
#17722=ADVANCED_FACE('',(#1694),#433,.F.);
#17723=ADVANCED_FACE('',(#1695),#434,.F.);
#17724=ADVANCED_FACE('',(#1696),#435,.F.);
#17725=ADVANCED_FACE('',(#1697),#436,.F.);
#17726=ADVANCED_FACE('',(#1698),#437,.F.);
#17727=ADVANCED_FACE('',(#1699),#438,.F.);
#17728=ADVANCED_FACE('',(#1700),#439,.F.);
#17729=ADVANCED_FACE('',(#1701),#440,.F.);
#17730=ADVANCED_FACE('',(#1702),#441,.F.);
#17731=ADVANCED_FACE('',(#1703),#442,.F.);
#17732=ADVANCED_FACE('',(#1704),#443,.F.);
#17733=ADVANCED_FACE('',(#1705),#444,.F.);
#17734=ADVANCED_FACE('',(#1706),#445,.F.);
#17735=ADVANCED_FACE('',(#1707),#446,.F.);
#17736=ADVANCED_FACE('',(#1708),#447,.F.);
#17737=ADVANCED_FACE('',(#1709),#448,.F.);
#17738=ADVANCED_FACE('',(#1710),#449,.F.);
#17739=ADVANCED_FACE('',(#1711),#450,.F.);
#17740=ADVANCED_FACE('',(#1712),#451,.F.);
#17741=ADVANCED_FACE('',(#1713),#452,.F.);
#17742=ADVANCED_FACE('',(#1714),#453,.F.);
#17743=ADVANCED_FACE('',(#1715),#454,.F.);
#17744=ADVANCED_FACE('',(#1716),#455,.F.);
#17745=ADVANCED_FACE('',(#1717),#456,.F.);
#17746=ADVANCED_FACE('',(#1718),#457,.F.);
#17747=ADVANCED_FACE('',(#1719),#458,.F.);
#17748=ADVANCED_FACE('',(#1720),#459,.F.);
#17749=ADVANCED_FACE('',(#1721),#460,.F.);
#17750=ADVANCED_FACE('',(#1722),#461,.F.);
#17751=ADVANCED_FACE('',(#1723),#462,.F.);
#17752=ADVANCED_FACE('',(#1724),#463,.F.);
#17753=ADVANCED_FACE('',(#1725),#464,.F.);
#17754=ADVANCED_FACE('',(#1726),#465,.F.);
#17755=ADVANCED_FACE('',(#1727),#466,.F.);
#17756=ADVANCED_FACE('',(#1728),#467,.F.);
#17757=ADVANCED_FACE('',(#1729),#468,.F.);
#17758=ADVANCED_FACE('',(#1730),#469,.F.);
#17759=ADVANCED_FACE('',(#1731),#470,.F.);
#17760=ADVANCED_FACE('',(#1732),#471,.F.);
#17761=ADVANCED_FACE('',(#1733),#472,.F.);
#17762=ADVANCED_FACE('',(#1734),#473,.F.);
#17763=ADVANCED_FACE('',(#1735),#474,.F.);
#17764=ADVANCED_FACE('',(#1736),#475,.F.);
#17765=ADVANCED_FACE('',(#1737),#476,.F.);
#17766=ADVANCED_FACE('',(#1738),#477,.F.);
#17767=ADVANCED_FACE('',(#1739),#478,.F.);
#17768=ADVANCED_FACE('',(#1740),#479,.F.);
#17769=ADVANCED_FACE('',(#1741),#480,.F.);
#17770=ADVANCED_FACE('',(#1742),#481,.F.);
#17771=ADVANCED_FACE('',(#1743),#482,.F.);
#17772=ADVANCED_FACE('',(#1744),#483,.F.);
#17773=ADVANCED_FACE('',(#1745),#484,.F.);
#17774=ADVANCED_FACE('',(#1746),#485,.F.);
#17775=ADVANCED_FACE('',(#1747),#486,.F.);
#17776=ADVANCED_FACE('',(#1748),#487,.F.);
#17777=ADVANCED_FACE('',(#1749),#488,.F.);
#17778=ADVANCED_FACE('',(#1750),#489,.F.);
#17779=ADVANCED_FACE('',(#1751),#490,.F.);
#17780=ADVANCED_FACE('',(#1752),#491,.F.);
#17781=ADVANCED_FACE('',(#1753),#492,.F.);
#17782=ADVANCED_FACE('',(#1754),#493,.F.);
#17783=ADVANCED_FACE('',(#1755),#494,.F.);
#17784=ADVANCED_FACE('',(#1756),#495,.F.);
#17785=ADVANCED_FACE('',(#1757),#496,.F.);
#17786=ADVANCED_FACE('',(#1758),#497,.F.);
#17787=ADVANCED_FACE('',(#1759),#498,.F.);
#17788=ADVANCED_FACE('',(#1760),#499,.F.);
#17789=ADVANCED_FACE('',(#1761),#500,.F.);
#17790=ADVANCED_FACE('',(#1762),#501,.F.);
#17791=ADVANCED_FACE('',(#1763),#502,.F.);
#17792=ADVANCED_FACE('',(#1764),#503,.F.);
#17793=ADVANCED_FACE('',(#1765),#504,.F.);
#17794=ADVANCED_FACE('',(#1766),#505,.F.);
#17795=ADVANCED_FACE('',(#1767),#506,.F.);
#17796=ADVANCED_FACE('',(#1768),#507,.F.);
#17797=ADVANCED_FACE('',(#1769),#508,.F.);
#17798=ADVANCED_FACE('',(#1770),#509,.F.);
#17799=ADVANCED_FACE('',(#1771),#510,.F.);
#17800=ADVANCED_FACE('',(#1772),#511,.F.);
#17801=ADVANCED_FACE('',(#1773),#512,.F.);
#17802=ADVANCED_FACE('',(#1774),#513,.F.);
#17803=ADVANCED_FACE('',(#1775),#514,.F.);
#17804=ADVANCED_FACE('',(#1776),#515,.F.);
#17805=ADVANCED_FACE('',(#1777),#516,.F.);
#17806=ADVANCED_FACE('',(#1778),#517,.F.);
#17807=ADVANCED_FACE('',(#1779),#518,.F.);
#17808=ADVANCED_FACE('',(#1780),#519,.F.);
#17809=ADVANCED_FACE('',(#1781),#520,.F.);
#17810=ADVANCED_FACE('',(#1782),#521,.F.);
#17811=ADVANCED_FACE('',(#1783),#522,.F.);
#17812=ADVANCED_FACE('',(#1784),#523,.F.);
#17813=ADVANCED_FACE('',(#1785),#524,.F.);
#17814=ADVANCED_FACE('',(#1786),#525,.F.);
#17815=ADVANCED_FACE('',(#1787),#526,.F.);
#17816=ADVANCED_FACE('',(#1788),#527,.F.);
#17817=ADVANCED_FACE('',(#1789),#528,.F.);
#17818=ADVANCED_FACE('',(#1790),#529,.F.);
#17819=ADVANCED_FACE('',(#1791),#530,.F.);
#17820=ADVANCED_FACE('',(#1792),#531,.F.);
#17821=ADVANCED_FACE('',(#1793),#532,.F.);
#17822=ADVANCED_FACE('',(#1794),#533,.F.);
#17823=ADVANCED_FACE('',(#1795),#534,.F.);
#17824=ADVANCED_FACE('',(#1796),#535,.F.);
#17825=ADVANCED_FACE('',(#1797),#536,.F.);
#17826=ADVANCED_FACE('',(#1798),#537,.F.);
#17827=ADVANCED_FACE('',(#1799),#538,.F.);
#17828=ADVANCED_FACE('',(#1800),#539,.F.);
#17829=ADVANCED_FACE('',(#1801),#540,.F.);
#17830=ADVANCED_FACE('',(#1802),#541,.F.);
#17831=ADVANCED_FACE('',(#1803),#542,.F.);
#17832=ADVANCED_FACE('',(#1804),#543,.F.);
#17833=ADVANCED_FACE('',(#1805),#544,.F.);
#17834=ADVANCED_FACE('',(#1806),#545,.F.);
#17835=ADVANCED_FACE('',(#1807),#546,.F.);
#17836=ADVANCED_FACE('',(#1808),#547,.F.);
#17837=ADVANCED_FACE('',(#1809),#548,.F.);
#17838=ADVANCED_FACE('',(#1810),#549,.F.);
#17839=ADVANCED_FACE('',(#1811),#550,.F.);
#17840=ADVANCED_FACE('',(#1812),#551,.F.);
#17841=ADVANCED_FACE('',(#1813),#552,.F.);
#17842=ADVANCED_FACE('',(#1814),#553,.F.);
#17843=ADVANCED_FACE('',(#1815),#554,.F.);
#17844=ADVANCED_FACE('',(#1816),#555,.F.);
#17845=ADVANCED_FACE('',(#1817),#556,.F.);
#17846=ADVANCED_FACE('',(#1818),#557,.F.);
#17847=ADVANCED_FACE('',(#1819),#558,.F.);
#17848=ADVANCED_FACE('',(#1820),#559,.F.);
#17849=ADVANCED_FACE('',(#1821),#560,.F.);
#17850=ADVANCED_FACE('',(#1822),#561,.F.);
#17851=ADVANCED_FACE('',(#1823),#562,.F.);
#17852=ADVANCED_FACE('',(#1824),#563,.F.);
#17853=ADVANCED_FACE('',(#1825),#564,.F.);
#17854=ADVANCED_FACE('',(#1826),#565,.F.);
#17855=ADVANCED_FACE('',(#1827),#566,.F.);
#17856=ADVANCED_FACE('',(#1828),#567,.F.);
#17857=ADVANCED_FACE('',(#1829),#568,.F.);
#17858=ADVANCED_FACE('',(#1830),#569,.F.);
#17859=ADVANCED_FACE('',(#1831),#570,.F.);
#17860=ADVANCED_FACE('',(#1832),#571,.F.);
#17861=ADVANCED_FACE('',(#1833),#572,.F.);
#17862=ADVANCED_FACE('',(#1834),#573,.F.);
#17863=ADVANCED_FACE('',(#1835),#574,.F.);
#17864=ADVANCED_FACE('',(#1836),#575,.F.);
#17865=ADVANCED_FACE('',(#1837),#576,.F.);
#17866=ADVANCED_FACE('',(#1838),#577,.F.);
#17867=ADVANCED_FACE('',(#1839),#578,.F.);
#17868=ADVANCED_FACE('',(#1840),#579,.F.);
#17869=ADVANCED_FACE('',(#1841),#580,.F.);
#17870=ADVANCED_FACE('',(#1842),#581,.F.);
#17871=ADVANCED_FACE('',(#1843),#582,.F.);
#17872=ADVANCED_FACE('',(#1844),#583,.F.);
#17873=ADVANCED_FACE('',(#1845),#584,.F.);
#17874=ADVANCED_FACE('',(#1846),#585,.F.);
#17875=ADVANCED_FACE('',(#1847),#586,.F.);
#17876=ADVANCED_FACE('',(#1848),#587,.F.);
#17877=ADVANCED_FACE('',(#1849),#588,.F.);
#17878=ADVANCED_FACE('',(#1850),#589,.F.);
#17879=ADVANCED_FACE('',(#1851),#590,.F.);
#17880=ADVANCED_FACE('',(#1852),#17301,.F.);
#17881=ADVANCED_FACE('',(#1853),#591,.T.);
#18300=CLOSED_SHELL('',(#17678,#17679,#17680,#17681,#17682,#17683,#17684,
#17685,#17686,#17687,#17688,#17689,#17690,#17691,#17692,#17693,#17694,#17695,
#17696,#17697,#17698,#17699,#17700,#17701,#17702,#17703,#17704,#17705,#17706,
#17707,#17708,#17709,#17710,#17711,#17712,#17713,#17714,#17715,#17716,#17717,
#17718,#17719,#17720,#17721,#17722,#17723,#17724,#17725,#17726,#17727,#17728,
#17729,#17730,#17731,#17732,#17733,#17734,#17735,#17736,#17737,#17738,#17739,
#17740,#17741,#17742,#17743,#17744,#17745,#17746,#17747,#17748,#17749,#17750,
#17751,#17752,#17753,#17754,#17755,#17756,#17757,#17758,#17759,#17760,#17761,
#17762,#17763,#17764,#17765,#17766,#17767,#17768,#17769,#17770,#17771,#17772,
#17773,#17774,#17775,#17776,#17777,#17778,#17779,#17780,#17781,#17782,#17783,
#17784,#17785,#17786,#17787,#17788,#17789,#17790,#17791,#17792,#17793,#17794,
#17795,#17796,#17797,#17798,#17799,#17800,#17801,#17802,#17803,#17804,#17805,
#17806,#17807,#17808,#17809,#17810,#17811,#17812,#17813,#17814,#17815,#17816,
#17817,#17818,#17819,#17820,#17821,#17822,#17823,#17824,#17825,#17826,#17827,
#17828,#17829,#17830,#17831,#17832,#17833,#17834,#17835,#17836,#17837,#17838,
#17839,#17840,#17841,#17842,#17843,#17844,#17845,#17846,#17847,#17848,#17849,
#17850,#17851,#17852,#17853,#17854,#17855,#17856,#17857,#17858,#17859,#17860,
#17861,#17862,#17863,#17864,#17865,#17866,#17867,#17868,#17869,#17870,#17871,
#17872,#17873,#17874,#17875,#17876,#17877,#17878,#17879,#17880,#17881));
#18938=AXIS2_PLACEMENT_3D('',#43758,#21004,#21005);
#18939=AXIS2_PLACEMENT_3D('',#43759,#21006,#21007);
#18940=AXIS2_PLACEMENT_3D('',#43768,#21012,#21013);
#18941=AXIS2_PLACEMENT_3D('',#43775,#21017,#21018);
#18942=AXIS2_PLACEMENT_3D('',#43776,#21019,#21020);
#18943=AXIS2_PLACEMENT_3D('',#43782,#21024,#21025);
#18944=AXIS2_PLACEMENT_3D('',#43787,#21028,#21029);
#18945=AXIS2_PLACEMENT_3D('',#43789,#21030,#21031);
#18946=AXIS2_PLACEMENT_3D('',#43791,#21032,#21033);
#18947=AXIS2_PLACEMENT_3D('',#43793,#21034,#21035);
#18948=AXIS2_PLACEMENT_3D('',#43963,#21120,#21121);
#18949=AXIS2_PLACEMENT_3D('',#43964,#21122,#21123);
#18950=AXIS2_PLACEMENT_3D('',#43975,#21124,#21125);
#18951=AXIS2_PLACEMENT_3D('',#43984,#21126,#21127);
#18952=AXIS2_PLACEMENT_3D('',#43993,#21130,#21131);
#18953=AXIS2_PLACEMENT_3D('',#43995,#21132,#21133);
#18954=AXIS2_PLACEMENT_3D('',#44001,#21134,#21135);
#18955=AXIS2_PLACEMENT_3D('',#44010,#21136,#21137);
#18956=AXIS2_PLACEMENT_3D('',#44013,#21140,#21141);
#18957=AXIS2_PLACEMENT_3D('',#44015,#21143,#21144);
#18958=AXIS2_PLACEMENT_3D('',#44018,#21146,#21147);
#18959=AXIS2_PLACEMENT_3D('',#44020,#21148,#21149);
#18960=AXIS2_PLACEMENT_3D('',#44022,#21150,#21151);
#18961=AXIS2_PLACEMENT_3D('',#44192,#21236,#21237);
#18962=AXIS2_PLACEMENT_3D('',#44193,#21238,#21239);
#18963=AXIS2_PLACEMENT_3D('',#44194,#21240,#21241);
#18964=AXIS2_PLACEMENT_3D('',#44197,#21243,#21244);
#18965=AXIS2_PLACEMENT_3D('',#44198,#21245,#21246);
#18966=AXIS2_PLACEMENT_3D('',#44201,#21248,#21249);
#18967=AXIS2_PLACEMENT_3D('',#44202,#21250,#21251);
#18968=AXIS2_PLACEMENT_3D('',#44204,#21253,#21254);
#18969=AXIS2_PLACEMENT_3D('',#44207,#21256,#21257);
#18970=AXIS2_PLACEMENT_3D('',#44208,#21258,#21259);
#18971=AXIS2_PLACEMENT_3D('',#44211,#21261,#21262);
#18972=AXIS2_PLACEMENT_3D('',#44212,#21263,#21264);
#18973=AXIS2_PLACEMENT_3D('',#44214,#21266,#21267);
#18974=AXIS2_PLACEMENT_3D('',#44217,#21269,#21270);
#18975=AXIS2_PLACEMENT_3D('',#44218,#21271,#21272);
#18976=AXIS2_PLACEMENT_3D('',#44221,#21274,#21275);
#18977=AXIS2_PLACEMENT_3D('',#44222,#21276,#21277);
#18978=AXIS2_PLACEMENT_3D('',#44224,#21279,#21280);
#18979=AXIS2_PLACEMENT_3D('',#44227,#21282,#21283);
#18980=AXIS2_PLACEMENT_3D('',#44228,#21284,#21285);
#18981=AXIS2_PLACEMENT_3D('',#44271,#21287,#21288);
#18982=AXIS2_PLACEMENT_3D('',#44277,#21292,#21293);
#18983=AXIS2_PLACEMENT_3D('',#44281,#21296,#21297);
#18984=AXIS2_PLACEMENT_3D('',#44285,#21300,#21301);
#18985=AXIS2_PLACEMENT_3D('',#44289,#21304,#21305);
#18986=AXIS2_PLACEMENT_3D('',#44293,#21308,#21309);
#18987=AXIS2_PLACEMENT_3D('',#44297,#21312,#21313);
#18988=AXIS2_PLACEMENT_3D('',#44301,#21316,#21317);
#18989=AXIS2_PLACEMENT_3D('',#44305,#21320,#21321);
#18990=AXIS2_PLACEMENT_3D('',#44309,#21324,#21325);
#18991=AXIS2_PLACEMENT_3D('',#44313,#21328,#21329);
#18992=AXIS2_PLACEMENT_3D('',#44317,#21332,#21333);
#18993=AXIS2_PLACEMENT_3D('',#44321,#21336,#21337);
#18994=AXIS2_PLACEMENT_3D('',#44325,#21340,#21341);
#18995=AXIS2_PLACEMENT_3D('',#44327,#21343,#21344);
#18996=AXIS2_PLACEMENT_3D('',#44328,#21345,#21346);
#18997=AXIS2_PLACEMENT_3D('',#44334,#21350,#21351);
#18998=AXIS2_PLACEMENT_3D('',#44338,#21354,#21355);
#18999=AXIS2_PLACEMENT_3D('',#44342,#21358,#21359);
#19000=AXIS2_PLACEMENT_3D('',#44346,#21362,#21363);
#19001=AXIS2_PLACEMENT_3D('',#44350,#21366,#21367);
#19002=AXIS2_PLACEMENT_3D('',#44354,#21370,#21371);
#19003=AXIS2_PLACEMENT_3D('',#44358,#21374,#21375);
#19004=AXIS2_PLACEMENT_3D('',#44362,#21378,#21379);
#19005=AXIS2_PLACEMENT_3D('',#44366,#21382,#21383);
#19006=AXIS2_PLACEMENT_3D('',#44370,#21386,#21387);
#19007=AXIS2_PLACEMENT_3D('',#44374,#21390,#21391);
#19008=AXIS2_PLACEMENT_3D('',#44378,#21394,#21395);
#19009=AXIS2_PLACEMENT_3D('',#44382,#21398,#21399);
#19010=AXIS2_PLACEMENT_3D('',#44384,#21401,#21402);
#19011=AXIS2_PLACEMENT_3D('',#44385,#21403,#21404);
#19012=AXIS2_PLACEMENT_3D('',#44391,#21408,#21409);
#19013=AXIS2_PLACEMENT_3D('',#44395,#21412,#21413);
#19014=AXIS2_PLACEMENT_3D('',#44399,#21416,#21417);
#19015=AXIS2_PLACEMENT_3D('',#44403,#21420,#21421);
#19016=AXIS2_PLACEMENT_3D('',#44407,#21424,#21425);
#19017=AXIS2_PLACEMENT_3D('',#44411,#21428,#21429);
#19018=AXIS2_PLACEMENT_3D('',#44415,#21432,#21433);
#19019=AXIS2_PLACEMENT_3D('',#44419,#21436,#21437);
#19020=AXIS2_PLACEMENT_3D('',#44423,#21440,#21441);
#19021=AXIS2_PLACEMENT_3D('',#44427,#21444,#21445);
#19022=AXIS2_PLACEMENT_3D('',#44431,#21448,#21449);
#19023=AXIS2_PLACEMENT_3D('',#44435,#21452,#21453);
#19024=AXIS2_PLACEMENT_3D('',#44439,#21456,#21457);
#19025=AXIS2_PLACEMENT_3D('',#44441,#21459,#21460);
#19026=AXIS2_PLACEMENT_3D('',#44442,#21461,#21462);
#19027=AXIS2_PLACEMENT_3D('',#44448,#21466,#21467);
#19028=AXIS2_PLACEMENT_3D('',#44452,#21470,#21471);
#19029=AXIS2_PLACEMENT_3D('',#44456,#21474,#21475);
#19030=AXIS2_PLACEMENT_3D('',#44460,#21478,#21479);
#19031=AXIS2_PLACEMENT_3D('',#44464,#21482,#21483);
#19032=AXIS2_PLACEMENT_3D('',#44468,#21486,#21487);
#19033=AXIS2_PLACEMENT_3D('',#44472,#21490,#21491);
#19034=AXIS2_PLACEMENT_3D('',#44476,#21494,#21495);
#19035=AXIS2_PLACEMENT_3D('',#44480,#21498,#21499);
#19036=AXIS2_PLACEMENT_3D('',#44484,#21502,#21503);
#19037=AXIS2_PLACEMENT_3D('',#44488,#21506,#21507);
#19038=AXIS2_PLACEMENT_3D('',#44492,#21510,#21511);
#19039=AXIS2_PLACEMENT_3D('',#44496,#21514,#21515);
#19040=AXIS2_PLACEMENT_3D('',#44498,#21517,#21518);
#19041=AXIS2_PLACEMENT_3D('',#44499,#21519,#21520);
#19042=AXIS2_PLACEMENT_3D('',#44505,#21524,#21525);
#19043=AXIS2_PLACEMENT_3D('',#44509,#21528,#21529);
#19044=AXIS2_PLACEMENT_3D('',#44513,#21532,#21533);
#19045=AXIS2_PLACEMENT_3D('',#44517,#21536,#21537);
#19046=AXIS2_PLACEMENT_3D('',#44521,#21540,#21541);
#19047=AXIS2_PLACEMENT_3D('',#44525,#21544,#21545);
#19048=AXIS2_PLACEMENT_3D('',#44529,#21548,#21549);
#19049=AXIS2_PLACEMENT_3D('',#44533,#21552,#21553);
#19050=AXIS2_PLACEMENT_3D('',#44537,#21556,#21557);
#19051=AXIS2_PLACEMENT_3D('',#44541,#21560,#21561);
#19052=AXIS2_PLACEMENT_3D('',#44545,#21564,#21565);
#19053=AXIS2_PLACEMENT_3D('',#44549,#21568,#21569);
#19054=AXIS2_PLACEMENT_3D('',#44553,#21572,#21573);
#19055=AXIS2_PLACEMENT_3D('',#44555,#21575,#21576);
#19056=AXIS2_PLACEMENT_3D('',#44556,#21577,#21578);
#19057=AXIS2_PLACEMENT_3D('',#44562,#21582,#21583);
#19058=AXIS2_PLACEMENT_3D('',#44566,#21586,#21587);
#19059=AXIS2_PLACEMENT_3D('',#44570,#21590,#21591);
#19060=AXIS2_PLACEMENT_3D('',#44574,#21594,#21595);
#19061=AXIS2_PLACEMENT_3D('',#44578,#21598,#21599);
#19062=AXIS2_PLACEMENT_3D('',#44582,#21602,#21603);
#19063=AXIS2_PLACEMENT_3D('',#44586,#21606,#21607);
#19064=AXIS2_PLACEMENT_3D('',#44590,#21610,#21611);
#19065=AXIS2_PLACEMENT_3D('',#44594,#21614,#21615);
#19066=AXIS2_PLACEMENT_3D('',#44598,#21618,#21619);
#19067=AXIS2_PLACEMENT_3D('',#44602,#21622,#21623);
#19068=AXIS2_PLACEMENT_3D('',#44606,#21626,#21627);
#19069=AXIS2_PLACEMENT_3D('',#44610,#21630,#21631);
#19070=AXIS2_PLACEMENT_3D('',#44612,#21633,#21634);
#19071=AXIS2_PLACEMENT_3D('',#44613,#21635,#21636);
#19072=AXIS2_PLACEMENT_3D('',#44619,#21640,#21641);
#19073=AXIS2_PLACEMENT_3D('',#44623,#21644,#21645);
#19074=AXIS2_PLACEMENT_3D('',#44627,#21648,#21649);
#19075=AXIS2_PLACEMENT_3D('',#44631,#21652,#21653);
#19076=AXIS2_PLACEMENT_3D('',#44635,#21656,#21657);
#19077=AXIS2_PLACEMENT_3D('',#44639,#21660,#21661);
#19078=AXIS2_PLACEMENT_3D('',#44643,#21664,#21665);
#19079=AXIS2_PLACEMENT_3D('',#44647,#21668,#21669);
#19080=AXIS2_PLACEMENT_3D('',#44651,#21672,#21673);
#19081=AXIS2_PLACEMENT_3D('',#44655,#21676,#21677);
#19082=AXIS2_PLACEMENT_3D('',#44659,#21680,#21681);
#19083=AXIS2_PLACEMENT_3D('',#44663,#21684,#21685);
#19084=AXIS2_PLACEMENT_3D('',#44667,#21688,#21689);
#19085=AXIS2_PLACEMENT_3D('',#44669,#21691,#21692);
#19086=AXIS2_PLACEMENT_3D('',#44670,#21693,#21694);
#19087=AXIS2_PLACEMENT_3D('',#44676,#21698,#21699);
#19088=AXIS2_PLACEMENT_3D('',#44680,#21702,#21703);
#19089=AXIS2_PLACEMENT_3D('',#44684,#21706,#21707);
#19090=AXIS2_PLACEMENT_3D('',#44688,#21710,#21711);
#19091=AXIS2_PLACEMENT_3D('',#44692,#21714,#21715);
#19092=AXIS2_PLACEMENT_3D('',#44696,#21718,#21719);
#19093=AXIS2_PLACEMENT_3D('',#44700,#21722,#21723);
#19094=AXIS2_PLACEMENT_3D('',#44704,#21726,#21727);
#19095=AXIS2_PLACEMENT_3D('',#44708,#21730,#21731);
#19096=AXIS2_PLACEMENT_3D('',#44712,#21734,#21735);
#19097=AXIS2_PLACEMENT_3D('',#44716,#21738,#21739);
#19098=AXIS2_PLACEMENT_3D('',#44720,#21742,#21743);
#19099=AXIS2_PLACEMENT_3D('',#44724,#21746,#21747);
#19100=AXIS2_PLACEMENT_3D('',#44726,#21749,#21750);
#19101=AXIS2_PLACEMENT_3D('',#44727,#21751,#21752);
#19102=AXIS2_PLACEMENT_3D('',#44733,#21756,#21757);
#19103=AXIS2_PLACEMENT_3D('',#44737,#21760,#21761);
#19104=AXIS2_PLACEMENT_3D('',#44741,#21764,#21765);
#19105=AXIS2_PLACEMENT_3D('',#44745,#21768,#21769);
#19106=AXIS2_PLACEMENT_3D('',#44749,#21772,#21773);
#19107=AXIS2_PLACEMENT_3D('',#44753,#21776,#21777);
#19108=AXIS2_PLACEMENT_3D('',#44757,#21780,#21781);
#19109=AXIS2_PLACEMENT_3D('',#44761,#21784,#21785);
#19110=AXIS2_PLACEMENT_3D('',#44765,#21788,#21789);
#19111=AXIS2_PLACEMENT_3D('',#44769,#21792,#21793);
#19112=AXIS2_PLACEMENT_3D('',#44773,#21796,#21797);
#19113=AXIS2_PLACEMENT_3D('',#44777,#21800,#21801);
#19114=AXIS2_PLACEMENT_3D('',#44781,#21804,#21805);
#19115=AXIS2_PLACEMENT_3D('',#44783,#21807,#21808);
#19116=AXIS2_PLACEMENT_3D('',#44784,#21809,#21810);
#19117=AXIS2_PLACEMENT_3D('',#44790,#21814,#21815);
#19118=AXIS2_PLACEMENT_3D('',#44794,#21818,#21819);
#19119=AXIS2_PLACEMENT_3D('',#44798,#21822,#21823);
#19120=AXIS2_PLACEMENT_3D('',#44802,#21826,#21827);
#19121=AXIS2_PLACEMENT_3D('',#44806,#21830,#21831);
#19122=AXIS2_PLACEMENT_3D('',#44810,#21834,#21835);
#19123=AXIS2_PLACEMENT_3D('',#44814,#21838,#21839);
#19124=AXIS2_PLACEMENT_3D('',#44818,#21842,#21843);
#19125=AXIS2_PLACEMENT_3D('',#44822,#21846,#21847);
#19126=AXIS2_PLACEMENT_3D('',#44826,#21850,#21851);
#19127=AXIS2_PLACEMENT_3D('',#44830,#21854,#21855);
#19128=AXIS2_PLACEMENT_3D('',#44834,#21858,#21859);
#19129=AXIS2_PLACEMENT_3D('',#44838,#21862,#21863);
#19130=AXIS2_PLACEMENT_3D('',#44840,#21865,#21866);
#19131=AXIS2_PLACEMENT_3D('',#44841,#21867,#21868);
#19132=AXIS2_PLACEMENT_3D('',#44847,#21872,#21873);
#19133=AXIS2_PLACEMENT_3D('',#44851,#21876,#21877);
#19134=AXIS2_PLACEMENT_3D('',#44855,#21880,#21881);
#19135=AXIS2_PLACEMENT_3D('',#44859,#21884,#21885);
#19136=AXIS2_PLACEMENT_3D('',#44863,#21888,#21889);
#19137=AXIS2_PLACEMENT_3D('',#44867,#21892,#21893);
#19138=AXIS2_PLACEMENT_3D('',#44871,#21896,#21897);
#19139=AXIS2_PLACEMENT_3D('',#44875,#21900,#21901);
#19140=AXIS2_PLACEMENT_3D('',#44879,#21904,#21905);
#19141=AXIS2_PLACEMENT_3D('',#44883,#21908,#21909);
#19142=AXIS2_PLACEMENT_3D('',#44887,#21912,#21913);
#19143=AXIS2_PLACEMENT_3D('',#44891,#21916,#21917);
#19144=AXIS2_PLACEMENT_3D('',#44895,#21920,#21921);
#19145=AXIS2_PLACEMENT_3D('',#44897,#21923,#21924);
#19146=AXIS2_PLACEMENT_3D('',#44898,#21925,#21926);
#19147=AXIS2_PLACEMENT_3D('',#44904,#21930,#21931);
#19148=AXIS2_PLACEMENT_3D('',#44908,#21934,#21935);
#19149=AXIS2_PLACEMENT_3D('',#44912,#21938,#21939);
#19150=AXIS2_PLACEMENT_3D('',#44916,#21942,#21943);
#19151=AXIS2_PLACEMENT_3D('',#44920,#21946,#21947);
#19152=AXIS2_PLACEMENT_3D('',#44924,#21950,#21951);
#19153=AXIS2_PLACEMENT_3D('',#44928,#21954,#21955);
#19154=AXIS2_PLACEMENT_3D('',#44932,#21958,#21959);
#19155=AXIS2_PLACEMENT_3D('',#44936,#21962,#21963);
#19156=AXIS2_PLACEMENT_3D('',#44940,#21966,#21967);
#19157=AXIS2_PLACEMENT_3D('',#44944,#21970,#21971);
#19158=AXIS2_PLACEMENT_3D('',#44948,#21974,#21975);
#19159=AXIS2_PLACEMENT_3D('',#44952,#21978,#21979);
#19160=AXIS2_PLACEMENT_3D('',#44954,#21981,#21982);
#19161=AXIS2_PLACEMENT_3D('',#44955,#21983,#21984);
#19162=AXIS2_PLACEMENT_3D('',#44958,#21987,#21988);
#21004=DIRECTION('axis',(0.,0.,1.));
#21005=DIRECTION('refdir',(1.,0.,0.));
#21006=DIRECTION('center_axis',(0.707106781186548,0.,0.707106781186548));
#21007=DIRECTION('ref_axis',(0.707106781186548,0.,-0.707106781186548));
#21008=DIRECTION('',(0.707106781186548,0.,-0.707106781186548));
#21009=DIRECTION('',(0.,-1.,0.));
#21010=DIRECTION('',(-0.707106781186548,0.,0.707106781186548));
#21011=DIRECTION('',(0.,1.,0.));
#21012=DIRECTION('center_axis',(0.,0.,1.));
#21013=DIRECTION('ref_axis',(0.,-1.,0.));
#21014=DIRECTION('',(1.,0.,0.));
#21015=DIRECTION('',(0.,1.,0.));
#21016=DIRECTION('',(1.,0.,0.));
#21017=DIRECTION('center_axis',(0.,0.,1.));
#21018=DIRECTION('ref_axis',(1.,0.,0.));
#21019=DIRECTION('center_axis',(-0.707106781186548,0.,0.707106781186547));
#21020=DIRECTION('ref_axis',(0.707106781186547,0.,0.707106781186548));
#21021=DIRECTION('',(0.707106781186547,0.,0.707106781186548));
#21022=DIRECTION('',(0.,-1.,0.));
#21023=DIRECTION('',(-0.707106781186547,0.,-0.707106781186548));
#21024=DIRECTION('center_axis',(1.,0.,0.));
#21025=DIRECTION('ref_axis',(0.,0.,-1.));
#21026=DIRECTION('',(0.,0.,1.));
#21027=DIRECTION('',(0.,0.,-1.));
#21028=DIRECTION('center_axis',(1.,0.,0.));
#21029=DIRECTION('ref_axis',(0.,0.,-1.));
#21030=DIRECTION('center_axis',(-1.,0.,0.));
#21031=DIRECTION('ref_axis',(0.,0.,-1.));
#21032=DIRECTION('center_axis',(-1.,0.,0.));
#21033=DIRECTION('ref_axis',(0.,0.,-1.));
#21034=DIRECTION('center_axis',(-1.,0.,0.));
#21035=DIRECTION('ref_axis',(0.,0.,-1.));
#21036=DIRECTION('',(0.,-0.754709580222771,-0.656059028990508));
#21037=DIRECTION('',(0.,0.615661475325658,-0.788010753606722));
#21038=DIRECTION('',(0.,0.754709580222772,0.656059028990508));
#21039=DIRECTION('',(0.,0.681998360062499,0.73135370161917));
#21040=DIRECTION('',(0.,0.601815023152048,0.798635510047293));
#21041=DIRECTION('',(0.,0.515038074910053,0.857167300702113));
#21042=DIRECTION('',(0.,0.422618261740699,0.90630778703665));
#21043=DIRECTION('',(0.,0.325568154457157,0.945518575599317));
#21044=DIRECTION('',(0.,-0.961261695938319,0.275637355816999));
#21045=DIRECTION('',(0.,-0.325568154457155,-0.945518575599317));
#21046=DIRECTION('',(0.,-0.422618261740698,-0.90630778703665));
#21047=DIRECTION('',(0.,-0.515038074910055,-0.857167300702112));
#21048=DIRECTION('',(0.,-0.601815023152048,-0.798635510047293));
#21049=DIRECTION('',(0.,-0.681998360062499,-0.73135370161917));
#21050=DIRECTION('',(0.,-0.190808995376545,0.981627183447664));
#21051=DIRECTION('',(0.,-0.99026806874157,-0.139173100960066));
#21052=DIRECTION('',(0.,0.190808995376543,-0.981627183447664));
#21053=DIRECTION('',(0.,0.292371704722737,-0.956304755963035));
#21054=DIRECTION('',(0.,0.390731128489274,-0.92050485345244));
#21055=DIRECTION('',(0.,0.484809620246337,-0.874619707139396));
#21056=DIRECTION('',(0.,0.573576436351047,-0.819152044288991));
#21057=DIRECTION('',(0.,0.656059028990507,-0.754709580222772));
#21058=DIRECTION('',(0.,0.719339800338651,0.694658370458997));
#21059=DIRECTION('',(0.,-0.656059028990507,0.754709580222772));
#21060=DIRECTION('',(0.,-0.573576436351047,0.819152044288992));
#21061=DIRECTION('',(0.,-0.484809620246337,0.874619707139396));
#21062=DIRECTION('',(0.,-0.390731128489274,0.92050485345244));
#21063=DIRECTION('',(0.,-0.292371704722737,0.956304755963036));
#21064=DIRECTION('',(0.,0.754709580222772,0.656059028990507));
#21065=DIRECTION('',(0.,-0.615661475325659,0.788010753606722));
#21066=DIRECTION('',(0.,-0.754709580222772,-0.656059028990507));
#21067=DIRECTION('',(0.,-0.681998360062498,-0.731353701619171));
#21068=DIRECTION('',(0.,-0.601815023152048,-0.798635510047293));
#21069=DIRECTION('',(0.,-0.515038074910054,-0.857167300702112));
#21070=DIRECTION('',(0.,-0.4226182617407,-0.90630778703665));
#21071=DIRECTION('',(0.,-0.325568154457159,-0.945518575599316));
#21072=DIRECTION('',(0.,0.961261695938319,-0.275637355816999));
#21073=DIRECTION('',(0.,0.325568154457156,0.945518575599317));
#21074=DIRECTION('',(0.,0.422618261740699,0.90630778703665));
#21075=DIRECTION('',(0.,0.515038074910054,0.857167300702112));
#21076=DIRECTION('',(0.,0.601815023152049,0.798635510047292));
#21077=DIRECTION('',(0.,0.681998360062498,0.731353701619171));
#21078=DIRECTION('',(0.,0.945518575599317,-0.325568154457157));
#21079=DIRECTION('',(0.,0.374606593415912,0.927183854566787));
#21080=DIRECTION('',(0.,-0.945518575599316,0.325568154457158));
#21081=DIRECTION('',(0.,-0.974370064785235,0.224951054343866));
#21082=DIRECTION('',(0.,-0.992546151641322,0.121869343405146));
#21083=DIRECTION('',(0.,-0.999847695156391,0.017452406437284));
#21084=DIRECTION('',(0.,-0.996194698091745,-0.0871557427476604));
#21085=DIRECTION('',(0.,-0.981627183447664,-0.190808995376544));
#21086=DIRECTION('',(0.,0.241921895599668,-0.970295726275996));
#21087=DIRECTION('',(0.,0.981627183447664,0.190808995376545));
#21088=DIRECTION('',(0.,0.996194698091746,0.0871557427476587));
#21089=DIRECTION('',(0.,0.999847695156391,-0.0174524064372842));
#21090=DIRECTION('',(0.,0.992546151641322,-0.121869343405146));
#21091=DIRECTION('',(0.,0.974370064785235,-0.224951054343866));
#21092=DIRECTION('',(0.,0.190808995376546,-0.981627183447664));
#21093=DIRECTION('',(0.,0.99026806874157,0.139173100960065));
#21094=DIRECTION('',(0.,-0.190808995376545,0.981627183447664));
#21095=DIRECTION('',(0.,-0.292371704722736,0.956304755963036));
#21096=DIRECTION('',(0.,-0.390731128489274,0.92050485345244));
#21097=DIRECTION('',(0.,-0.484809620246338,0.874619707139396));
#21098=DIRECTION('',(0.,-0.573576436351046,0.819152044288992));
#21099=DIRECTION('',(0.,-0.656059028990507,0.754709580222772));
#21100=DIRECTION('',(0.,-0.719339800338651,-0.694658370458997));
#21101=DIRECTION('',(0.,0.656059028990507,-0.754709580222773));
#21102=DIRECTION('',(0.,0.573576436351045,-0.819152044288992));
#21103=DIRECTION('',(0.,0.484809620246337,-0.874619707139396));
#21104=DIRECTION('',(0.,0.390731128489275,-0.92050485345244));
#21105=DIRECTION('',(0.,0.292371704722736,-0.956304755963036));
#21106=DIRECTION('',(0.,-0.945518575599317,0.325568154457156));
#21107=DIRECTION('',(0.,-0.374606593415912,-0.927183854566787));
#21108=DIRECTION('',(0.,0.945518575599317,-0.325568154457156));
#21109=DIRECTION('',(0.,0.974370064785235,-0.224951054343867));
#21110=DIRECTION('',(0.,0.992546151641322,-0.121869343405148));
#21111=DIRECTION('',(0.,0.999847695156391,-0.017452406437284));
#21112=DIRECTION('',(0.,0.996194698091746,0.087155742747658));
#21113=DIRECTION('',(0.,0.981627183447664,0.190808995376544));
#21114=DIRECTION('',(0.,-0.241921895599667,0.970295726275997));
#21115=DIRECTION('',(0.,-0.981627183447664,-0.190808995376545));
#21116=DIRECTION('',(0.,-0.996194698091746,-0.0871557427476568));
#21117=DIRECTION('',(0.,-0.999847695156391,0.0174524064372842));
#21118=DIRECTION('',(0.,-0.992546151641322,0.121869343405148));
#21119=DIRECTION('',(0.,-0.974370064785235,0.224951054343865));
#21120=DIRECTION('center_axis',(-1.,0.,0.));
#21121=DIRECTION('ref_axis',(0.,0.,-1.));
#21122=DIRECTION('center_axis',(1.,0.,0.));
#21123=DIRECTION('ref_axis',(0.,0.,-1.));
#21124=DIRECTION('center_axis',(-1.,0.,0.));
#21125=DIRECTION('ref_axis',(0.,0.,-1.));
#21126=DIRECTION('center_axis',(0.,-0.591720064565827,0.806143514016092));
#21127=DIRECTION('ref_axis',(1.,0.,0.));
#21128=DIRECTION('',(-1.,0.,0.));
#21129=DIRECTION('',(1.,0.,0.));
#21130=DIRECTION('center_axis',(-1.,0.,0.));
#21131=DIRECTION('ref_axis',(0.,0.,-1.));
#21132=DIRECTION('center_axis',(1.,0.,0.));
#21133=DIRECTION('ref_axis',(0.,0.,-1.));
#21134=DIRECTION('center_axis',(-1.,0.,0.));
#21135=DIRECTION('ref_axis',(0.,0.,-1.));
#21136=DIRECTION('center_axis',(0.,0.591720064565827,0.806143514016092));
#21137=DIRECTION('ref_axis',(1.,0.,0.));
#21138=DIRECTION('',(-1.,0.,0.));
#21139=DIRECTION('',(1.,0.,0.));
#21140=DIRECTION('center_axis',(0.,1.,0.));
#21141=DIRECTION('ref_axis',(0.,0.,1.));
#21142=DIRECTION('',(0.,0.,1.));
#21143=DIRECTION('center_axis',(1.,0.,0.));
#21144=DIRECTION('ref_axis',(0.,0.,-1.));
#21145=DIRECTION('',(0.,0.,-1.));
#21146=DIRECTION('center_axis',(1.,0.,0.));
#21147=DIRECTION('ref_axis',(0.,0.,-1.));
#21148=DIRECTION('center_axis',(1.,0.,0.));
#21149=DIRECTION('ref_axis',(0.,0.,-1.));
#21150=DIRECTION('center_axis',(-1.,0.,0.));
#21151=DIRECTION('ref_axis',(0.,0.,-1.));
#21152=DIRECTION('',(0.,-0.754709580222772,-0.656059028990508));
#21153=DIRECTION('',(0.,-0.615661475325658,0.788010753606722));
#21154=DIRECTION('',(0.,0.754709580222771,0.656059028990508));
#21155=DIRECTION('',(0.,0.681998360062499,0.73135370161917));
#21156=DIRECTION('',(0.,0.601815023152048,0.798635510047293));
#21157=DIRECTION('',(0.,0.515038074910055,0.857167300702112));
#21158=DIRECTION('',(0.,0.422618261740698,0.90630778703665));
#21159=DIRECTION('',(0.,0.325568154457155,0.945518575599317));
#21160=DIRECTION('',(0.,0.961261695938319,-0.275637355816999));
#21161=DIRECTION('',(0.,-0.325568154457157,-0.945518575599317));
#21162=DIRECTION('',(0.,-0.422618261740699,-0.90630778703665));
#21163=DIRECTION('',(0.,-0.515038074910053,-0.857167300702113));
#21164=DIRECTION('',(0.,-0.601815023152048,-0.798635510047293));
#21165=DIRECTION('',(0.,-0.681998360062499,-0.73135370161917));
#21166=DIRECTION('',(0.,-0.190808995376543,0.981627183447664));
#21167=DIRECTION('',(0.,0.99026806874157,0.139173100960066));
#21168=DIRECTION('',(0.,0.190808995376545,-0.981627183447664));
#21169=DIRECTION('',(0.,0.292371704722737,-0.956304755963036));
#21170=DIRECTION('',(0.,0.390731128489274,-0.92050485345244));
#21171=DIRECTION('',(0.,0.484809620246337,-0.874619707139396));
#21172=DIRECTION('',(0.,0.573576436351047,-0.819152044288992));
#21173=DIRECTION('',(0.,0.656059028990507,-0.754709580222772));
#21174=DIRECTION('',(0.,-0.719339800338651,-0.694658370458997));
#21175=DIRECTION('',(0.,-0.656059028990507,0.754709580222772));
#21176=DIRECTION('',(0.,-0.573576436351047,0.819152044288991));
#21177=DIRECTION('',(0.,-0.484809620246337,0.874619707139396));
#21178=DIRECTION('',(0.,-0.390731128489274,0.92050485345244));
#21179=DIRECTION('',(0.,-0.292371704722737,0.956304755963035));
#21180=DIRECTION('',(0.,0.754709580222772,0.656059028990507));
#21181=DIRECTION('',(0.,0.615661475325659,-0.788010753606722));
#21182=DIRECTION('',(0.,-0.754709580222772,-0.656059028990507));
#21183=DIRECTION('',(0.,-0.681998360062498,-0.731353701619171));
#21184=DIRECTION('',(0.,-0.601815023152049,-0.798635510047292));
#21185=DIRECTION('',(0.,-0.515038074910054,-0.857167300702112));
#21186=DIRECTION('',(0.,-0.422618261740699,-0.90630778703665));
#21187=DIRECTION('',(0.,-0.325568154457156,-0.945518575599317));
#21188=DIRECTION('',(0.,-0.961261695938319,0.275637355816999));
#21189=DIRECTION('',(0.,0.325568154457159,0.945518575599316));
#21190=DIRECTION('',(0.,0.4226182617407,0.90630778703665));
#21191=DIRECTION('',(0.,0.515038074910054,0.857167300702112));
#21192=DIRECTION('',(0.,0.601815023152048,0.798635510047293));
#21193=DIRECTION('',(0.,0.681998360062498,0.731353701619171));
#21194=DIRECTION('',(0.,0.945518575599316,-0.325568154457158));
#21195=DIRECTION('',(0.,-0.374606593415912,-0.927183854566787));
#21196=DIRECTION('',(0.,-0.945518575599317,0.325568154457157));
#21197=DIRECTION('',(0.,-0.974370064785235,0.224951054343866));
#21198=DIRECTION('',(0.,-0.992546151641322,0.121869343405146));
#21199=DIRECTION('',(0.,-0.999847695156391,0.0174524064372842));
#21200=DIRECTION('',(0.,-0.996194698091746,-0.0871557427476587));
#21201=DIRECTION('',(0.,-0.981627183447664,-0.190808995376545));
#21202=DIRECTION('',(0.,-0.241921895599668,0.970295726275996));
#21203=DIRECTION('',(0.,0.981627183447664,0.190808995376544));
#21204=DIRECTION('',(0.,0.996194698091745,0.0871557427476604));
#21205=DIRECTION('',(0.,0.999847695156391,-0.017452406437284));
#21206=DIRECTION('',(0.,0.992546151641322,-0.121869343405146));
#21207=DIRECTION('',(0.,0.974370064785235,-0.224951054343866));
#21208=DIRECTION('',(0.,0.190808995376545,-0.981627183447664));
#21209=DIRECTION('',(0.,-0.99026806874157,-0.139173100960065));
#21210=DIRECTION('',(0.,-0.190808995376546,0.981627183447664));
#21211=DIRECTION('',(0.,-0.292371704722736,0.956304755963036));
#21212=DIRECTION('',(0.,-0.390731128489275,0.92050485345244));
#21213=DIRECTION('',(0.,-0.484809620246337,0.874619707139396));
#21214=DIRECTION('',(0.,-0.573576436351045,0.819152044288992));
#21215=DIRECTION('',(0.,-0.656059028990507,0.754709580222773));
#21216=DIRECTION('',(0.,0.719339800338651,0.694658370458997));
#21217=DIRECTION('',(0.,0.656059028990507,-0.754709580222772));
#21218=DIRECTION('',(0.,0.573576436351046,-0.819152044288992));
#21219=DIRECTION('',(0.,0.484809620246338,-0.874619707139396));
#21220=DIRECTION('',(0.,0.390731128489274,-0.92050485345244));
#21221=DIRECTION('',(0.,0.292371704722736,-0.956304755963036));
#21222=DIRECTION('',(0.,-0.945518575599317,0.325568154457156));
#21223=DIRECTION('',(0.,0.374606593415912,0.927183854566787));
#21224=DIRECTION('',(0.,0.945518575599317,-0.325568154457156));
#21225=DIRECTION('',(0.,0.974370064785235,-0.224951054343865));
#21226=DIRECTION('',(0.,0.992546151641322,-0.121869343405148));
#21227=DIRECTION('',(0.,0.999847695156391,-0.0174524064372842));
#21228=DIRECTION('',(0.,0.996194698091746,0.0871557427476568));
#21229=DIRECTION('',(0.,0.981627183447664,0.190808995376545));
#21230=DIRECTION('',(0.,0.241921895599667,-0.970295726275997));
#21231=DIRECTION('',(0.,-0.981627183447664,-0.190808995376544));
#21232=DIRECTION('',(0.,-0.996194698091746,-0.087155742747658));
#21233=DIRECTION('',(0.,-0.999847695156391,0.017452406437284));
#21234=DIRECTION('',(0.,-0.992546151641322,0.121869343405148));
#21235=DIRECTION('',(0.,-0.974370064785235,0.224951054343867));
#21236=DIRECTION('center_axis',(1.,0.,0.));
#21237=DIRECTION('ref_axis',(0.,0.,-1.));
#21238=DIRECTION('center_axis',(1.,0.,0.));
#21239=DIRECTION('ref_axis',(0.,0.,-1.));
#21240=DIRECTION('center_axis',(-1.,0.,0.));
#21241=DIRECTION('ref_axis',(0.,0.,-1.));
#21242=DIRECTION('',(0.707106781186547,-8.65956056235494E-17,-0.707106781186548));
#21243=DIRECTION('center_axis',(1.,0.,0.));
#21244=DIRECTION('ref_axis',(0.,0.,-1.));
#21245=DIRECTION('center_axis',(1.,0.,0.));
#21246=DIRECTION('ref_axis',(0.,0.,-1.));
#21247=DIRECTION('',(1.,0.,0.));
#21248=DIRECTION('center_axis',(-1.,0.,0.));
#21249=DIRECTION('ref_axis',(0.,0.,-1.));
#21250=DIRECTION('center_axis',(1.,0.,0.));
#21251=DIRECTION('ref_axis',(0.,0.,-1.));
#21252=DIRECTION('',(-0.707106781186548,8.65956056235493E-17,-0.707106781186548));
#21253=DIRECTION('center_axis',(-1.,0.,0.));
#21254=DIRECTION('ref_axis',(0.,0.,-1.));
#21255=DIRECTION('',(0.707106781186547,-8.65956056235494E-17,-0.707106781186548));
#21256=DIRECTION('center_axis',(1.,0.,0.));
#21257=DIRECTION('ref_axis',(0.,0.,-1.));
#21258=DIRECTION('center_axis',(1.,0.,0.));
#21259=DIRECTION('ref_axis',(0.,0.,-1.));
#21260=DIRECTION('',(1.,0.,0.));
#21261=DIRECTION('center_axis',(-1.,0.,0.));
#21262=DIRECTION('ref_axis',(0.,0.,-1.));
#21263=DIRECTION('center_axis',(1.,0.,0.));
#21264=DIRECTION('ref_axis',(0.,0.,-1.));
#21265=DIRECTION('',(-0.707106781186548,8.65956056235493E-17,-0.707106781186548));
#21266=DIRECTION('center_axis',(-1.,0.,0.));
#21267=DIRECTION('ref_axis',(0.,0.,-1.));
#21268=DIRECTION('',(0.707106781186547,-8.65956056235494E-17,-0.707106781186548));
#21269=DIRECTION('center_axis',(1.,0.,0.));
#21270=DIRECTION('ref_axis',(0.,0.,-1.));
#21271=DIRECTION('center_axis',(1.,0.,0.));
#21272=DIRECTION('ref_axis',(0.,0.,-1.));
#21273=DIRECTION('',(1.,0.,0.));
#21274=DIRECTION('center_axis',(-1.,0.,0.));
#21275=DIRECTION('ref_axis',(0.,0.,-1.));
#21276=DIRECTION('center_axis',(1.,0.,0.));
#21277=DIRECTION('ref_axis',(0.,0.,-1.));
#21278=DIRECTION('',(-0.707106781186548,8.65956056235493E-17,-0.707106781186548));
#21279=DIRECTION('center_axis',(0.,0.,1.));
#21280=DIRECTION('ref_axis',(1.,0.,0.));
#21281=DIRECTION('',(0.707106781186548,8.65956056235494E-17,-0.707106781186548));
#21282=DIRECTION('center_axis',(0.,0.,-1.));
#21283=DIRECTION('ref_axis',(1.,0.,0.));
#21284=DIRECTION('center_axis',(0.,0.,-1.));
#21285=DIRECTION('ref_axis',(1.,0.,0.));
#21286=DIRECTION('',(0.,0.,-1.));
#21287=DIRECTION('center_axis',(0.,-0.325568154457156,-0.945518575599317));
#21288=DIRECTION('ref_axis',(0.,-0.945518575599317,0.325568154457156));
#21289=DIRECTION('',(-1.,0.,0.));
#21290=DIRECTION('',(0.,-0.945518575599317,0.325568154457156));
#21291=DIRECTION('',(-1.,0.,0.));
#21292=DIRECTION('center_axis',(0.,-0.224951054343867,-0.974370064785235));
#21293=DIRECTION('ref_axis',(0.,-0.974370064785235,0.224951054343867));
#21294=DIRECTION('',(-1.,0.,0.));
#21295=DIRECTION('',(0.,-0.974370064785235,0.224951054343867));
#21296=DIRECTION('center_axis',(0.,-0.121869343405148,-0.992546151641322));
#21297=DIRECTION('ref_axis',(0.,-0.992546151641322,0.121869343405148));
#21298=DIRECTION('',(-1.,0.,0.));
#21299=DIRECTION('',(0.,-0.992546151641322,0.121869343405148));
#21300=DIRECTION('center_axis',(0.,-0.017452406437284,-0.999847695156391));
#21301=DIRECTION('ref_axis',(0.,-0.999847695156391,0.017452406437284));
#21302=DIRECTION('',(-1.,0.,0.));
#21303=DIRECTION('',(0.,-0.999847695156391,0.017452406437284));
#21304=DIRECTION('center_axis',(0.,0.087155742747658,-0.996194698091746));
#21305=DIRECTION('ref_axis',(0.,-0.996194698091746,-0.087155742747658));
#21306=DIRECTION('',(-1.,0.,0.));
#21307=DIRECTION('',(0.,-0.996194698091746,-0.087155742747658));
#21308=DIRECTION('center_axis',(0.,0.190808995376544,-0.981627183447664));
#21309=DIRECTION('ref_axis',(0.,-0.981627183447664,-0.190808995376544));
#21310=DIRECTION('',(-1.,0.,0.));
#21311=DIRECTION('',(0.,-0.981627183447664,-0.190808995376544));
#21312=DIRECTION('center_axis',(0.,0.970295726275997,0.241921895599667));
#21313=DIRECTION('ref_axis',(0.,0.241921895599667,-0.970295726275997));
#21314=DIRECTION('',(-1.,0.,0.));
#21315=DIRECTION('',(0.,0.241921895599667,-0.970295726275997));
#21316=DIRECTION('center_axis',(0.,-0.190808995376545,0.981627183447664));
#21317=DIRECTION('ref_axis',(0.,0.981627183447664,0.190808995376545));
#21318=DIRECTION('',(-1.,0.,0.));
#21319=DIRECTION('',(0.,0.981627183447664,0.190808995376545));
#21320=DIRECTION('center_axis',(0.,-0.0871557427476568,0.996194698091746));
#21321=DIRECTION('ref_axis',(0.,0.996194698091746,0.0871557427476568));
#21322=DIRECTION('',(-1.,0.,0.));
#21323=DIRECTION('',(0.,0.996194698091746,0.0871557427476568));
#21324=DIRECTION('center_axis',(0.,0.0174524064372842,0.999847695156391));
#21325=DIRECTION('ref_axis',(0.,0.999847695156391,-0.0174524064372842));
#21326=DIRECTION('',(-1.,0.,0.));
#21327=DIRECTION('',(0.,0.999847695156391,-0.0174524064372842));
#21328=DIRECTION('center_axis',(0.,0.121869343405148,0.992546151641322));
#21329=DIRECTION('ref_axis',(0.,0.992546151641322,-0.121869343405148));
#21330=DIRECTION('',(-1.,0.,0.));
#21331=DIRECTION('',(0.,0.992546151641322,-0.121869343405148));
#21332=DIRECTION('center_axis',(0.,0.224951054343865,0.974370064785235));
#21333=DIRECTION('ref_axis',(0.,0.974370064785235,-0.224951054343865));
#21334=DIRECTION('',(-1.,0.,0.));
#21335=DIRECTION('',(0.,0.974370064785235,-0.224951054343865));
#21336=DIRECTION('center_axis',(0.,0.325568154457156,0.945518575599317));
#21337=DIRECTION('ref_axis',(0.,0.945518575599317,-0.325568154457156));
#21338=DIRECTION('',(-1.,0.,0.));
#21339=DIRECTION('',(0.,0.945518575599317,-0.325568154457156));
#21340=DIRECTION('center_axis',(0.,-0.927183854566787,0.374606593415912));
#21341=DIRECTION('ref_axis',(0.,0.374606593415912,0.927183854566787));
#21342=DIRECTION('',(0.,0.374606593415912,0.927183854566787));
#21343=DIRECTION('center_axis',(-1.,0.,0.));
#21344=DIRECTION('ref_axis',(0.,0.,1.));
#21345=DIRECTION('center_axis',(0.,0.981627183447664,0.190808995376545));
#21346=DIRECTION('ref_axis',(0.,0.190808995376545,-0.981627183447664));
#21347=DIRECTION('',(-1.,0.,0.));
#21348=DIRECTION('',(0.,0.190808995376545,-0.981627183447664));
#21349=DIRECTION('',(-1.,0.,0.));
#21350=DIRECTION('center_axis',(0.,0.956304755963036,0.292371704722736));
#21351=DIRECTION('ref_axis',(0.,0.292371704722736,-0.956304755963036));
#21352=DIRECTION('',(-1.,0.,0.));
#21353=DIRECTION('',(0.,0.292371704722736,-0.956304755963036));
#21354=DIRECTION('center_axis',(0.,0.92050485345244,0.390731128489274));
#21355=DIRECTION('ref_axis',(0.,0.390731128489274,-0.92050485345244));
#21356=DIRECTION('',(-1.,0.,0.));
#21357=DIRECTION('',(0.,0.390731128489274,-0.92050485345244));
#21358=DIRECTION('center_axis',(0.,0.874619707139396,0.484809620246338));
#21359=DIRECTION('ref_axis',(0.,0.484809620246338,-0.874619707139396));
#21360=DIRECTION('',(-1.,0.,0.));
#21361=DIRECTION('',(0.,0.484809620246338,-0.874619707139396));
#21362=DIRECTION('center_axis',(0.,0.819152044288992,0.573576436351046));
#21363=DIRECTION('ref_axis',(0.,0.573576436351046,-0.819152044288992));
#21364=DIRECTION('',(-1.,0.,0.));
#21365=DIRECTION('',(0.,0.573576436351046,-0.819152044288992));
#21366=DIRECTION('center_axis',(0.,0.754709580222772,0.656059028990507));
#21367=DIRECTION('ref_axis',(0.,0.656059028990507,-0.754709580222772));
#21368=DIRECTION('',(-1.,0.,0.));
#21369=DIRECTION('',(0.,0.656059028990507,-0.754709580222772));
#21370=DIRECTION('center_axis',(0.,-0.694658370458997,0.719339800338651));
#21371=DIRECTION('ref_axis',(0.,0.719339800338651,0.694658370458997));
#21372=DIRECTION('',(-1.,0.,0.));
#21373=DIRECTION('',(0.,0.719339800338651,0.694658370458997));
#21374=DIRECTION('center_axis',(0.,-0.754709580222773,-0.656059028990507));
#21375=DIRECTION('ref_axis',(0.,-0.656059028990507,0.754709580222773));
#21376=DIRECTION('',(-1.,0.,0.));
#21377=DIRECTION('',(0.,-0.656059028990507,0.754709580222773));
#21378=DIRECTION('center_axis',(0.,-0.819152044288992,-0.573576436351045));
#21379=DIRECTION('ref_axis',(0.,-0.573576436351045,0.819152044288992));
#21380=DIRECTION('',(-1.,0.,0.));
#21381=DIRECTION('',(0.,-0.573576436351045,0.819152044288992));
#21382=DIRECTION('center_axis',(0.,-0.874619707139396,-0.484809620246337));
#21383=DIRECTION('ref_axis',(0.,-0.484809620246337,0.874619707139396));
#21384=DIRECTION('',(-1.,0.,0.));
#21385=DIRECTION('',(0.,-0.484809620246338,0.874619707139396));
#21386=DIRECTION('center_axis',(0.,-0.92050485345244,-0.390731128489275));
#21387=DIRECTION('ref_axis',(0.,-0.390731128489275,0.92050485345244));
#21388=DIRECTION('',(-1.,0.,0.));
#21389=DIRECTION('',(0.,-0.390731128489275,0.92050485345244));
#21390=DIRECTION('center_axis',(0.,-0.956304755963036,-0.292371704722736));
#21391=DIRECTION('ref_axis',(0.,-0.292371704722736,0.956304755963036));
#21392=DIRECTION('',(-1.,0.,0.));
#21393=DIRECTION('',(0.,-0.292371704722736,0.956304755963036));
#21394=DIRECTION('center_axis',(0.,-0.981627183447664,-0.190808995376546));
#21395=DIRECTION('ref_axis',(0.,-0.190808995376546,0.981627183447664));
#21396=DIRECTION('',(-1.,0.,0.));
#21397=DIRECTION('',(0.,-0.190808995376546,0.981627183447664));
#21398=DIRECTION('center_axis',(0.,0.139173100960065,-0.99026806874157));
#21399=DIRECTION('ref_axis',(0.,-0.99026806874157,-0.139173100960065));
#21400=DIRECTION('',(0.,-0.99026806874157,-0.139173100960065));
#21401=DIRECTION('center_axis',(-1.,0.,0.));
#21402=DIRECTION('ref_axis',(0.,0.,1.));
#21403=DIRECTION('center_axis',(0.,0.325568154457158,0.945518575599316));
#21404=DIRECTION('ref_axis',(0.,0.945518575599316,-0.325568154457158));
#21405=DIRECTION('',(-1.,0.,0.));
#21406=DIRECTION('',(0.,0.945518575599316,-0.325568154457158));
#21407=DIRECTION('',(-1.,0.,0.));
#21408=DIRECTION('center_axis',(0.,0.224951054343866,0.974370064785235));
#21409=DIRECTION('ref_axis',(0.,0.974370064785235,-0.224951054343866));
#21410=DIRECTION('',(-1.,0.,0.));
#21411=DIRECTION('',(0.,0.974370064785235,-0.224951054343866));
#21412=DIRECTION('center_axis',(0.,0.121869343405146,0.992546151641322));
#21413=DIRECTION('ref_axis',(0.,0.992546151641322,-0.121869343405146));
#21414=DIRECTION('',(-1.,0.,0.));
#21415=DIRECTION('',(0.,0.992546151641322,-0.121869343405145));
#21416=DIRECTION('center_axis',(0.,0.017452406437284,0.999847695156391));
#21417=DIRECTION('ref_axis',(0.,0.999847695156391,-0.017452406437284));
#21418=DIRECTION('',(-1.,0.,0.));
#21419=DIRECTION('',(0.,0.999847695156391,-0.017452406437284));
#21420=DIRECTION('center_axis',(0.,-0.0871557427476604,0.996194698091745));
#21421=DIRECTION('ref_axis',(0.,0.996194698091745,0.0871557427476604));
#21422=DIRECTION('',(-1.,0.,0.));
#21423=DIRECTION('',(0.,0.996194698091745,0.0871557427476604));
#21424=DIRECTION('center_axis',(0.,-0.190808995376544,0.981627183447664));
#21425=DIRECTION('ref_axis',(0.,0.981627183447664,0.190808995376544));
#21426=DIRECTION('',(-1.,0.,0.));
#21427=DIRECTION('',(0.,0.981627183447664,0.190808995376544));
#21428=DIRECTION('center_axis',(0.,-0.970295726275996,-0.241921895599668));
#21429=DIRECTION('ref_axis',(0.,-0.241921895599668,0.970295726275996));
#21430=DIRECTION('',(-1.,0.,0.));
#21431=DIRECTION('',(0.,-0.241921895599668,0.970295726275996));
#21432=DIRECTION('center_axis',(0.,0.190808995376545,-0.981627183447664));
#21433=DIRECTION('ref_axis',(0.,-0.981627183447664,-0.190808995376545));
#21434=DIRECTION('',(-1.,0.,0.));
#21435=DIRECTION('',(0.,-0.981627183447664,-0.190808995376545));
#21436=DIRECTION('center_axis',(0.,0.0871557427476587,-0.996194698091746));
#21437=DIRECTION('ref_axis',(0.,-0.996194698091746,-0.0871557427476587));
#21438=DIRECTION('',(-1.,0.,0.));
#21439=DIRECTION('',(0.,-0.996194698091746,-0.0871557427476587));
#21440=DIRECTION('center_axis',(0.,-0.0174524064372842,-0.999847695156391));
#21441=DIRECTION('ref_axis',(0.,-0.999847695156391,0.0174524064372842));
#21442=DIRECTION('',(-1.,0.,0.));
#21443=DIRECTION('',(0.,-0.999847695156391,0.0174524064372842));
#21444=DIRECTION('center_axis',(0.,-0.121869343405146,-0.992546151641322));
#21445=DIRECTION('ref_axis',(0.,-0.992546151641322,0.121869343405146));
#21446=DIRECTION('',(-1.,0.,0.));
#21447=DIRECTION('',(0.,-0.992546151641322,0.121869343405146));
#21448=DIRECTION('center_axis',(0.,-0.224951054343866,-0.974370064785235));
#21449=DIRECTION('ref_axis',(0.,-0.974370064785235,0.224951054343866));
#21450=DIRECTION('',(-1.,0.,0.));
#21451=DIRECTION('',(0.,-0.974370064785235,0.224951054343866));
#21452=DIRECTION('center_axis',(0.,-0.325568154457157,-0.945518575599317));
#21453=DIRECTION('ref_axis',(0.,-0.945518575599317,0.325568154457157));
#21454=DIRECTION('',(-1.,0.,0.));
#21455=DIRECTION('',(0.,-0.945518575599317,0.325568154457157));
#21456=DIRECTION('center_axis',(0.,0.927183854566787,-0.374606593415912));
#21457=DIRECTION('ref_axis',(0.,-0.374606593415912,-0.927183854566787));
#21458=DIRECTION('',(0.,-0.374606593415912,-0.927183854566787));
#21459=DIRECTION('center_axis',(-1.,0.,0.));
#21460=DIRECTION('ref_axis',(0.,0.,1.));
#21461=DIRECTION('center_axis',(0.,-0.656059028990507,0.754709580222772));
#21462=DIRECTION('ref_axis',(0.,0.754709580222772,0.656059028990507));
#21463=DIRECTION('',(-1.,0.,0.));
#21464=DIRECTION('',(0.,0.754709580222772,0.656059028990507));
#21465=DIRECTION('',(-1.,0.,0.));
#21466=DIRECTION('center_axis',(0.,-0.731353701619171,0.681998360062498));
#21467=DIRECTION('ref_axis',(0.,0.681998360062498,0.731353701619171));
#21468=DIRECTION('',(-1.,0.,0.));
#21469=DIRECTION('',(0.,0.681998360062498,0.731353701619171));
#21470=DIRECTION('center_axis',(0.,-0.798635510047293,0.601815023152048));
#21471=DIRECTION('ref_axis',(0.,0.601815023152048,0.798635510047293));
#21472=DIRECTION('',(-1.,0.,0.));
#21473=DIRECTION('',(0.,0.601815023152048,0.798635510047293));
#21474=DIRECTION('center_axis',(0.,-0.857167300702112,0.515038074910054));
#21475=DIRECTION('ref_axis',(0.,0.515038074910054,0.857167300702112));
#21476=DIRECTION('',(-1.,0.,0.));
#21477=DIRECTION('',(0.,0.515038074910054,0.857167300702112));
#21478=DIRECTION('center_axis',(0.,-0.90630778703665,0.4226182617407));
#21479=DIRECTION('ref_axis',(0.,0.4226182617407,0.90630778703665));
#21480=DIRECTION('',(-1.,0.,0.));
#21481=DIRECTION('',(0.,0.4226182617407,0.90630778703665));
#21482=DIRECTION('center_axis',(0.,-0.945518575599316,0.325568154457159));
#21483=DIRECTION('ref_axis',(0.,0.325568154457159,0.945518575599316));
#21484=DIRECTION('',(-1.,0.,0.));
#21485=DIRECTION('',(0.,0.325568154457159,0.945518575599316));
#21486=DIRECTION('center_axis',(0.,-0.275637355816999,-0.961261695938319));
#21487=DIRECTION('ref_axis',(0.,-0.961261695938319,0.275637355816999));
#21488=DIRECTION('',(-1.,0.,0.));
#21489=DIRECTION('',(0.,-0.961261695938319,0.275637355816999));
#21490=DIRECTION('center_axis',(0.,0.945518575599317,-0.325568154457157));
#21491=DIRECTION('ref_axis',(0.,-0.325568154457156,-0.945518575599317));
#21492=DIRECTION('',(-1.,0.,0.));
#21493=DIRECTION('',(0.,-0.325568154457156,-0.945518575599317));
#21494=DIRECTION('center_axis',(0.,0.90630778703665,-0.422618261740699));
#21495=DIRECTION('ref_axis',(0.,-0.422618261740699,-0.90630778703665));
#21496=DIRECTION('',(-1.,0.,0.));
#21497=DIRECTION('',(0.,-0.422618261740699,-0.90630778703665));
#21498=DIRECTION('center_axis',(0.,0.857167300702112,-0.515038074910054));
#21499=DIRECTION('ref_axis',(0.,-0.515038074910054,-0.857167300702112));
#21500=DIRECTION('',(-1.,0.,0.));
#21501=DIRECTION('',(0.,-0.515038074910054,-0.857167300702112));
#21502=DIRECTION('center_axis',(0.,0.798635510047292,-0.601815023152049));
#21503=DIRECTION('ref_axis',(0.,-0.601815023152049,-0.798635510047292));
#21504=DIRECTION('',(-1.,0.,0.));
#21505=DIRECTION('',(0.,-0.601815023152049,-0.798635510047292));
#21506=DIRECTION('center_axis',(0.,0.731353701619171,-0.681998360062498));
#21507=DIRECTION('ref_axis',(0.,-0.681998360062498,-0.731353701619171));
#21508=DIRECTION('',(-1.,0.,0.));
#21509=DIRECTION('',(0.,-0.681998360062498,-0.731353701619171));
#21510=DIRECTION('center_axis',(0.,0.656059028990507,-0.754709580222772));
#21511=DIRECTION('ref_axis',(0.,-0.754709580222772,-0.656059028990507));
#21512=DIRECTION('',(-1.,0.,0.));
#21513=DIRECTION('',(0.,-0.754709580222772,-0.656059028990507));
#21514=DIRECTION('center_axis',(0.,0.788010753606722,0.615661475325659));
#21515=DIRECTION('ref_axis',(0.,0.615661475325659,-0.788010753606722));
#21516=DIRECTION('',(0.,0.615661475325659,-0.788010753606722));
#21517=DIRECTION('center_axis',(-1.,0.,0.));
#21518=DIRECTION('ref_axis',(0.,0.,1.));
#21519=DIRECTION('center_axis',(0.,-0.981627183447664,-0.190808995376543));
#21520=DIRECTION('ref_axis',(0.,-0.190808995376543,0.981627183447664));
#21521=DIRECTION('',(-1.,0.,0.));
#21522=DIRECTION('',(0.,-0.190808995376543,0.981627183447664));
#21523=DIRECTION('',(-1.,0.,0.));
#21524=DIRECTION('center_axis',(0.,-0.956304755963035,-0.292371704722737));
#21525=DIRECTION('ref_axis',(0.,-0.292371704722737,0.956304755963035));
#21526=DIRECTION('',(-1.,0.,0.));
#21527=DIRECTION('',(0.,-0.292371704722737,0.956304755963035));
#21528=DIRECTION('center_axis',(0.,-0.92050485345244,-0.390731128489274));
#21529=DIRECTION('ref_axis',(0.,-0.390731128489274,0.92050485345244));
#21530=DIRECTION('',(-1.,0.,0.));
#21531=DIRECTION('',(0.,-0.390731128489274,0.92050485345244));
#21532=DIRECTION('center_axis',(0.,-0.874619707139396,-0.484809620246337));
#21533=DIRECTION('ref_axis',(0.,-0.484809620246337,0.874619707139396));
#21534=DIRECTION('',(-1.,0.,0.));
#21535=DIRECTION('',(0.,-0.484809620246337,0.874619707139396));
#21536=DIRECTION('center_axis',(0.,-0.819152044288991,-0.573576436351047));
#21537=DIRECTION('ref_axis',(0.,-0.573576436351047,0.819152044288991));
#21538=DIRECTION('',(-1.,0.,0.));
#21539=DIRECTION('',(0.,-0.573576436351047,0.819152044288991));
#21540=DIRECTION('center_axis',(0.,-0.754709580222772,-0.656059028990507));
#21541=DIRECTION('ref_axis',(0.,-0.656059028990507,0.754709580222772));
#21542=DIRECTION('',(-1.,0.,0.));
#21543=DIRECTION('',(0.,-0.656059028990507,0.754709580222772));
#21544=DIRECTION('center_axis',(0.,0.694658370458997,-0.719339800338651));
#21545=DIRECTION('ref_axis',(0.,-0.719339800338651,-0.694658370458997));
#21546=DIRECTION('',(-1.,0.,0.));
#21547=DIRECTION('',(0.,-0.719339800338651,-0.694658370458997));
#21548=DIRECTION('center_axis',(0.,0.754709580222772,0.656059028990507));
#21549=DIRECTION('ref_axis',(0.,0.656059028990507,-0.754709580222772));
#21550=DIRECTION('',(-1.,0.,0.));
#21551=DIRECTION('',(0.,0.656059028990507,-0.754709580222772));
#21552=DIRECTION('center_axis',(0.,0.819152044288992,0.573576436351047));
#21553=DIRECTION('ref_axis',(0.,0.573576436351047,-0.819152044288992));
#21554=DIRECTION('',(-1.,0.,0.));
#21555=DIRECTION('',(0.,0.573576436351047,-0.819152044288992));
#21556=DIRECTION('center_axis',(0.,0.874619707139396,0.484809620246337));
#21557=DIRECTION('ref_axis',(0.,0.484809620246337,-0.874619707139396));
#21558=DIRECTION('',(-1.,0.,0.));
#21559=DIRECTION('',(0.,0.484809620246337,-0.874619707139396));
#21560=DIRECTION('center_axis',(0.,0.92050485345244,0.390731128489274));
#21561=DIRECTION('ref_axis',(0.,0.390731128489274,-0.92050485345244));
#21562=DIRECTION('',(-1.,0.,0.));
#21563=DIRECTION('',(0.,0.390731128489274,-0.92050485345244));
#21564=DIRECTION('center_axis',(0.,0.956304755963036,0.292371704722737));
#21565=DIRECTION('ref_axis',(0.,0.292371704722737,-0.956304755963036));
#21566=DIRECTION('',(-1.,0.,0.));
#21567=DIRECTION('',(0.,0.292371704722737,-0.956304755963036));
#21568=DIRECTION('center_axis',(0.,0.981627183447664,0.190808995376545));
#21569=DIRECTION('ref_axis',(0.,0.190808995376545,-0.981627183447664));
#21570=DIRECTION('',(-1.,0.,0.));
#21571=DIRECTION('',(0.,0.190808995376545,-0.981627183447664));
#21572=DIRECTION('center_axis',(0.,-0.139173100960066,0.99026806874157));
#21573=DIRECTION('ref_axis',(0.,0.99026806874157,0.139173100960066));
#21574=DIRECTION('',(0.,0.99026806874157,0.139173100960066));
#21575=DIRECTION('center_axis',(-1.,0.,0.));
#21576=DIRECTION('ref_axis',(0.,0.,1.));
#21577=DIRECTION('center_axis',(0.,0.656059028990508,-0.754709580222772));
#21578=DIRECTION('ref_axis',(0.,-0.754709580222772,-0.656059028990508));
#21579=DIRECTION('',(-1.,0.,0.));
#21580=DIRECTION('',(0.,-0.754709580222772,-0.656059028990508));
#21581=DIRECTION('',(-1.,0.,0.));
#21582=DIRECTION('center_axis',(0.,0.73135370161917,-0.681998360062499));
#21583=DIRECTION('ref_axis',(0.,-0.681998360062499,-0.73135370161917));
#21584=DIRECTION('',(-1.,0.,0.));
#21585=DIRECTION('',(0.,-0.681998360062499,-0.73135370161917));
#21586=DIRECTION('center_axis',(0.,0.798635510047293,-0.601815023152048));
#21587=DIRECTION('ref_axis',(0.,-0.601815023152048,-0.798635510047293));
#21588=DIRECTION('',(-1.,0.,0.));
#21589=DIRECTION('',(0.,-0.601815023152048,-0.798635510047293));
#21590=DIRECTION('center_axis',(0.,0.857167300702113,-0.515038074910053));
#21591=DIRECTION('ref_axis',(0.,-0.515038074910053,-0.857167300702113));
#21592=DIRECTION('',(-1.,0.,0.));
#21593=DIRECTION('',(0.,-0.515038074910053,-0.857167300702113));
#21594=DIRECTION('center_axis',(0.,0.90630778703665,-0.422618261740699));
#21595=DIRECTION('ref_axis',(0.,-0.422618261740699,-0.90630778703665));
#21596=DIRECTION('',(-1.,0.,0.));
#21597=DIRECTION('',(0.,-0.422618261740699,-0.90630778703665));
#21598=DIRECTION('center_axis',(0.,0.945518575599317,-0.325568154457157));
#21599=DIRECTION('ref_axis',(0.,-0.325568154457157,-0.945518575599317));
#21600=DIRECTION('',(-1.,0.,0.));
#21601=DIRECTION('',(0.,-0.325568154457157,-0.945518575599317));
#21602=DIRECTION('center_axis',(0.,0.275637355816999,0.961261695938319));
#21603=DIRECTION('ref_axis',(0.,0.961261695938319,-0.275637355816999));
#21604=DIRECTION('',(-1.,0.,0.));
#21605=DIRECTION('',(0.,0.961261695938319,-0.275637355816999));
#21606=DIRECTION('center_axis',(0.,-0.945518575599317,0.325568154457155));
#21607=DIRECTION('ref_axis',(0.,0.325568154457155,0.945518575599317));
#21608=DIRECTION('',(-1.,0.,0.));
#21609=DIRECTION('',(0.,0.325568154457155,0.945518575599317));
#21610=DIRECTION('center_axis',(0.,-0.90630778703665,0.422618261740698));
#21611=DIRECTION('ref_axis',(0.,0.422618261740698,0.90630778703665));
#21612=DIRECTION('',(-1.,0.,0.));
#21613=DIRECTION('',(0.,0.422618261740698,0.90630778703665));
#21614=DIRECTION('center_axis',(0.,-0.857167300702112,0.515038074910055));
#21615=DIRECTION('ref_axis',(0.,0.515038074910055,0.857167300702112));
#21616=DIRECTION('',(-1.,0.,0.));
#21617=DIRECTION('',(0.,0.515038074910055,0.857167300702112));
#21618=DIRECTION('center_axis',(0.,-0.798635510047293,0.601815023152048));
#21619=DIRECTION('ref_axis',(0.,0.601815023152048,0.798635510047293));
#21620=DIRECTION('',(-1.,0.,0.));
#21621=DIRECTION('',(0.,0.601815023152048,0.798635510047293));
#21622=DIRECTION('center_axis',(0.,-0.73135370161917,0.681998360062499));
#21623=DIRECTION('ref_axis',(0.,0.681998360062499,0.73135370161917));
#21624=DIRECTION('',(-1.,0.,0.));
#21625=DIRECTION('',(0.,0.681998360062499,0.73135370161917));
#21626=DIRECTION('center_axis',(0.,-0.656059028990508,0.754709580222771));
#21627=DIRECTION('ref_axis',(0.,0.754709580222771,0.656059028990508));
#21628=DIRECTION('',(-1.,0.,0.));
#21629=DIRECTION('',(0.,0.754709580222771,0.656059028990508));
#21630=DIRECTION('center_axis',(0.,-0.788010753606722,-0.615661475325659));
#21631=DIRECTION('ref_axis',(0.,-0.615661475325658,0.788010753606722));
#21632=DIRECTION('',(0.,-0.615661475325658,0.788010753606722));
#21633=DIRECTION('center_axis',(-1.,0.,0.));
#21634=DIRECTION('ref_axis',(0.,0.,1.));
#21635=DIRECTION('center_axis',(0.,0.325568154457156,0.945518575599317));
#21636=DIRECTION('ref_axis',(0.,-0.945518575599317,0.325568154457156));
#21637=DIRECTION('',(1.,0.,0.));
#21638=DIRECTION('',(0.,-0.945518575599317,0.325568154457156));
#21639=DIRECTION('',(1.,0.,0.));
#21640=DIRECTION('center_axis',(0.,0.224951054343865,0.974370064785235));
#21641=DIRECTION('ref_axis',(0.,-0.974370064785235,0.224951054343865));
#21642=DIRECTION('',(1.,0.,0.));
#21643=DIRECTION('',(0.,-0.974370064785235,0.224951054343865));
#21644=DIRECTION('center_axis',(0.,0.121869343405148,0.992546151641322));
#21645=DIRECTION('ref_axis',(0.,-0.992546151641322,0.121869343405148));
#21646=DIRECTION('',(1.,0.,0.));
#21647=DIRECTION('',(0.,-0.992546151641322,0.121869343405148));
#21648=DIRECTION('center_axis',(0.,0.0174524064372842,0.999847695156391));
#21649=DIRECTION('ref_axis',(0.,-0.999847695156391,0.0174524064372842));
#21650=DIRECTION('',(1.,0.,0.));
#21651=DIRECTION('',(0.,-0.999847695156391,0.0174524064372842));
#21652=DIRECTION('center_axis',(0.,-0.0871557427476568,0.996194698091746));
#21653=DIRECTION('ref_axis',(0.,-0.996194698091746,-0.0871557427476568));
#21654=DIRECTION('',(1.,0.,0.));
#21655=DIRECTION('',(0.,-0.996194698091746,-0.0871557427476568));
#21656=DIRECTION('center_axis',(0.,-0.190808995376545,0.981627183447664));
#21657=DIRECTION('ref_axis',(0.,-0.981627183447664,-0.190808995376545));
#21658=DIRECTION('',(1.,0.,0.));
#21659=DIRECTION('',(0.,-0.981627183447664,-0.190808995376545));
#21660=DIRECTION('center_axis',(0.,0.970295726275997,0.241921895599667));
#21661=DIRECTION('ref_axis',(0.,-0.241921895599667,0.970295726275997));
#21662=DIRECTION('',(1.,0.,0.));
#21663=DIRECTION('',(0.,-0.241921895599667,0.970295726275997));
#21664=DIRECTION('center_axis',(0.,0.190808995376544,-0.981627183447664));
#21665=DIRECTION('ref_axis',(0.,0.981627183447664,0.190808995376544));
#21666=DIRECTION('',(1.,0.,0.));
#21667=DIRECTION('',(0.,0.981627183447664,0.190808995376544));
#21668=DIRECTION('center_axis',(0.,0.087155742747658,-0.996194698091746));
#21669=DIRECTION('ref_axis',(0.,0.996194698091746,0.087155742747658));
#21670=DIRECTION('',(1.,0.,0.));
#21671=DIRECTION('',(0.,0.996194698091746,0.087155742747658));
#21672=DIRECTION('center_axis',(0.,-0.017452406437284,-0.999847695156391));
#21673=DIRECTION('ref_axis',(0.,0.999847695156391,-0.017452406437284));
#21674=DIRECTION('',(1.,0.,0.));
#21675=DIRECTION('',(0.,0.999847695156391,-0.017452406437284));
#21676=DIRECTION('center_axis',(0.,-0.121869343405148,-0.992546151641322));
#21677=DIRECTION('ref_axis',(0.,0.992546151641322,-0.121869343405148));
#21678=DIRECTION('',(1.,0.,0.));
#21679=DIRECTION('',(0.,0.992546151641322,-0.121869343405148));
#21680=DIRECTION('center_axis',(0.,-0.224951054343867,-0.974370064785235));
#21681=DIRECTION('ref_axis',(0.,0.974370064785235,-0.224951054343867));
#21682=DIRECTION('',(1.,0.,0.));
#21683=DIRECTION('',(0.,0.974370064785235,-0.224951054343867));
#21684=DIRECTION('center_axis',(0.,-0.325568154457156,-0.945518575599317));
#21685=DIRECTION('ref_axis',(0.,0.945518575599317,-0.325568154457156));
#21686=DIRECTION('',(1.,0.,0.));
#21687=DIRECTION('',(0.,0.945518575599317,-0.325568154457156));
#21688=DIRECTION('center_axis',(0.,-0.927183854566787,0.374606593415912));
#21689=DIRECTION('ref_axis',(0.,-0.374606593415912,-0.927183854566787));
#21690=DIRECTION('',(0.,-0.374606593415912,-0.927183854566787));
#21691=DIRECTION('center_axis',(1.,0.,0.));
#21692=DIRECTION('ref_axis',(0.,0.,-1.));
#21693=DIRECTION('center_axis',(0.,-0.981627183447664,-0.190808995376546));
#21694=DIRECTION('ref_axis',(0.,0.190808995376546,-0.981627183447664));
#21695=DIRECTION('',(1.,0.,0.));
#21696=DIRECTION('',(0.,0.190808995376546,-0.981627183447664));
#21697=DIRECTION('',(1.,0.,0.));
#21698=DIRECTION('center_axis',(0.,-0.956304755963036,-0.292371704722736));
#21699=DIRECTION('ref_axis',(0.,0.292371704722736,-0.956304755963036));
#21700=DIRECTION('',(1.,0.,0.));
#21701=DIRECTION('',(0.,0.292371704722736,-0.956304755963036));
#21702=DIRECTION('center_axis',(0.,-0.92050485345244,-0.390731128489275));
#21703=DIRECTION('ref_axis',(0.,0.390731128489275,-0.92050485345244));
#21704=DIRECTION('',(1.,0.,0.));
#21705=DIRECTION('',(0.,0.390731128489275,-0.92050485345244));
#21706=DIRECTION('center_axis',(0.,-0.874619707139396,-0.484809620246337));
#21707=DIRECTION('ref_axis',(0.,0.484809620246337,-0.874619707139396));
#21708=DIRECTION('',(1.,0.,0.));
#21709=DIRECTION('',(0.,0.484809620246338,-0.874619707139396));
#21710=DIRECTION('center_axis',(0.,-0.819152044288992,-0.573576436351045));
#21711=DIRECTION('ref_axis',(0.,0.573576436351045,-0.819152044288992));
#21712=DIRECTION('',(1.,0.,0.));
#21713=DIRECTION('',(0.,0.573576436351045,-0.819152044288992));
#21714=DIRECTION('center_axis',(0.,-0.754709580222773,-0.656059028990507));
#21715=DIRECTION('ref_axis',(0.,0.656059028990507,-0.754709580222773));
#21716=DIRECTION('',(1.,0.,0.));
#21717=DIRECTION('',(0.,0.656059028990507,-0.754709580222773));
#21718=DIRECTION('center_axis',(0.,-0.694658370458997,0.719339800338651));
#21719=DIRECTION('ref_axis',(0.,-0.719339800338651,-0.694658370458997));
#21720=DIRECTION('',(1.,0.,0.));
#21721=DIRECTION('',(0.,-0.719339800338651,-0.694658370458997));
#21722=DIRECTION('center_axis',(0.,0.754709580222772,0.656059028990507));
#21723=DIRECTION('ref_axis',(0.,-0.656059028990507,0.754709580222772));
#21724=DIRECTION('',(1.,0.,0.));
#21725=DIRECTION('',(0.,-0.656059028990507,0.754709580222772));
#21726=DIRECTION('center_axis',(0.,0.819152044288992,0.573576436351046));
#21727=DIRECTION('ref_axis',(0.,-0.573576436351046,0.819152044288992));
#21728=DIRECTION('',(1.,0.,0.));
#21729=DIRECTION('',(0.,-0.573576436351046,0.819152044288992));
#21730=DIRECTION('center_axis',(0.,0.874619707139396,0.484809620246338));
#21731=DIRECTION('ref_axis',(0.,-0.484809620246338,0.874619707139396));
#21732=DIRECTION('',(1.,0.,0.));
#21733=DIRECTION('',(0.,-0.484809620246338,0.874619707139396));
#21734=DIRECTION('center_axis',(0.,0.92050485345244,0.390731128489274));
#21735=DIRECTION('ref_axis',(0.,-0.390731128489274,0.92050485345244));
#21736=DIRECTION('',(1.,0.,0.));
#21737=DIRECTION('',(0.,-0.390731128489274,0.92050485345244));
#21738=DIRECTION('center_axis',(0.,0.956304755963036,0.292371704722736));
#21739=DIRECTION('ref_axis',(0.,-0.292371704722736,0.956304755963036));
#21740=DIRECTION('',(1.,0.,0.));
#21741=DIRECTION('',(0.,-0.292371704722736,0.956304755963036));
#21742=DIRECTION('center_axis',(0.,0.981627183447664,0.190808995376545));
#21743=DIRECTION('ref_axis',(0.,-0.190808995376545,0.981627183447664));
#21744=DIRECTION('',(1.,0.,0.));
#21745=DIRECTION('',(0.,-0.190808995376545,0.981627183447664));
#21746=DIRECTION('center_axis',(0.,0.139173100960065,-0.99026806874157));
#21747=DIRECTION('ref_axis',(0.,0.99026806874157,0.139173100960065));
#21748=DIRECTION('',(0.,0.99026806874157,0.139173100960065));
#21749=DIRECTION('center_axis',(1.,0.,0.));
#21750=DIRECTION('ref_axis',(0.,0.,-1.));
#21751=DIRECTION('center_axis',(0.,-0.325568154457157,-0.945518575599317));
#21752=DIRECTION('ref_axis',(0.,0.945518575599317,-0.325568154457157));
#21753=DIRECTION('',(1.,0.,0.));
#21754=DIRECTION('',(0.,0.945518575599317,-0.325568154457157));
#21755=DIRECTION('',(1.,0.,0.));
#21756=DIRECTION('center_axis',(0.,-0.224951054343866,-0.974370064785235));
#21757=DIRECTION('ref_axis',(0.,0.974370064785235,-0.224951054343866));
#21758=DIRECTION('',(1.,0.,0.));
#21759=DIRECTION('',(0.,0.974370064785235,-0.224951054343866));
#21760=DIRECTION('center_axis',(0.,-0.121869343405146,-0.992546151641322));
#21761=DIRECTION('ref_axis',(0.,0.992546151641322,-0.121869343405146));
#21762=DIRECTION('',(1.,0.,0.));
#21763=DIRECTION('',(0.,0.992546151641322,-0.121869343405146));
#21764=DIRECTION('center_axis',(0.,-0.0174524064372842,-0.999847695156391));
#21765=DIRECTION('ref_axis',(0.,0.999847695156391,-0.0174524064372842));
#21766=DIRECTION('',(1.,0.,0.));
#21767=DIRECTION('',(0.,0.999847695156391,-0.0174524064372842));
#21768=DIRECTION('center_axis',(0.,0.0871557427476587,-0.996194698091746));
#21769=DIRECTION('ref_axis',(0.,0.996194698091746,0.0871557427476587));
#21770=DIRECTION('',(1.,0.,0.));
#21771=DIRECTION('',(0.,0.996194698091746,0.0871557427476587));
#21772=DIRECTION('center_axis',(0.,0.190808995376545,-0.981627183447664));
#21773=DIRECTION('ref_axis',(0.,0.981627183447664,0.190808995376545));
#21774=DIRECTION('',(1.,0.,0.));
#21775=DIRECTION('',(0.,0.981627183447664,0.190808995376545));
#21776=DIRECTION('center_axis',(0.,-0.970295726275996,-0.241921895599668));
#21777=DIRECTION('ref_axis',(0.,0.241921895599668,-0.970295726275996));
#21778=DIRECTION('',(1.,0.,0.));
#21779=DIRECTION('',(0.,0.241921895599668,-0.970295726275996));
#21780=DIRECTION('center_axis',(0.,-0.190808995376544,0.981627183447664));
#21781=DIRECTION('ref_axis',(0.,-0.981627183447664,-0.190808995376544));
#21782=DIRECTION('',(1.,0.,0.));
#21783=DIRECTION('',(0.,-0.981627183447664,-0.190808995376544));
#21784=DIRECTION('center_axis',(0.,-0.0871557427476604,0.996194698091745));
#21785=DIRECTION('ref_axis',(0.,-0.996194698091745,-0.0871557427476604));
#21786=DIRECTION('',(1.,0.,0.));
#21787=DIRECTION('',(0.,-0.996194698091745,-0.0871557427476604));
#21788=DIRECTION('center_axis',(0.,0.017452406437284,0.999847695156391));
#21789=DIRECTION('ref_axis',(0.,-0.999847695156391,0.017452406437284));
#21790=DIRECTION('',(1.,0.,0.));
#21791=DIRECTION('',(0.,-0.999847695156391,0.017452406437284));
#21792=DIRECTION('center_axis',(0.,0.121869343405146,0.992546151641322));
#21793=DIRECTION('ref_axis',(0.,-0.992546151641322,0.121869343405146));
#21794=DIRECTION('',(1.,0.,0.));
#21795=DIRECTION('',(0.,-0.992546151641322,0.121869343405145));
#21796=DIRECTION('center_axis',(0.,0.224951054343866,0.974370064785235));
#21797=DIRECTION('ref_axis',(0.,-0.974370064785235,0.224951054343866));
#21798=DIRECTION('',(1.,0.,0.));
#21799=DIRECTION('',(0.,-0.974370064785235,0.224951054343866));
#21800=DIRECTION('center_axis',(0.,0.325568154457158,0.945518575599316));
#21801=DIRECTION('ref_axis',(0.,-0.945518575599316,0.325568154457158));
#21802=DIRECTION('',(1.,0.,0.));
#21803=DIRECTION('',(0.,-0.945518575599316,0.325568154457158));
#21804=DIRECTION('center_axis',(0.,0.927183854566787,-0.374606593415912));
#21805=DIRECTION('ref_axis',(0.,0.374606593415912,0.927183854566787));
#21806=DIRECTION('',(0.,0.374606593415912,0.927183854566787));
#21807=DIRECTION('center_axis',(1.,0.,0.));
#21808=DIRECTION('ref_axis',(0.,0.,-1.));
#21809=DIRECTION('center_axis',(0.,0.656059028990507,-0.754709580222772));
#21810=DIRECTION('ref_axis',(0.,0.754709580222772,0.656059028990507));
#21811=DIRECTION('',(1.,0.,0.));
#21812=DIRECTION('',(0.,0.754709580222772,0.656059028990507));
#21813=DIRECTION('',(1.,0.,0.));
#21814=DIRECTION('center_axis',(0.,0.731353701619171,-0.681998360062498));
#21815=DIRECTION('ref_axis',(0.,0.681998360062498,0.731353701619171));
#21816=DIRECTION('',(1.,0.,0.));
#21817=DIRECTION('',(0.,0.681998360062498,0.731353701619171));
#21818=DIRECTION('center_axis',(0.,0.798635510047292,-0.601815023152049));
#21819=DIRECTION('ref_axis',(0.,0.601815023152049,0.798635510047292));
#21820=DIRECTION('',(1.,0.,0.));
#21821=DIRECTION('',(0.,0.601815023152049,0.798635510047292));
#21822=DIRECTION('center_axis',(0.,0.857167300702112,-0.515038074910054));
#21823=DIRECTION('ref_axis',(0.,0.515038074910054,0.857167300702112));
#21824=DIRECTION('',(1.,0.,0.));
#21825=DIRECTION('',(0.,0.515038074910054,0.857167300702112));
#21826=DIRECTION('center_axis',(0.,0.90630778703665,-0.422618261740699));
#21827=DIRECTION('ref_axis',(0.,0.422618261740699,0.90630778703665));
#21828=DIRECTION('',(1.,0.,0.));
#21829=DIRECTION('',(0.,0.422618261740699,0.90630778703665));
#21830=DIRECTION('center_axis',(0.,0.945518575599317,-0.325568154457157));
#21831=DIRECTION('ref_axis',(0.,0.325568154457156,0.945518575599317));
#21832=DIRECTION('',(1.,0.,0.));
#21833=DIRECTION('',(0.,0.325568154457156,0.945518575599317));
#21834=DIRECTION('center_axis',(0.,-0.275637355816999,-0.961261695938319));
#21835=DIRECTION('ref_axis',(0.,0.961261695938319,-0.275637355816999));
#21836=DIRECTION('',(1.,0.,0.));
#21837=DIRECTION('',(0.,0.961261695938319,-0.275637355816999));
#21838=DIRECTION('center_axis',(0.,-0.945518575599316,0.325568154457159));
#21839=DIRECTION('ref_axis',(0.,-0.325568154457159,-0.945518575599316));
#21840=DIRECTION('',(1.,0.,0.));
#21841=DIRECTION('',(0.,-0.325568154457159,-0.945518575599316));
#21842=DIRECTION('center_axis',(0.,-0.90630778703665,0.4226182617407));
#21843=DIRECTION('ref_axis',(0.,-0.4226182617407,-0.90630778703665));
#21844=DIRECTION('',(1.,0.,0.));
#21845=DIRECTION('',(0.,-0.4226182617407,-0.90630778703665));
#21846=DIRECTION('center_axis',(0.,-0.857167300702112,0.515038074910054));
#21847=DIRECTION('ref_axis',(0.,-0.515038074910054,-0.857167300702112));
#21848=DIRECTION('',(1.,0.,0.));
#21849=DIRECTION('',(0.,-0.515038074910054,-0.857167300702112));
#21850=DIRECTION('center_axis',(0.,-0.798635510047293,0.601815023152048));
#21851=DIRECTION('ref_axis',(0.,-0.601815023152048,-0.798635510047293));
#21852=DIRECTION('',(1.,0.,0.));
#21853=DIRECTION('',(0.,-0.601815023152048,-0.798635510047293));
#21854=DIRECTION('center_axis',(0.,-0.731353701619171,0.681998360062498));
#21855=DIRECTION('ref_axis',(0.,-0.681998360062498,-0.731353701619171));
#21856=DIRECTION('',(1.,0.,0.));
#21857=DIRECTION('',(0.,-0.681998360062498,-0.731353701619171));
#21858=DIRECTION('center_axis',(0.,-0.656059028990507,0.754709580222772));
#21859=DIRECTION('ref_axis',(0.,-0.754709580222772,-0.656059028990507));
#21860=DIRECTION('',(1.,0.,0.));
#21861=DIRECTION('',(0.,-0.754709580222772,-0.656059028990507));
#21862=DIRECTION('center_axis',(0.,0.788010753606722,0.615661475325659));
#21863=DIRECTION('ref_axis',(0.,-0.615661475325659,0.788010753606722));
#21864=DIRECTION('',(0.,-0.615661475325659,0.788010753606722));
#21865=DIRECTION('center_axis',(1.,0.,0.));
#21866=DIRECTION('ref_axis',(0.,0.,-1.));
#21867=DIRECTION('center_axis',(0.,0.981627183447664,0.190808995376545));
#21868=DIRECTION('ref_axis',(0.,-0.190808995376545,0.981627183447664));
#21869=DIRECTION('',(1.,0.,0.));
#21870=DIRECTION('',(0.,-0.190808995376545,0.981627183447664));
#21871=DIRECTION('',(1.,0.,0.));
#21872=DIRECTION('center_axis',(0.,0.956304755963036,0.292371704722737));
#21873=DIRECTION('ref_axis',(0.,-0.292371704722737,0.956304755963036));
#21874=DIRECTION('',(1.,0.,0.));
#21875=DIRECTION('',(0.,-0.292371704722737,0.956304755963036));
#21876=DIRECTION('center_axis',(0.,0.92050485345244,0.390731128489274));
#21877=DIRECTION('ref_axis',(0.,-0.390731128489274,0.92050485345244));
#21878=DIRECTION('',(1.,0.,0.));
#21879=DIRECTION('',(0.,-0.390731128489274,0.92050485345244));
#21880=DIRECTION('center_axis',(0.,0.874619707139396,0.484809620246337));
#21881=DIRECTION('ref_axis',(0.,-0.484809620246337,0.874619707139396));
#21882=DIRECTION('',(1.,0.,0.));
#21883=DIRECTION('',(0.,-0.484809620246337,0.874619707139396));
#21884=DIRECTION('center_axis',(0.,0.819152044288992,0.573576436351047));
#21885=DIRECTION('ref_axis',(0.,-0.573576436351047,0.819152044288992));
#21886=DIRECTION('',(1.,0.,0.));
#21887=DIRECTION('',(0.,-0.573576436351047,0.819152044288992));
#21888=DIRECTION('center_axis',(0.,0.754709580222772,0.656059028990507));
#21889=DIRECTION('ref_axis',(0.,-0.656059028990507,0.754709580222772));
#21890=DIRECTION('',(1.,0.,0.));
#21891=DIRECTION('',(0.,-0.656059028990507,0.754709580222772));
#21892=DIRECTION('center_axis',(0.,0.694658370458997,-0.719339800338651));
#21893=DIRECTION('ref_axis',(0.,0.719339800338651,0.694658370458997));
#21894=DIRECTION('',(1.,0.,0.));
#21895=DIRECTION('',(0.,0.719339800338651,0.694658370458997));
#21896=DIRECTION('center_axis',(0.,-0.754709580222772,-0.656059028990507));
#21897=DIRECTION('ref_axis',(0.,0.656059028990507,-0.754709580222772));
#21898=DIRECTION('',(1.,0.,0.));
#21899=DIRECTION('',(0.,0.656059028990507,-0.754709580222772));
#21900=DIRECTION('center_axis',(0.,-0.819152044288991,-0.573576436351047));
#21901=DIRECTION('ref_axis',(0.,0.573576436351047,-0.819152044288991));
#21902=DIRECTION('',(1.,0.,0.));
#21903=DIRECTION('',(0.,0.573576436351047,-0.819152044288991));
#21904=DIRECTION('center_axis',(0.,-0.874619707139396,-0.484809620246337));
#21905=DIRECTION('ref_axis',(0.,0.484809620246337,-0.874619707139396));
#21906=DIRECTION('',(1.,0.,0.));
#21907=DIRECTION('',(0.,0.484809620246337,-0.874619707139396));
#21908=DIRECTION('center_axis',(0.,-0.92050485345244,-0.390731128489274));
#21909=DIRECTION('ref_axis',(0.,0.390731128489274,-0.92050485345244));
#21910=DIRECTION('',(1.,0.,0.));
#21911=DIRECTION('',(0.,0.390731128489274,-0.92050485345244));
#21912=DIRECTION('center_axis',(0.,-0.956304755963035,-0.292371704722737));
#21913=DIRECTION('ref_axis',(0.,0.292371704722737,-0.956304755963035));
#21914=DIRECTION('',(1.,0.,0.));
#21915=DIRECTION('',(0.,0.292371704722737,-0.956304755963035));
#21916=DIRECTION('center_axis',(0.,-0.981627183447664,-0.190808995376543));
#21917=DIRECTION('ref_axis',(0.,0.190808995376543,-0.981627183447664));
#21918=DIRECTION('',(1.,0.,0.));
#21919=DIRECTION('',(0.,0.190808995376543,-0.981627183447664));
#21920=DIRECTION('center_axis',(0.,-0.139173100960066,0.99026806874157));
#21921=DIRECTION('ref_axis',(0.,-0.99026806874157,-0.139173100960066));
#21922=DIRECTION('',(0.,-0.99026806874157,-0.139173100960066));
#21923=DIRECTION('center_axis',(1.,0.,0.));
#21924=DIRECTION('ref_axis',(0.,0.,-1.));
#21925=DIRECTION('center_axis',(0.,-0.656059028990508,0.754709580222771));
#21926=DIRECTION('ref_axis',(0.,-0.754709580222771,-0.656059028990508));
#21927=DIRECTION('',(1.,0.,0.));
#21928=DIRECTION('',(0.,-0.754709580222771,-0.656059028990508));
#21929=DIRECTION('',(1.,0.,0.));
#21930=DIRECTION('center_axis',(0.,-0.73135370161917,0.681998360062499));
#21931=DIRECTION('ref_axis',(0.,-0.681998360062499,-0.73135370161917));
#21932=DIRECTION('',(1.,0.,0.));
#21933=DIRECTION('',(0.,-0.681998360062499,-0.73135370161917));
#21934=DIRECTION('center_axis',(0.,-0.798635510047293,0.601815023152048));
#21935=DIRECTION('ref_axis',(0.,-0.601815023152048,-0.798635510047293));
#21936=DIRECTION('',(1.,0.,0.));
#21937=DIRECTION('',(0.,-0.601815023152048,-0.798635510047293));
#21938=DIRECTION('center_axis',(0.,-0.857167300702112,0.515038074910055));
#21939=DIRECTION('ref_axis',(0.,-0.515038074910055,-0.857167300702112));
#21940=DIRECTION('',(1.,0.,0.));
#21941=DIRECTION('',(0.,-0.515038074910055,-0.857167300702112));
#21942=DIRECTION('center_axis',(0.,-0.90630778703665,0.422618261740698));
#21943=DIRECTION('ref_axis',(0.,-0.422618261740698,-0.90630778703665));
#21944=DIRECTION('',(1.,0.,0.));
#21945=DIRECTION('',(0.,-0.422618261740698,-0.90630778703665));
#21946=DIRECTION('center_axis',(0.,-0.945518575599317,0.325568154457155));
#21947=DIRECTION('ref_axis',(0.,-0.325568154457155,-0.945518575599317));
#21948=DIRECTION('',(1.,0.,0.));
#21949=DIRECTION('',(0.,-0.325568154457155,-0.945518575599317));
#21950=DIRECTION('center_axis',(0.,0.275637355816999,0.961261695938319));
#21951=DIRECTION('ref_axis',(0.,-0.961261695938319,0.275637355816999));
#21952=DIRECTION('',(1.,0.,0.));
#21953=DIRECTION('',(0.,-0.961261695938319,0.275637355816999));
#21954=DIRECTION('center_axis',(0.,0.945518575599317,-0.325568154457157));
#21955=DIRECTION('ref_axis',(0.,0.325568154457157,0.945518575599317));
#21956=DIRECTION('',(1.,0.,0.));
#21957=DIRECTION('',(0.,0.325568154457157,0.945518575599317));
#21958=DIRECTION('center_axis',(0.,0.90630778703665,-0.422618261740699));
#21959=DIRECTION('ref_axis',(0.,0.422618261740699,0.90630778703665));
#21960=DIRECTION('',(1.,0.,0.));
#21961=DIRECTION('',(0.,0.422618261740699,0.90630778703665));
#21962=DIRECTION('center_axis',(0.,0.857167300702113,-0.515038074910053));
#21963=DIRECTION('ref_axis',(0.,0.515038074910053,0.857167300702113));
#21964=DIRECTION('',(1.,0.,0.));
#21965=DIRECTION('',(0.,0.515038074910053,0.857167300702113));
#21966=DIRECTION('center_axis',(0.,0.798635510047293,-0.601815023152048));
#21967=DIRECTION('ref_axis',(0.,0.601815023152048,0.798635510047293));
#21968=DIRECTION('',(1.,0.,0.));
#21969=DIRECTION('',(0.,0.601815023152048,0.798635510047293));
#21970=DIRECTION('center_axis',(0.,0.73135370161917,-0.681998360062499));
#21971=DIRECTION('ref_axis',(0.,0.681998360062499,0.73135370161917));
#21972=DIRECTION('',(1.,0.,0.));
#21973=DIRECTION('',(0.,0.681998360062499,0.73135370161917));
#21974=DIRECTION('center_axis',(0.,0.656059028990508,-0.754709580222772));
#21975=DIRECTION('ref_axis',(0.,0.754709580222772,0.656059028990508));
#21976=DIRECTION('',(1.,0.,0.));
#21977=DIRECTION('',(0.,0.754709580222772,0.656059028990508));
#21978=DIRECTION('center_axis',(0.,-0.788010753606722,-0.615661475325659));
#21979=DIRECTION('ref_axis',(0.,0.615661475325658,-0.788010753606722));
#21980=DIRECTION('',(0.,0.615661475325658,-0.788010753606722));
#21981=DIRECTION('center_axis',(1.,0.,0.));
#21982=DIRECTION('ref_axis',(0.,0.,-1.));
#21983=DIRECTION('center_axis',(1.,0.,0.));
#21984=DIRECTION('ref_axis',(0.,0.,-1.));
#21985=DIRECTION('',(-1.,0.,0.));
#21986=DIRECTION('',(-1.,0.,0.));
#21987=DIRECTION('center_axis',(0.,-1.,0.));
#21988=DIRECTION('ref_axis',(0.,0.,-1.));
#43758=CARTESIAN_POINT('',(0.,0.,0.));
#43759=CARTESIAN_POINT('Origin',(3.9,2.5,14.9));
#43760=CARTESIAN_POINT('',(4.,5.,14.8));
#43761=CARTESIAN_POINT('',(3.8,5.,15.));
#43762=CARTESIAN_POINT('',(2.58798079768202,5.,16.212019202318));
#43763=CARTESIAN_POINT('',(3.8,-5.,15.));
#43764=CARTESIAN_POINT('',(3.8,2.5,15.));
#43765=CARTESIAN_POINT('',(4.,-5.,14.8));
#43766=CARTESIAN_POINT('',(2.9,-5.,15.9));
#43767=CARTESIAN_POINT('',(4.,2.5,14.8));
#43768=CARTESIAN_POINT('Origin',(0.,5.,15.));
#43769=CARTESIAN_POINT('',(0.2,5.,15.));
#43770=CARTESIAN_POINT('',(0.,5.,15.));
#43771=CARTESIAN_POINT('',(0.2,-5.,15.));
#43772=CARTESIAN_POINT('',(0.2,2.5,15.));
#43773=CARTESIAN_POINT('',(0.,-5.,15.));
#43774=CARTESIAN_POINT('',(0.8,-1.46957615897682E-16,15.));
#43775=CARTESIAN_POINT('Origin',(2.,0.,15.));
#43776=CARTESIAN_POINT('Origin',(0.1,2.5,14.9));
#43777=CARTESIAN_POINT('',(0.,5.,14.8));
#43778=CARTESIAN_POINT('',(0.41201920231798,5.,15.212019202318));
#43779=CARTESIAN_POINT('',(0.,-5.,14.8));
#43780=CARTESIAN_POINT('',(0.,2.5,14.8));
#43781=CARTESIAN_POINT('',(0.1,-5.,14.9));
#43782=CARTESIAN_POINT('Origin',(0.,0.,-0.375961595364038));
#43783=CARTESIAN_POINT('',(0.,-5.,16.0387031894726));
#43784=CARTESIAN_POINT('',(0.,-5.,15.));
#43785=CARTESIAN_POINT('',(0.,5.,16.0387031894726));
#43786=CARTESIAN_POINT('',(0.,5.,21.));
#43787=CARTESIAN_POINT('Origin',(0.,0.,0.));
#43788=CARTESIAN_POINT('',(0.,-2.13088543051639E-15,-10.65));
#43789=CARTESIAN_POINT('Origin',(0.,-2.47990976827339E-15,-13.5));
#43790=CARTESIAN_POINT('',(0.,-11.6913429510899,-3.9));
#43791=CARTESIAN_POINT('Origin',(0.,-11.6913429510899,-6.75));
#43792=CARTESIAN_POINT('',(0.,-7.16418377501202E-16,5.85));
#43793=CARTESIAN_POINT('Origin',(0.,0.,0.));
#43794=CARTESIAN_POINT('',(0.,5.00154026730478,-5.17924656243829));
#43795=CARTESIAN_POINT('',(0.,4.43276262234474,-5.6736774259684));
#43796=CARTESIAN_POINT('',(0.,4.76627016532424,-5.38376374189465));
#43797=CARTESIAN_POINT('',(0.,6.52601163845198,-8.35291398823125));
#43798=CARTESIAN_POINT('',(0.,2.30757979347878,-2.95356744728099));
#43799=CARTESIAN_POINT('',(0.,7.36337872686537,-7.6250018835897));
#43800=CARTESIAN_POINT('',(0.,6.64227771981479,-8.2518454256447));
#43801=CARTESIAN_POINT('',(0.,8.12007109706117,-6.81354866267731));
#43802=CARTESIAN_POINT('',(0.,7.45879037646094,-7.52268541599157));
#43803=CARTESIAN_POINT('',(0.,8.78779826908344,-5.92744477678991));
#43804=CARTESIAN_POINT('',(0.,8.19665351987491,-6.7119203550552));
#43805=CARTESIAN_POINT('',(0.,9.35924448430463,-4.97639856553044));
#43806=CARTESIAN_POINT('',(0.,8.84767122648022,-5.82779944224681));
#43807=CARTESIAN_POINT('',(0.,9.82814885840795,-3.97082989020866));
#43808=CARTESIAN_POINT('',(0.,9.40446975509177,-4.8794126593455));
#43809=CARTESIAN_POINT('',(0.,10.1893739769462,-2.92175597166019));
#43810=CARTESIAN_POINT('',(0.,9.8605888704256,-3.87661725443506));
#43811=CARTESIAN_POINT('',(0.,6.9210842107559,-1.98458896188239));
#43812=CARTESIAN_POINT('',(0.,5.1444943114719,-1.475160005877));
#43813=CARTESIAN_POINT('',(0.,6.67572375288087,-2.69716747259456));
#43814=CARTESIAN_POINT('',(0.,6.80187782867024,-2.33078943342394));
#43815=CARTESIAN_POINT('',(0.,6.35722266858427,-3.38019525205841));
#43816=CARTESIAN_POINT('',(0.,6.52409765906803,-3.02233068010603));
#43817=CARTESIAN_POINT('',(0.,5.9690705223963,-4.02618890498938));
#43818=CARTESIAN_POINT('',(0.,6.17719603562876,-3.67980988356293));
#43819=CARTESIAN_POINT('',(0.,5.51551999045664,-4.62807078974308));
#43820=CARTESIAN_POINT('',(0.,5.76533351921956,-4.29655704002753));
#43821=CARTESIAN_POINT('',(0.,5.2932636167153,-4.86641157054685));
#43822=CARTESIAN_POINT('',(0.,-6.98612922918717,-1.74183764831761));
#43823=CARTESIAN_POINT('',(0.,-7.12993009493931,-1.00204632691247));
#43824=CARTESIAN_POINT('',(0.,-6.98687002250157,-1.73802659709701));
#43825=CARTESIAN_POINT('',(0.,-10.4968415286606,-1.47523487017669));
#43826=CARTESIAN_POINT('',(0.,-3.59087231247837,-0.504664192105417));
#43827=CARTESIAN_POINT('',(0.,-10.2851346985256,-2.56437209335648));
#43828=CARTESIAN_POINT('',(0.,-10.4087053980032,-1.92865595510232));
#43829=CARTESIAN_POINT('',(0.,-9.96074178033063,-3.62541351925209));
#43830=CARTESIAN_POINT('',(0.,-10.1514777049506,-3.00154442077003));
#43831=CARTESIAN_POINT('',(0.,-9.52721689077117,-4.64673415596422));
#43832=CARTESIAN_POINT('',(0.,-9.78474952320472,-4.04002529456882));
#43833=CARTESIAN_POINT('',(0.,-8.98930981925811,-5.61714420087197));
#43834=CARTESIAN_POINT('',(0.,-9.3130317440988,-5.03313438903098));
#43835=CARTESIAN_POINT('',(0.,-8.35291398823125,-6.52601163845198));
#43836=CARTESIAN_POINT('',(0.,-8.74188877728577,-5.97049806879083));
#43837=CARTESIAN_POINT('',(0.,-7.6250018835897,-7.36337872686537));
#43838=CARTESIAN_POINT('',(0.,-8.07786027133033,-6.84242474466351));
#43839=CARTESIAN_POINT('',(0.,-5.17924656243829,-5.00154026730478));
#43840=CARTESIAN_POINT('',(0.,-3.90643408422442,-3.77239954465928));
#43841=CARTESIAN_POINT('',(0.,-5.6736774259684,-4.43276262234474));
#43842=CARTESIAN_POINT('',(0.,-5.20977858758028,-4.96641719017296));
#43843=CARTESIAN_POINT('',(0.,-6.10594629232627,-3.81541870247908));
#43844=CARTESIAN_POINT('',(0.,-5.69342255834225,-4.40456365090217));
#43845=CARTESIAN_POINT('',(0.,-6.471317133354,-3.15627225688136));
#43846=CARTESIAN_POINT('',(0.,-6.1175806237891,-3.79442981291947));
#43847=CARTESIAN_POINT('',(0.,-6.76578686965854,-2.46254503194481));
#43848=CARTESIAN_POINT('',(0.,-6.4773235326941,-3.14212206678592));
#43849=CARTESIAN_POINT('',(0.,-6.76831369551442,-2.45428015697765));
#43850=CARTESIAN_POINT('',(0.,-5.00154026730478,5.17924656243829));
#43851=CARTESIAN_POINT('',(0.,-4.43276262234474,5.6736774259684));
#43852=CARTESIAN_POINT('',(0.,-4.95242154680531,5.22194481474698));
#43853=CARTESIAN_POINT('',(0.,-6.52601163845198,8.35291398823125));
#43854=CARTESIAN_POINT('',(0.,-2.12518282886596,2.7201099786874));
#43855=CARTESIAN_POINT('',(0.,-7.36337872686537,7.6250018835897));
#43856=CARTESIAN_POINT('',(0.,-6.82842910129586,8.09002649849703));
#43857=CARTESIAN_POINT('',(0.,-8.12007109706117,6.81354866267732));
#43858=CARTESIAN_POINT('',(0.,-7.64631326236769,7.32159174073164));
#43859=CARTESIAN_POINT('',(0.,-8.78779826908344,5.92744477678992));
#43860=CARTESIAN_POINT('',(0.,-8.37735226025856,6.47212502735574));
#43861=CARTESIAN_POINT('',(0.,-9.35924448430463,4.97639856553044));
#43862=CARTESIAN_POINT('',(0.,-9.01364841929725,5.55156700570328));
#43863=CARTESIAN_POINT('',(0.,-9.82814885840794,3.97082989020867));
#43864=CARTESIAN_POINT('',(0.,-9.54847140056915,4.57060013405449));
#43865=CARTESIAN_POINT('',(0.,-10.1893739769462,2.92175597166019));
#43866=CARTESIAN_POINT('',(0.,-9.9763214056594,3.54050556670805));
#43867=CARTESIAN_POINT('',(0.,-6.9210842107559,1.98458896188239));
#43868=CARTESIAN_POINT('',(0.,-5.04487966547428,1.44659596578319));
#43869=CARTESIAN_POINT('',(0.,-6.67572375288087,2.69716747259457));
#43870=CARTESIAN_POINT('',(0.,-6.91761036390404,1.99467774569693));
#43871=CARTESIAN_POINT('',(0.,-6.35722266858427,3.38019525205841));
#43872=CARTESIAN_POINT('',(0.,-6.66809930454541,2.71351815481502));
#43873=CARTESIAN_POINT('',(0.,-5.9690705223963,4.02618890498938));
#43874=CARTESIAN_POINT('',(0.,-6.3431732284458,3.40357744701939));
#43875=CARTESIAN_POINT('',(0.,-5.51551999045664,4.62807078974308));
#43876=CARTESIAN_POINT('',(0.,-5.94603225960321,4.05676171232808));
#43877=CARTESIAN_POINT('',(0.,-5.48078650262205,4.66531789528692));
#43878=CARTESIAN_POINT('',(0.,1.98458896188239,6.9210842107559));
#43879=CARTESIAN_POINT('',(0.,2.69716747259457,6.67572375288087));
#43880=CARTESIAN_POINT('',(0.,2.22059985717734,6.83981914246863));
#43881=CARTESIAN_POINT('',(0.,3.97082989020867,9.82814885840795));
#43882=CARTESIAN_POINT('',(0.,1.2832925189996,3.17626044286338));
#43883=CARTESIAN_POINT('',(0.,2.92175597166019,10.1893739769462));
#43884=CARTESIAN_POINT('',(0.,3.76642767818846,9.89853018422399));
#43885=CARTESIAN_POINT('',(0.,1.84067068326946,10.4389621819294));
#43886=CARTESIAN_POINT('',(0.,2.69268732848961,10.2422586402386));
#43887=CARTESIAN_POINT('',(0.,0.739418621687727,10.5741789327541));
#43888=CARTESIAN_POINT('',(0.,1.5880960033298,10.469974453101));
#43889=CARTESIAN_POINT('',(0.,-0.36993466504651,10.5935427664024));
#43890=CARTESIAN_POINT('',(0.,0.465360517618589,10.5789626347548));
#43891=CARTESIAN_POINT('',(0.,-1.4752348701767,10.4968415286606));
#43892=CARTESIAN_POINT('',(0.,-0.662580977805997,10.5679395316133));
#43893=CARTESIAN_POINT('',(0.,-2.56437209335648,10.2851346985256));
#43894=CARTESIAN_POINT('',(0.,-1.78272859909527,10.4370708025755));
#43895=CARTESIAN_POINT('',(0.,-1.74183764831761,6.98612922918717));
#43896=CARTESIAN_POINT('',(0.,-1.23806022724748,4.96558835401325));
#43897=CARTESIAN_POINT('',(0.,-1.00204632691247,7.12993009493931));
#43898=CARTESIAN_POINT('',(0.,-1.59209924108996,7.01523542707388));
#43899=CARTESIAN_POINT('',(0.,-0.251276376258007,7.19561395453749));
#43900=CARTESIAN_POINT('',(0.,-0.830675100725787,7.14492313448518));
#43901=CARTESIAN_POINT('',(0.,0.502246610957702,7.18246116187073));
#43902=CARTESIAN_POINT('',(0.,-0.0596154118396585,7.19226849995936));
#43903=CARTESIAN_POINT('',(0.,1.2502668792019,7.0906158216879));
#43904=CARTESIAN_POINT('',(0.,0.711990013474533,7.15670791029043));
#43905=CARTESIAN_POINT('',(0.,1.47505007879912,7.03872053100147));
#43906=CARTESIAN_POINT('',(0.,6.98612922918717,1.74183764831761));
#43907=CARTESIAN_POINT('',(0.,7.12993009493931,1.00204632691247));
#43908=CARTESIAN_POINT('',(0.,7.05728886874884,1.37575303883564));
#43909=CARTESIAN_POINT('',(0.,10.4968415286606,1.47523487017669));
#43910=CARTESIAN_POINT('',(0.,3.53905778246093,0.497382134807054));
#43911=CARTESIAN_POINT('',(0.,10.2851346985256,2.56437209335648));
#43912=CARTESIAN_POINT('',(0.,10.4791242442505,1.56638239684096));
#43913=CARTESIAN_POINT('',(0.,9.96074178033063,3.62541351925209));
#43914=CARTESIAN_POINT('',(0.,10.2565952330031,2.65772047889074));
#43915=CARTESIAN_POINT('',(0.,9.52721689077117,4.64673415596422));
#43916=CARTESIAN_POINT('',(0.,9.91997159267681,3.72146206229143));
#43917=CARTESIAN_POINT('',(0.,8.98930981925811,5.61714420087197));
#43918=CARTESIAN_POINT('',(0.,9.472448501687,4.74553894535134));
#43919=CARTESIAN_POINT('',(0.,8.35291398823125,6.52601163845198));
#43920=CARTESIAN_POINT('',(0.,8.91853294571702,5.71822405174313));
#43921=CARTESIAN_POINT('',(0.,7.6250018835897,7.36337872686537));
#43922=CARTESIAN_POINT('',(0.,8.2640116528114,6.62828207644714));
#43923=CARTESIAN_POINT('',(0.,5.17924656243829,5.00154026730478));
#43924=CARTESIAN_POINT('',(0.,3.71856779936528,3.59097918220609));
#43925=CARTESIAN_POINT('',(0.,5.6736774259684,4.43276262234474));
#43926=CARTESIAN_POINT('',(0.,5.39592996906135,4.75227452195658));
#43927=CARTESIAN_POINT('',(0.,6.10594629232627,3.81541870247908));
#43928=CARTESIAN_POINT('',(0.,5.87006672677349,4.15228963385447));
#43929=CARTESIAN_POINT('',(0.,6.471317133354,3.15627225688136));
#43930=CARTESIAN_POINT('',(0.,6.2769973813773,3.50683436923982));
#43931=CARTESIAN_POINT('',(0.,6.76578686965854,2.46254503194481));
#43932=CARTESIAN_POINT('',(0.,6.61254560216618,2.82355883450853));
#43933=CARTESIAN_POINT('',(0.,6.87343122356698,2.11045621509837));
#43934=CARTESIAN_POINT('',(0.,-1.9845889618824,-6.92108421075589));
#43935=CARTESIAN_POINT('',(0.,-2.69716747259457,-6.67572375288087));
#43936=CARTESIAN_POINT('',(0.,-2.10486732194354,-6.87966905010565));
#43937=CARTESIAN_POINT('',(0.,-3.97082989020867,-9.82814885840794));
#43938=CARTESIAN_POINT('',(0.,-1.41387495359497,-3.49946331001749));
#43939=CARTESIAN_POINT('',(0.,-2.9217559716602,-10.1893739769462));
#43940=CARTESIAN_POINT('',(0.,-3.65069514295465,-9.93838009186101));
#43941=CARTESIAN_POINT('',(0.,-1.84067068326946,-10.4389621819294));
#43942=CARTESIAN_POINT('',(0.,-2.61028197063542,-10.2612834161454));
#43943=CARTESIAN_POINT('',(0.,-0.739418621687731,-10.5741789327541));
#43944=CARTESIAN_POINT('',(0.,-1.54261933241824,-10.4755582861702));
#43945=CARTESIAN_POINT('',(0.,0.369934665046504,-10.5935427664024));
#43946=CARTESIAN_POINT('',(0.,-0.458800082389754,-10.5790771475776));
#43947=CARTESIAN_POINT('',(0.,1.47523487017669,-10.4968415286606));
#43948=CARTESIAN_POINT('',(0.,0.629938454852123,-10.5707953823206));
#43949=CARTESIAN_POINT('',(0.,2.56437209335647,-10.2851346985256));
#43950=CARTESIAN_POINT('',(0.,1.712309752848,-10.4507588396782));
#43951=CARTESIAN_POINT('',(0.,1.74183764831761,-6.98612922918718));
#43952=CARTESIAN_POINT('',(0.,1.326311866109,-5.31954634451231));
#43953=CARTESIAN_POINT('',(0.,1.00204632691247,-7.12993009493931));
#43954=CARTESIAN_POINT('',(0.,1.52168039484269,-7.02892346417654));
#43955=CARTESIAN_POINT('',(0.,0.251276376258003,-7.19561395453749));
#43956=CARTESIAN_POINT('',(0.,0.798032577771921,-7.14777898519253));
#43957=CARTESIAN_POINT('',(0.,-0.502246610957704,-7.18246116187073));
#43958=CARTESIAN_POINT('',(0.,0.0661758470684938,-7.19238301278224));
#43959=CARTESIAN_POINT('',(0.,-1.2502668792019,-7.0906158216879));
#43960=CARTESIAN_POINT('',(0.,-0.666513342562969,-7.16229174335963));
#43961=CARTESIAN_POINT('',(0.,-1.39264472094493,-7.05774530690832));
#43962=CARTESIAN_POINT('',(0.,11.6913429510899,-3.90000000000001));
#43963=CARTESIAN_POINT('Origin',(0.,11.6913429510899,-6.75000000000001));
#43964=CARTESIAN_POINT('Origin',(0.1,0.,0.));
#43965=CARTESIAN_POINT('',(0.0089490830417863,5.,16.0480768092719));
#43966=CARTESIAN_POINT('Ctrl Pts',(5.20417042793042E-17,5.,16.0387031894726));
#43967=CARTESIAN_POINT('Ctrl Pts',(0.00447323435791146,5.,16.0433887514115));
#43968=CARTESIAN_POINT('Ctrl Pts',(0.0089490830417863,5.,16.0480768092719));
#43969=CARTESIAN_POINT('',(0.2,5.19080451686515,16.1881298631958));
#43970=CARTESIAN_POINT('Ctrl Pts',(0.00894908304178668,5.,16.0480768092719));
#43971=CARTESIAN_POINT('Ctrl Pts',(0.07251246250349,5.06367493004374,16.0948150550825));
#43972=CARTESIAN_POINT('Ctrl Pts',(0.136203613263926,5.12728130687429,16.1415029819226));
#43973=CARTESIAN_POINT('Ctrl Pts',(0.2,5.19080451686515,16.1881298631958));
#43974=CARTESIAN_POINT('',(0.2,-5.19080451686515,16.1881298631958));
#43975=CARTESIAN_POINT('Origin',(0.2,0.,0.));
#43976=CARTESIAN_POINT('',(0.0089490830417863,-5.,16.0480768092719));
#43977=CARTESIAN_POINT('Ctrl Pts',(0.2,-5.19080451686515,16.1881298631958));
#43978=CARTESIAN_POINT('Ctrl Pts',(0.136203613263926,-5.12728130687429,
16.1415029819226));
#43979=CARTESIAN_POINT('Ctrl Pts',(0.07251246250349,-5.06367493004374,16.0948150550825));
#43980=CARTESIAN_POINT('Ctrl Pts',(0.00894908304178668,-5.,16.0480768092719));
#43981=CARTESIAN_POINT('Ctrl Pts',(0.0089490830417863,-5.,16.0480768092719));
#43982=CARTESIAN_POINT('Ctrl Pts',(0.00447323435791139,-5.,16.0433887514115));
#43983=CARTESIAN_POINT('Ctrl Pts',(5.20417042793042E-17,-5.,16.0387031894726));
#43984=CARTESIAN_POINT('Origin',(0.,5.09540225843257,16.1181033362339));
#43985=CARTESIAN_POINT('',(3.8,5.19080451686515,16.1881298631958));
#43986=CARTESIAN_POINT('',(0.,5.19080451686515,16.1881298631958));
#43987=CARTESIAN_POINT('',(3.99105091695821,5.,16.0480768092719));
#43988=CARTESIAN_POINT('',(0.,5.,16.0480768092719));
#43989=CARTESIAN_POINT('Ctrl Pts',(3.99105091695821,5.,16.0480768092719));
#43990=CARTESIAN_POINT('Ctrl Pts',(3.92748753749667,5.06367493004358,16.0948150550824));
#43991=CARTESIAN_POINT('Ctrl Pts',(3.8637963867364,5.12728130687397,16.1415029819224));
#43992=CARTESIAN_POINT('Ctrl Pts',(3.8,5.19080451686515,16.1881298631958));
#43993=CARTESIAN_POINT('Origin',(3.9,0.,0.));
#43994=CARTESIAN_POINT('',(3.8,-5.19080451686515,16.1881298631958));
#43995=CARTESIAN_POINT('Origin',(3.8,0.,0.));
#43996=CARTESIAN_POINT('',(4.,5.,16.0387031894726));
#43997=CARTESIAN_POINT('Ctrl Pts',(3.99105091695821,5.,16.0480768092719));
#43998=CARTESIAN_POINT('Ctrl Pts',(3.99552676564209,5.,16.0433887514115));
#43999=CARTESIAN_POINT('Ctrl Pts',(4.,5.,16.0387031894726));
#44000=CARTESIAN_POINT('',(4.,-5.,16.0387031894726));
#44001=CARTESIAN_POINT('Origin',(4.,0.,0.));
#44002=CARTESIAN_POINT('',(3.99105091695821,-5.,16.0480768092719));
#44003=CARTESIAN_POINT('Ctrl Pts',(4.,-5.,16.0387031894726));
#44004=CARTESIAN_POINT('Ctrl Pts',(3.99552676564209,-5.,16.0433887514115));
#44005=CARTESIAN_POINT('Ctrl Pts',(3.99105091695821,-5.,16.0480768092719));
#44006=CARTESIAN_POINT('Ctrl Pts',(3.8,-5.19080451686515,16.1881298631958));
#44007=CARTESIAN_POINT('Ctrl Pts',(3.8637963867364,-5.12728130687397,16.1415029819224));
#44008=CARTESIAN_POINT('Ctrl Pts',(3.92748753749667,-5.06367493004358,16.0948150550824));
#44009=CARTESIAN_POINT('Ctrl Pts',(3.99105091695821,-5.,16.0480768092719));
#44010=CARTESIAN_POINT('Origin',(0.,-5.09540225843257,16.1181033362339));
#44011=CARTESIAN_POINT('',(0.,-5.,16.0480768092719));
#44012=CARTESIAN_POINT('',(0.,-5.19080451686515,16.1881298631958));
#44013=CARTESIAN_POINT('Origin',(0.,-5.,15.));
#44014=CARTESIAN_POINT('',(4.,-5.,15.));
#44015=CARTESIAN_POINT('Origin',(4.,0.,-0.375961595364038));
#44016=CARTESIAN_POINT('',(4.,5.,21.));
#44017=CARTESIAN_POINT('',(4.,-2.82893410603039E-15,-10.65));
#44018=CARTESIAN_POINT('Origin',(4.,-2.47990976827339E-15,-13.5));
#44019=CARTESIAN_POINT('',(4.,-11.6913429510899,-3.9));
#44020=CARTESIAN_POINT('Origin',(4.,-11.6913429510899,-6.75));
#44021=CARTESIAN_POINT('',(4.,-7.16418377501202E-16,5.85));
#44022=CARTESIAN_POINT('Origin',(4.,0.,0.));
#44023=CARTESIAN_POINT('',(4.,7.36337872686537,-7.6250018835897));
#44024=CARTESIAN_POINT('',(4.,6.52601163845198,-8.35291398823125));
#44025=CARTESIAN_POINT('',(4.,7.06096126402149,-7.88788937332392));
#44026=CARTESIAN_POINT('',(4.,4.43276262234474,-5.6736774259684));
#44027=CARTESIAN_POINT('',(4.,3.3542043015324,-4.29318572841242));
#44028=CARTESIAN_POINT('',(4.,5.00154026730478,-5.17924656243829));
#44029=CARTESIAN_POINT('',(4.,4.48188134284422,-5.6309791736597));
#44030=CARTESIAN_POINT('',(4.,5.51551999045664,-4.62807078974308));
#44031=CARTESIAN_POINT('',(4.,5.03627375513937,-5.14199945689445));
#44032=CARTESIAN_POINT('',(4.,5.9690705223963,-4.02618890498938));
#44033=CARTESIAN_POINT('',(4.,5.53855825324973,-4.59749798240438));
#44034=CARTESIAN_POINT('',(4.,6.35722266858427,-3.38019525205841));
#44035=CARTESIAN_POINT('',(4.,5.98311996253477,-4.00280671002841));
#44036=CARTESIAN_POINT('',(4.,6.67572375288087,-2.69716747259456));
#44037=CARTESIAN_POINT('',(4.,6.36484711691973,-3.36384456983795));
#44038=CARTESIAN_POINT('',(4.,6.9210842107559,-1.98458896188239));
#44039=CARTESIAN_POINT('',(4.,6.67919759973273,-2.68707868878003));
#44040=CARTESIAN_POINT('',(4.,10.1893739769462,-2.92175597166019));
#44041=CARTESIAN_POINT('',(4.,3.51034942837676,-1.00657650098811));
#44042=CARTESIAN_POINT('',(4.,9.82814885840795,-3.97082989020866));
#44043=CARTESIAN_POINT('',(4.,10.0412014296947,-3.35208029516082));
#44044=CARTESIAN_POINT('',(4.,9.35924448430463,-4.97639856553044));
#44045=CARTESIAN_POINT('',(4.,9.63892194214343,-4.37662832168461));
#44046=CARTESIAN_POINT('',(4.,8.78779826908344,-5.92744477678991));
#44047=CARTESIAN_POINT('',(4.,9.13339433409081,-5.35227633661707));
#44048=CARTESIAN_POINT('',(4.,8.12007109706117,-6.81354866267731));
#44049=CARTESIAN_POINT('',(4.,8.53051710588605,-6.2688684121115));
#44050=CARTESIAN_POINT('',(4.,7.83713656155884,-7.11695880553538));
#44051=CARTESIAN_POINT('',(4.,-10.2851346985256,-2.56437209335648));
#44052=CARTESIAN_POINT('',(4.,-10.4968415286606,-1.47523487017669));
#44053=CARTESIAN_POINT('',(4.,-10.3028519829357,-2.47322456669221));
#44054=CARTESIAN_POINT('',(4.,-7.12993009493931,-1.00204632691247));
#44055=CARTESIAN_POINT('',(4.,-5.27432802933904,-0.741258463737529));
#44056=CARTESIAN_POINT('',(4.,-6.98612922918717,-1.74183764831761));
#44057=CARTESIAN_POINT('',(4.,-7.05877045537764,-1.36813093639444));
#44058=CARTESIAN_POINT('',(4.,-6.76578686965854,-2.46254503194481));
#44059=CARTESIAN_POINT('',(4.,-6.87848487527874,-2.09392646516405));
#44060=CARTESIAN_POINT('',(4.,-6.471317133354,-3.15627225688136));
#44061=CARTESIAN_POINT('',(4.,-6.62455840084636,-2.79525845431765));
#44062=CARTESIAN_POINT('',(4.,-6.10594629232627,-3.81541870247908));
#44063=CARTESIAN_POINT('',(4.,-6.30026604430297,-3.46485659012061));
#44064=CARTESIAN_POINT('',(4.,-5.6736774259684,-4.43276262234474));
#44065=CARTESIAN_POINT('',(4.,-5.90955699152118,-4.09589169096934));
#44066=CARTESIAN_POINT('',(4.,-5.17924656243829,-5.00154026730478));
#44067=CARTESIAN_POINT('',(4.,-5.45699401934533,-4.68202836769294));
#44068=CARTESIAN_POINT('',(4.,-7.6250018835897,-7.36337872686537));
#44069=CARTESIAN_POINT('',(4.,-2.68355642364871,-2.59148031487898));
#44070=CARTESIAN_POINT('',(4.,-8.35291398823125,-6.52601163845198));
#44071=CARTESIAN_POINT('',(4.,-7.71390421900955,-7.26110828887021));
#44072=CARTESIAN_POINT('',(4.,-8.98930981925811,-5.61714420087197));
#44073=CARTESIAN_POINT('',(4.,-8.42369086177234,-6.42493178758083));
#44074=CARTESIAN_POINT('',(4.,-9.52721689077117,-4.64673415596422));
#44075=CARTESIAN_POINT('',(4.,-9.04407820834228,-5.51833941148486));
#44076=CARTESIAN_POINT('',(4.,-9.96074178033063,-3.62541351925209));
#44077=CARTESIAN_POINT('',(4.,-9.56798707842499,-4.55068561292488));
#44078=CARTESIAN_POINT('',(4.,-9.98928124585308,-3.53206513371783));
#44079=CARTESIAN_POINT('',(4.,-7.36337872686537,7.6250018835897));
#44080=CARTESIAN_POINT('',(4.,-6.52601163845198,8.35291398823125));
#44081=CARTESIAN_POINT('',(4.,-7.24711264550256,7.72607044617626));
#44082=CARTESIAN_POINT('',(4.,-4.43276262234474,5.6736774259684));
#44083=CARTESIAN_POINT('',(4.,-3.17180733691958,4.05972825981883));
#44084=CARTESIAN_POINT('',(4.,-5.00154026730478,5.17924656243829));
#44085=CARTESIAN_POINT('',(4.,-4.66803272432529,5.46916024651204));
#44086=CARTESIAN_POINT('',(4.,-5.51551999045664,4.62807078974308));
#44087=CARTESIAN_POINT('',(4.,-5.22379664104612,4.94090578163452));
#44088=CARTESIAN_POINT('',(4.,-5.9690705223963,4.02618890498938));
#44089=CARTESIAN_POINT('',(4.,-5.71925699363338,4.35770265470493));
#44090=CARTESIAN_POINT('',(4.,-6.35722266858427,3.38019525205841));
#44091=CARTESIAN_POINT('',(4.,-6.14909715535181,3.72657427348487));
#44092=CARTESIAN_POINT('',(4.,-6.67572375288087,2.69716747259457));
#44093=CARTESIAN_POINT('',(4.,-6.50884876239711,3.05503204454694));
#44094=CARTESIAN_POINT('',(4.,-6.9210842107559,1.98458896188239));
#44095=CARTESIAN_POINT('',(4.,-6.79493013496653,2.35096700105301));
#44096=CARTESIAN_POINT('',(4.,-10.1893739769462,2.92175597166019));
#44097=CARTESIAN_POINT('',(4.,-3.41073478237913,0.97801246089429));
#44098=CARTESIAN_POINT('',(4.,-9.82814885840794,3.97082989020867));
#44099=CARTESIAN_POINT('',(4.,-10.1569339649285,3.01596860743381));
#44100=CARTESIAN_POINT('',(4.,-9.35924448430463,4.97639856553044));
#44101=CARTESIAN_POINT('',(4.,-9.78292358762081,4.06781579639361));
#44102=CARTESIAN_POINT('',(4.,-8.78779826908344,5.92744477678992));
#44103=CARTESIAN_POINT('',(4.,-9.29937152690785,5.07604390007354));
#44104=CARTESIAN_POINT('',(4.,-8.12007109706117,6.81354866267732));
#44105=CARTESIAN_POINT('',(4.,-8.7112158462697,6.02907308441204));
#44106=CARTESIAN_POINT('',(4.,-8.02465944746559,6.91586513027545));
#44107=CARTESIAN_POINT('',(4.,2.92175597166019,10.1893739769462));
#44108=CARTESIAN_POINT('',(4.,3.97082989020867,9.82814885840795));
#44109=CARTESIAN_POINT('',(4.,3.24189071891422,10.0791427434931));
#44110=CARTESIAN_POINT('',(4.,2.69716747259457,6.67572375288087));
#44111=CARTESIAN_POINT('',(4.,1.92012372780665,4.75247299562692));
#44112=CARTESIAN_POINT('',(4.,1.98458896188239,6.9210842107559));
#44113=CARTESIAN_POINT('',(4.,2.57688911253343,6.71713891353112));
#44114=CARTESIAN_POINT('',(4.,1.2502668792019,7.0906158216879));
#44115=CARTESIAN_POINT('',(4.,1.84221112013937,6.95395472553547));
#44116=CARTESIAN_POINT('',(4.,0.502246610957702,7.18246116187073));
#44117=CARTESIAN_POINT('',(4.,1.08600014759663,7.11078524019901));
#44118=CARTESIAN_POINT('',(4.,-0.251276376258007,7.19561395453749));
#44119=CARTESIAN_POINT('',(4.,0.317146081768196,7.18569210362599));
#44120=CARTESIAN_POINT('',(4.,-1.00204632691247,7.12993009493931));
#44121=CARTESIAN_POINT('',(4.,-0.455290125398554,7.17776506428427));
#44122=CARTESIAN_POINT('',(4.,-1.74183764831761,6.98612922918717));
#44123=CARTESIAN_POINT('',(4.,-1.22220358038739,7.08713585994994));
#44124=CARTESIAN_POINT('',(4.,-2.56437209335648,10.2851346985256));
#44125=CARTESIAN_POINT('',(4.,-0.826793004728047,3.31608561934406));
#44126=CARTESIAN_POINT('',(4.,-1.4752348701767,10.4968415286606));
#44127=CARTESIAN_POINT('',(4.,-2.32729721068516,10.331217387508));
#44128=CARTESIAN_POINT('',(4.,-0.36993466504651,10.5935427664024));
#44129=CARTESIAN_POINT('',(4.,-1.21523108037109,10.5195889127424));
#44130=CARTESIAN_POINT('',(4.,0.739418621687727,10.5741789327541));
#44131=CARTESIAN_POINT('',(4.,-0.0893161257485295,10.5886445515789));
#44132=CARTESIAN_POINT('',(4.,1.84067068326946,10.4389621819294));
#44133=CARTESIAN_POINT('',(4.,1.03746997253894,10.5375828285134));
#44134=CARTESIAN_POINT('',(4.,2.15214468429424,10.3670527427302));
#44135=CARTESIAN_POINT('',(4.,10.2851346985256,2.56437209335648));
#44136=CARTESIAN_POINT('',(4.,10.4968415286606,1.47523487017669));
#44137=CARTESIAN_POINT('',(4.,10.373270829183,2.11095100843085));
#44138=CARTESIAN_POINT('',(4.,7.12993009493931,1.00204632691247));
#44139=CARTESIAN_POINT('',(4.,5.2225134993216,0.733976406439165));
#44140=CARTESIAN_POINT('',(4.,6.98612922918717,1.74183764831761));
#44141=CARTESIAN_POINT('',(4.,7.12918930162491,1.00585737813307));
#44142=CARTESIAN_POINT('',(4.,6.76578686965854,2.46254503194481));
#44143=CARTESIAN_POINT('',(4.,6.98360240333129,1.75010252328477));
#44144=CARTESIAN_POINT('',(4.,6.471317133354,3.15627225688136));
#44145=CARTESIAN_POINT('',(4.,6.75978047031845,2.47669522204026));
#44146=CARTESIAN_POINT('',(4.,6.10594629232627,3.81541870247908));
#44147=CARTESIAN_POINT('',(4.,6.45968280189117,3.17726114644097));
#44148=CARTESIAN_POINT('',(4.,5.6736774259684,4.43276262234474));
#44149=CARTESIAN_POINT('',(4.,6.08620115995242,3.84361767392164));
#44150=CARTESIAN_POINT('',(4.,5.17924656243829,5.00154026730478));
#44151=CARTESIAN_POINT('',(4.,5.64314540082641,4.46788569947656));
#44152=CARTESIAN_POINT('',(4.,7.6250018835897,7.36337872686537));
#44153=CARTESIAN_POINT('',(4.,2.49569013878957,2.4100599524258));
#44154=CARTESIAN_POINT('',(4.,8.35291398823125,6.52601163845198));
#44155=CARTESIAN_POINT('',(4.,7.90005560049063,7.04696562065383));
#44156=CARTESIAN_POINT('',(4.,8.98930981925811,5.61714420087197));
#44157=CARTESIAN_POINT('',(4.,8.60033503020359,6.17265777053313));
#44158=CARTESIAN_POINT('',(4.,9.52721689077117,4.64673415596422));
#44159=CARTESIAN_POINT('',(4.,9.20349496593048,5.23074396780521));
#44160=CARTESIAN_POINT('',(4.,9.96074178033063,3.62541351925209));
#44161=CARTESIAN_POINT('',(4.,9.70320914789708,4.23212238064749));
#44162=CARTESIAN_POINT('',(4.,10.0943987739056,3.18824119183854));
#44163=CARTESIAN_POINT('',(4.,-2.9217559716602,-10.1893739769462));
#44164=CARTESIAN_POINT('',(4.,-3.97082989020867,-9.82814885840794));
#44165=CARTESIAN_POINT('',(4.,-3.12615818368041,-10.1189926511301));
#44166=CARTESIAN_POINT('',(4.,-2.69716747259457,-6.67572375288087));
#44167=CARTESIAN_POINT('',(4.,-2.05070616240202,-5.07567586278102));
#44168=CARTESIAN_POINT('',(4.,-1.9845889618824,-6.92108421075589));
#44169=CARTESIAN_POINT('',(4.,-2.46115657729962,-6.75698882116814));
#44170=CARTESIAN_POINT('',(4.,-1.2502668792019,-7.0906158216879));
#44171=CARTESIAN_POINT('',(4.,-1.75980576228518,-6.97297950144232));
#44172=CARTESIAN_POINT('',(4.,-0.502246610957704,-7.18246116187073));
#44173=CARTESIAN_POINT('',(4.,-1.04052347668507,-7.11636907326821));
#44174=CARTESIAN_POINT('',(4.,0.251276376258003,-7.19561395453749));
#44175=CARTESIAN_POINT('',(4.,-0.31058564653936,-7.18580661644886));
#44176=CARTESIAN_POINT('',(4.,1.00204632691247,-7.12993009493931));
#44177=CARTESIAN_POINT('',(4.,0.422647602444687,-7.18062091499162));
#44178=CARTESIAN_POINT('',(4.,1.74183764831761,-6.98612922918718));
#44179=CARTESIAN_POINT('',(4.,1.15178473414012,-7.10082389705261));
#44180=CARTESIAN_POINT('',(4.,2.56437209335647,-10.2851346985256));
#44181=CARTESIAN_POINT('',(4.,0.915044643589561,-3.67004360984312));
#44182=CARTESIAN_POINT('',(4.,1.47523487017669,-10.4968415286606));
#44183=CARTESIAN_POINT('',(4.,2.25687836443789,-10.3449054246107));
#44184=CARTESIAN_POINT('',(4.,0.369934665046504,-10.5935427664024));
#44185=CARTESIAN_POINT('',(4.,1.18258855741722,-10.5224447634498));
#44186=CARTESIAN_POINT('',(4.,-0.739418621687731,-10.5741789327541));
#44187=CARTESIAN_POINT('',(4.,0.0958765609773636,-10.5887590644018));
#44188=CARTESIAN_POINT('',(4.,-1.84067068326946,-10.4389621819294));
#44189=CARTESIAN_POINT('',(4.,-0.991993301627379,-10.5431666615826));
#44190=CARTESIAN_POINT('',(4.,-2.06973932644006,-10.386077518637));
#44191=CARTESIAN_POINT('',(4.,11.6913429510899,-3.90000000000001));
#44192=CARTESIAN_POINT('Origin',(4.,11.6913429510899,-6.75000000000001));
#44193=CARTESIAN_POINT('Origin',(0.,0.,0.));
#44194=CARTESIAN_POINT('Origin',(0.1,-2.47990976827339E-15,-13.5));
#44195=CARTESIAN_POINT('',(0.2,-2.80444117004744E-15,-10.85));
#44196=CARTESIAN_POINT('',(0.1,-2.14313189850787E-15,-10.75));
#44197=CARTESIAN_POINT('Origin',(0.2,-2.47990976827339E-15,-13.5));
#44198=CARTESIAN_POINT('Origin',(0.,-2.47990976827339E-15,-13.5));
#44199=CARTESIAN_POINT('',(3.8,-2.15537836649934E-15,-10.85));
#44200=CARTESIAN_POINT('',(0.,-2.80444117004744E-15,-10.85));
#44201=CARTESIAN_POINT('Origin',(3.8,-2.47990976827339E-15,-13.5));
#44202=CARTESIAN_POINT('Origin',(3.9,-2.47990976827339E-15,-13.5));
#44203=CARTESIAN_POINT('',(3.9,-2.81668763803891E-15,-10.75));
#44204=CARTESIAN_POINT('Origin',(0.1,11.6913429510899,-6.75000000000001));
#44205=CARTESIAN_POINT('',(0.2,11.6913429510899,-4.10000000000001));
#44206=CARTESIAN_POINT('',(0.1,11.6913429510899,-4.00000000000001));
#44207=CARTESIAN_POINT('Origin',(0.2,11.6913429510899,-6.75000000000001));
#44208=CARTESIAN_POINT('Origin',(0.,11.6913429510899,-6.75000000000001));
#44209=CARTESIAN_POINT('',(3.8,11.6913429510899,-4.10000000000001));
#44210=CARTESIAN_POINT('',(0.,11.6913429510899,-4.10000000000001));
#44211=CARTESIAN_POINT('Origin',(3.8,11.6913429510899,-6.75000000000001));
#44212=CARTESIAN_POINT('Origin',(3.9,11.6913429510899,-6.75000000000001));
#44213=CARTESIAN_POINT('',(3.9,11.6913429510899,-4.00000000000001));
#44214=CARTESIAN_POINT('Origin',(0.1,-11.6913429510899,-6.75));
#44215=CARTESIAN_POINT('',(0.2,-11.6913429510899,-4.1));
#44216=CARTESIAN_POINT('',(0.1,-11.6913429510899,-4.));
#44217=CARTESIAN_POINT('Origin',(0.2,-11.6913429510899,-6.75));
#44218=CARTESIAN_POINT('Origin',(0.,-11.6913429510899,-6.75));
#44219=CARTESIAN_POINT('',(3.8,-11.6913429510899,-4.1));
#44220=CARTESIAN_POINT('',(0.,-11.6913429510899,-4.1));
#44221=CARTESIAN_POINT('Origin',(3.8,-11.6913429510899,-6.75));
#44222=CARTESIAN_POINT('Origin',(3.9,-11.6913429510899,-6.75));
#44223=CARTESIAN_POINT('',(3.9,-11.6913429510899,-4.));
#44224=CARTESIAN_POINT('Origin',(2.,0.,14.9));
#44225=CARTESIAN_POINT('',(1.,1.22464679914735E-16,14.8));
#44226=CARTESIAN_POINT('',(0.9,-1.34711147906209E-16,14.9));
#44227=CARTESIAN_POINT('Origin',(2.,0.,14.8));
#44228=CARTESIAN_POINT('Origin',(2.,0.,21.));
#44229=CARTESIAN_POINT('',(1.,1.47968513756208E-16,5.85));
#44230=CARTESIAN_POINT('',(1.,1.22464679914735E-16,21.));
#44231=CARTESIAN_POINT('',(2.,1.,5.76389625166866));
#44232=CARTESIAN_POINT('Ctrl Pts',(2.,1.,5.76389625166866));
#44233=CARTESIAN_POINT('Ctrl Pts',(1.87416996601027,1.,5.76389625166866));
#44234=CARTESIAN_POINT('Ctrl Pts',(1.74012546214185,0.974802142157817,5.76844303881019));
#44235=CARTESIAN_POINT('Ctrl Pts',(1.49382158240198,0.872672585527757,5.78477457060768));
#44236=CARTESIAN_POINT('Ctrl Pts',(1.38154050485319,0.795754067226289,5.79631351124354));
#44237=CARTESIAN_POINT('Ctrl Pts',(1.20424855638596,0.61846211875906,5.81790159694625));
#44238=CARTESIAN_POINT('Ctrl Pts',(1.127327980397,0.506179916337122,5.82936652378142));
#44239=CARTESIAN_POINT('Ctrl Pts',(1.02519693018325,0.259872166731316,5.84552808842072));
#44240=CARTESIAN_POINT('Ctrl Pts',(1.,0.125826309913858,5.85));
#44241=CARTESIAN_POINT('Ctrl Pts',(1.,1.04083408558608E-16,5.85));
#44242=CARTESIAN_POINT('',(3.,-4.44945362549441E-16,5.85));
#44243=CARTESIAN_POINT('Ctrl Pts',(3.,-1.73472347597681E-16,5.85));
#44244=CARTESIAN_POINT('Ctrl Pts',(3.,0.125826309913858,5.85));
#44245=CARTESIAN_POINT('Ctrl Pts',(2.97480306981675,0.259872166731315,5.84552808842072));
#44246=CARTESIAN_POINT('Ctrl Pts',(2.872672019603,0.50617991633712,5.82936652378142));
#44247=CARTESIAN_POINT('Ctrl Pts',(2.79575144361404,0.61846211875906,5.81790159694625));
#44248=CARTESIAN_POINT('Ctrl Pts',(2.61845949514681,0.795754067226288,5.79631351124354));
#44249=CARTESIAN_POINT('Ctrl Pts',(2.50617841759802,0.872672585527758,5.78477457060768));
#44250=CARTESIAN_POINT('Ctrl Pts',(2.25987453785815,0.974802142157818,5.76844303881019));
#44251=CARTESIAN_POINT('Ctrl Pts',(2.12583003398973,1.,5.76389625166866));
#44252=CARTESIAN_POINT('Ctrl Pts',(2.,1.,5.76389625166866));
#44253=CARTESIAN_POINT('Ctrl Pts',(1.,1.73472347597681E-16,5.85));
#44254=CARTESIAN_POINT('Ctrl Pts',(1.,-0.125826309913858,5.85));
#44255=CARTESIAN_POINT('Ctrl Pts',(1.02519693018325,-0.259872166731316,
5.84552808842072));
#44256=CARTESIAN_POINT('Ctrl Pts',(1.127327980397,-0.506179916337121,5.82936652378142));
#44257=CARTESIAN_POINT('Ctrl Pts',(1.20424855638596,-0.61846211875906,5.81790159694625));
#44258=CARTESIAN_POINT('Ctrl Pts',(1.38154050485319,-0.795754067226289,
5.79631351124354));
#44259=CARTESIAN_POINT('Ctrl Pts',(1.49382158240198,-0.872672585527757,
5.78477457060768));
#44260=CARTESIAN_POINT('Ctrl Pts',(1.74012546214185,-0.974802142157818,
5.76844303881019));
#44261=CARTESIAN_POINT('Ctrl Pts',(1.87416996601027,-1.,5.76389625166866));
#44262=CARTESIAN_POINT('Ctrl Pts',(2.12583003398973,-1.,5.76389625166866));
#44263=CARTESIAN_POINT('Ctrl Pts',(2.25987453785815,-0.974802142157817,
5.76844303881019));
#44264=CARTESIAN_POINT('Ctrl Pts',(2.50617841759802,-0.872672585527757,
5.78477457060768));
#44265=CARTESIAN_POINT('Ctrl Pts',(2.61845949514681,-0.795754067226289,
5.79631351124354));
#44266=CARTESIAN_POINT('Ctrl Pts',(2.79575144361404,-0.61846211875906,5.81790159694625));
#44267=CARTESIAN_POINT('Ctrl Pts',(2.872672019603,-0.506179916337122,5.82936652378142));
#44268=CARTESIAN_POINT('Ctrl Pts',(2.97480306981675,-0.259872166731316,
5.84552808842072));
#44269=CARTESIAN_POINT('Ctrl Pts',(3.,-0.125826309913858,5.85));
#44270=CARTESIAN_POINT('Ctrl Pts',(3.,-2.77555756156289E-16,5.85));
#44271=CARTESIAN_POINT('Origin',(4.,-2.9217559716602,-10.1893739769462));
#44272=CARTESIAN_POINT('',(3.85,-2.9217559716602,-10.1893739769462));
#44273=CARTESIAN_POINT('',(4.,-2.9217559716602,-10.1893739769462));
#44274=CARTESIAN_POINT('',(3.85,-3.97082989020867,-9.82814885840794));
#44275=CARTESIAN_POINT('',(3.85,-3.97082989020867,-9.82814885840794));
#44276=CARTESIAN_POINT('',(4.,-3.97082989020867,-9.82814885840794));
#44277=CARTESIAN_POINT('Origin',(4.,-1.84067068326946,-10.4389621819294));
#44278=CARTESIAN_POINT('',(3.85,-1.84067068326946,-10.4389621819294));
#44279=CARTESIAN_POINT('',(4.,-1.84067068326946,-10.4389621819294));
#44280=CARTESIAN_POINT('',(3.85,-2.9217559716602,-10.1893739769462));
#44281=CARTESIAN_POINT('Origin',(4.,-0.739418621687731,-10.5741789327541));
#44282=CARTESIAN_POINT('',(3.85,-0.739418621687731,-10.5741789327541));
#44283=CARTESIAN_POINT('',(4.,-0.739418621687731,-10.5741789327541));
#44284=CARTESIAN_POINT('',(3.85,-1.84067068326946,-10.4389621819294));
#44285=CARTESIAN_POINT('Origin',(4.,0.369934665046504,-10.5935427664024));
#44286=CARTESIAN_POINT('',(3.85,0.369934665046504,-10.5935427664024));
#44287=CARTESIAN_POINT('',(4.,0.369934665046504,-10.5935427664024));
#44288=CARTESIAN_POINT('',(3.85,-0.739418621687731,-10.5741789327541));
#44289=CARTESIAN_POINT('Origin',(4.,1.47523487017669,-10.4968415286606));
#44290=CARTESIAN_POINT('',(3.85,1.47523487017669,-10.4968415286606));
#44291=CARTESIAN_POINT('',(4.,1.47523487017669,-10.4968415286606));
#44292=CARTESIAN_POINT('',(3.85,0.369934665046504,-10.5935427664024));
#44293=CARTESIAN_POINT('Origin',(4.,2.56437209335647,-10.2851346985256));
#44294=CARTESIAN_POINT('',(3.85,2.56437209335647,-10.2851346985256));
#44295=CARTESIAN_POINT('',(4.,2.56437209335647,-10.2851346985256));
#44296=CARTESIAN_POINT('',(3.85,1.47523487017669,-10.4968415286606));
#44297=CARTESIAN_POINT('Origin',(4.,1.74183764831761,-6.98612922918718));
#44298=CARTESIAN_POINT('',(3.85,1.74183764831761,-6.98612922918718));
#44299=CARTESIAN_POINT('',(4.,1.74183764831761,-6.98612922918718));
#44300=CARTESIAN_POINT('',(3.85,2.56437209335647,-10.2851346985256));
#44301=CARTESIAN_POINT('Origin',(4.,1.00204632691247,-7.12993009493931));
#44302=CARTESIAN_POINT('',(3.85,1.00204632691247,-7.12993009493931));
#44303=CARTESIAN_POINT('',(4.,1.00204632691247,-7.12993009493931));
#44304=CARTESIAN_POINT('',(3.85,1.74183764831761,-6.98612922918718));
#44305=CARTESIAN_POINT('Origin',(4.,0.251276376258003,-7.19561395453749));
#44306=CARTESIAN_POINT('',(3.85,0.251276376258003,-7.19561395453749));
#44307=CARTESIAN_POINT('',(4.,0.251276376258003,-7.19561395453749));
#44308=CARTESIAN_POINT('',(3.85,1.00204632691247,-7.12993009493931));
#44309=CARTESIAN_POINT('Origin',(4.,-0.502246610957704,-7.18246116187073));
#44310=CARTESIAN_POINT('',(3.85,-0.502246610957704,-7.18246116187073));
#44311=CARTESIAN_POINT('',(4.,-0.502246610957704,-7.18246116187073));
#44312=CARTESIAN_POINT('',(3.85,0.251276376258003,-7.19561395453749));
#44313=CARTESIAN_POINT('Origin',(4.,-1.2502668792019,-7.0906158216879));
#44314=CARTESIAN_POINT('',(3.85,-1.2502668792019,-7.0906158216879));
#44315=CARTESIAN_POINT('',(4.,-1.2502668792019,-7.0906158216879));
#44316=CARTESIAN_POINT('',(3.85,-0.502246610957704,-7.18246116187073));
#44317=CARTESIAN_POINT('Origin',(4.,-1.9845889618824,-6.92108421075589));
#44318=CARTESIAN_POINT('',(3.85,-1.9845889618824,-6.92108421075589));
#44319=CARTESIAN_POINT('',(4.,-1.9845889618824,-6.92108421075589));
#44320=CARTESIAN_POINT('',(3.85,-1.2502668792019,-7.0906158216879));
#44321=CARTESIAN_POINT('Origin',(4.,-2.69716747259457,-6.67572375288087));
#44322=CARTESIAN_POINT('',(3.85,-2.69716747259457,-6.67572375288087));
#44323=CARTESIAN_POINT('',(4.,-2.69716747259457,-6.67572375288087));
#44324=CARTESIAN_POINT('',(3.85,-1.9845889618824,-6.92108421075589));
#44325=CARTESIAN_POINT('Origin',(4.,-3.97082989020867,-9.82814885840794));
#44326=CARTESIAN_POINT('',(3.85,-2.69716747259457,-6.67572375288087));
#44327=CARTESIAN_POINT('Origin',(3.85,-0.703228898426098,-8.63463325964164));
#44328=CARTESIAN_POINT('Origin',(4.,10.2851346985256,2.56437209335648));
#44329=CARTESIAN_POINT('',(3.85,10.2851346985256,2.56437209335648));
#44330=CARTESIAN_POINT('',(4.,10.2851346985256,2.56437209335648));
#44331=CARTESIAN_POINT('',(3.85,10.4968415286606,1.47523487017669));
#44332=CARTESIAN_POINT('',(3.85,10.4968415286606,1.47523487017669));
#44333=CARTESIAN_POINT('',(4.,10.4968415286606,1.47523487017669));
#44334=CARTESIAN_POINT('Origin',(4.,9.96074178033063,3.62541351925209));
#44335=CARTESIAN_POINT('',(3.85,9.96074178033063,3.62541351925209));
#44336=CARTESIAN_POINT('',(4.,9.96074178033063,3.62541351925209));
#44337=CARTESIAN_POINT('',(3.85,10.2851346985256,2.56437209335648));
#44338=CARTESIAN_POINT('Origin',(4.,9.52721689077117,4.64673415596422));
#44339=CARTESIAN_POINT('',(3.85,9.52721689077117,4.64673415596422));
#44340=CARTESIAN_POINT('',(4.,9.52721689077117,4.64673415596422));
#44341=CARTESIAN_POINT('',(3.85,9.96074178033063,3.62541351925209));
#44342=CARTESIAN_POINT('Origin',(4.,8.98930981925811,5.61714420087197));
#44343=CARTESIAN_POINT('',(3.85,8.98930981925811,5.61714420087197));
#44344=CARTESIAN_POINT('',(4.,8.98930981925811,5.61714420087197));
#44345=CARTESIAN_POINT('',(3.85,9.52721689077117,4.64673415596422));
#44346=CARTESIAN_POINT('Origin',(4.,8.35291398823125,6.52601163845198));
#44347=CARTESIAN_POINT('',(3.85,8.35291398823125,6.52601163845198));
#44348=CARTESIAN_POINT('',(4.,8.35291398823125,6.52601163845198));
#44349=CARTESIAN_POINT('',(3.85,8.98930981925811,5.61714420087197));
#44350=CARTESIAN_POINT('Origin',(4.,7.6250018835897,7.36337872686537));
#44351=CARTESIAN_POINT('',(3.85,7.6250018835897,7.36337872686537));
#44352=CARTESIAN_POINT('',(4.,7.6250018835897,7.36337872686537));
#44353=CARTESIAN_POINT('',(3.85,8.35291398823125,6.52601163845198));
#44354=CARTESIAN_POINT('Origin',(4.,5.17924656243829,5.00154026730478));
#44355=CARTESIAN_POINT('',(3.85,5.17924656243829,5.00154026730478));
#44356=CARTESIAN_POINT('',(4.,5.17924656243829,5.00154026730478));
#44357=CARTESIAN_POINT('',(3.85,7.6250018835897,7.36337872686537));
#44358=CARTESIAN_POINT('Origin',(4.,5.6736774259684,4.43276262234474));
#44359=CARTESIAN_POINT('',(3.85,5.6736774259684,4.43276262234474));
#44360=CARTESIAN_POINT('',(4.,5.6736774259684,4.43276262234474));
#44361=CARTESIAN_POINT('',(3.85,5.17924656243829,5.00154026730478));
#44362=CARTESIAN_POINT('Origin',(4.,6.10594629232627,3.81541870247908));
#44363=CARTESIAN_POINT('',(3.85,6.10594629232627,3.81541870247908));
#44364=CARTESIAN_POINT('',(4.,6.10594629232627,3.81541870247908));
#44365=CARTESIAN_POINT('',(3.85,5.6736774259684,4.43276262234474));
#44366=CARTESIAN_POINT('Origin',(4.,6.471317133354,3.15627225688136));
#44367=CARTESIAN_POINT('',(3.85,6.471317133354,3.15627225688136));
#44368=CARTESIAN_POINT('',(4.,6.471317133354,3.15627225688136));
#44369=CARTESIAN_POINT('',(3.85,6.10594629232627,3.81541870247908));
#44370=CARTESIAN_POINT('Origin',(4.,6.76578686965854,2.46254503194481));
#44371=CARTESIAN_POINT('',(3.85,6.76578686965854,2.46254503194481));
#44372=CARTESIAN_POINT('',(4.,6.76578686965854,2.46254503194481));
#44373=CARTESIAN_POINT('',(3.85,6.471317133354,3.15627225688136));
#44374=CARTESIAN_POINT('Origin',(4.,6.98612922918717,1.74183764831761));
#44375=CARTESIAN_POINT('',(3.85,6.98612922918717,1.74183764831761));
#44376=CARTESIAN_POINT('',(4.,6.98612922918717,1.74183764831761));
#44377=CARTESIAN_POINT('',(3.85,6.76578686965854,2.46254503194481));
#44378=CARTESIAN_POINT('Origin',(4.,7.12993009493931,1.00204632691247));
#44379=CARTESIAN_POINT('',(3.85,7.12993009493931,1.00204632691247));
#44380=CARTESIAN_POINT('',(4.,7.12993009493931,1.00204632691247));
#44381=CARTESIAN_POINT('',(3.85,6.98612922918717,1.74183764831761));
#44382=CARTESIAN_POINT('Origin',(4.,10.4968415286606,1.47523487017669));
#44383=CARTESIAN_POINT('',(3.85,7.12993009493931,1.00204632691247));
#44384=CARTESIAN_POINT('Origin',(3.85,7.83804404554947,4.18271252688892));
#44385=CARTESIAN_POINT('Origin',(4.,2.92175597166019,10.1893739769462));
#44386=CARTESIAN_POINT('',(3.85,2.92175597166019,10.1893739769462));
#44387=CARTESIAN_POINT('',(4.,2.92175597166019,10.1893739769462));
#44388=CARTESIAN_POINT('',(3.85,3.97082989020867,9.82814885840795));
#44389=CARTESIAN_POINT('',(3.85,3.97082989020867,9.82814885840795));
#44390=CARTESIAN_POINT('',(4.,3.97082989020867,9.82814885840795));
#44391=CARTESIAN_POINT('Origin',(4.,1.84067068326946,10.4389621819294));
#44392=CARTESIAN_POINT('',(3.85,1.84067068326946,10.4389621819294));
#44393=CARTESIAN_POINT('',(4.,1.84067068326946,10.4389621819294));
#44394=CARTESIAN_POINT('',(3.85,2.92175597166019,10.1893739769462));
#44395=CARTESIAN_POINT('Origin',(4.,0.739418621687727,10.5741789327541));
#44396=CARTESIAN_POINT('',(3.85,0.739418621687727,10.5741789327541));
#44397=CARTESIAN_POINT('',(4.,0.739418621687727,10.5741789327541));
#44398=CARTESIAN_POINT('',(3.85,1.84067068326946,10.4389621819294));
#44399=CARTESIAN_POINT('Origin',(4.,-0.36993466504651,10.5935427664024));
#44400=CARTESIAN_POINT('',(3.85,-0.36993466504651,10.5935427664024));
#44401=CARTESIAN_POINT('',(4.,-0.36993466504651,10.5935427664024));
#44402=CARTESIAN_POINT('',(3.85,0.739418621687727,10.5741789327541));
#44403=CARTESIAN_POINT('Origin',(4.,-1.4752348701767,10.4968415286606));
#44404=CARTESIAN_POINT('',(3.85,-1.47523487017669,10.4968415286606));
#44405=CARTESIAN_POINT('',(4.,-1.4752348701767,10.4968415286606));
#44406=CARTESIAN_POINT('',(3.85,-0.36993466504651,10.5935427664024));
#44407=CARTESIAN_POINT('Origin',(4.,-2.56437209335648,10.2851346985256));
#44408=CARTESIAN_POINT('',(3.85,-2.56437209335648,10.2851346985256));
#44409=CARTESIAN_POINT('',(4.,-2.56437209335648,10.2851346985256));
#44410=CARTESIAN_POINT('',(3.85,-1.4752348701767,10.4968415286606));
#44411=CARTESIAN_POINT('Origin',(4.,-1.74183764831761,6.98612922918717));
#44412=CARTESIAN_POINT('',(3.85,-1.74183764831761,6.98612922918717));
#44413=CARTESIAN_POINT('',(4.,-1.74183764831761,6.98612922918717));
#44414=CARTESIAN_POINT('',(3.85,-2.56437209335648,10.2851346985256));
#44415=CARTESIAN_POINT('Origin',(4.,-1.00204632691247,7.12993009493931));
#44416=CARTESIAN_POINT('',(3.85,-1.00204632691247,7.12993009493931));
#44417=CARTESIAN_POINT('',(4.,-1.00204632691247,7.12993009493931));
#44418=CARTESIAN_POINT('',(3.85,-1.74183764831761,6.98612922918717));
#44419=CARTESIAN_POINT('Origin',(4.,-0.251276376258007,7.19561395453749));
#44420=CARTESIAN_POINT('',(3.85,-0.251276376258007,7.19561395453749));
#44421=CARTESIAN_POINT('',(4.,-0.251276376258007,7.19561395453749));
#44422=CARTESIAN_POINT('',(3.85,-1.00204632691247,7.12993009493931));
#44423=CARTESIAN_POINT('Origin',(4.,0.502246610957702,7.18246116187073));
#44424=CARTESIAN_POINT('',(3.85,0.502246610957702,7.18246116187073));
#44425=CARTESIAN_POINT('',(4.,0.502246610957702,7.18246116187073));
#44426=CARTESIAN_POINT('',(3.85,-0.251276376258007,7.19561395453749));
#44427=CARTESIAN_POINT('Origin',(4.,1.2502668792019,7.0906158216879));
#44428=CARTESIAN_POINT('',(3.85,1.2502668792019,7.0906158216879));
#44429=CARTESIAN_POINT('',(4.,1.2502668792019,7.0906158216879));
#44430=CARTESIAN_POINT('',(3.85,0.502246610957702,7.18246116187073));
#44431=CARTESIAN_POINT('Origin',(4.,1.98458896188239,6.9210842107559));
#44432=CARTESIAN_POINT('',(3.85,1.98458896188239,6.9210842107559));
#44433=CARTESIAN_POINT('',(4.,1.98458896188239,6.9210842107559));
#44434=CARTESIAN_POINT('',(3.85,1.2502668792019,7.0906158216879));
#44435=CARTESIAN_POINT('Origin',(4.,2.69716747259457,6.67572375288087));
#44436=CARTESIAN_POINT('',(3.85,2.69716747259457,6.67572375288087));
#44437=CARTESIAN_POINT('',(4.,2.69716747259457,6.67572375288087));
#44438=CARTESIAN_POINT('',(3.85,1.98458896188239,6.9210842107559));
#44439=CARTESIAN_POINT('Origin',(4.,3.97082989020867,9.82814885840795));
#44440=CARTESIAN_POINT('',(3.85,2.69716747259457,6.67572375288087));
#44441=CARTESIAN_POINT('Origin',(3.85,0.703228898426094,8.63463325964164));
#44442=CARTESIAN_POINT('Origin',(4.,-7.36337872686537,7.6250018835897));
#44443=CARTESIAN_POINT('',(3.85,-7.36337872686537,7.6250018835897));
#44444=CARTESIAN_POINT('',(4.,-7.36337872686537,7.6250018835897));
#44445=CARTESIAN_POINT('',(3.85,-6.52601163845198,8.35291398823125));
#44446=CARTESIAN_POINT('',(3.85,-6.52601163845198,8.35291398823125));
#44447=CARTESIAN_POINT('',(4.,-6.52601163845198,8.35291398823125));
#44448=CARTESIAN_POINT('Origin',(4.,-8.12007109706117,6.81354866267732));
#44449=CARTESIAN_POINT('',(3.85,-8.12007109706117,6.81354866267732));
#44450=CARTESIAN_POINT('',(4.,-8.12007109706117,6.81354866267732));
#44451=CARTESIAN_POINT('',(3.85,-7.36337872686537,7.6250018835897));
#44452=CARTESIAN_POINT('Origin',(4.,-8.78779826908344,5.92744477678992));
#44453=CARTESIAN_POINT('',(3.85,-8.78779826908344,5.92744477678992));
#44454=CARTESIAN_POINT('',(4.,-8.78779826908344,5.92744477678992));
#44455=CARTESIAN_POINT('',(3.85,-8.12007109706117,6.81354866267732));
#44456=CARTESIAN_POINT('Origin',(4.,-9.35924448430463,4.97639856553044));
#44457=CARTESIAN_POINT('',(3.85,-9.35924448430463,4.97639856553044));
#44458=CARTESIAN_POINT('',(4.,-9.35924448430463,4.97639856553044));
#44459=CARTESIAN_POINT('',(3.85,-8.78779826908344,5.92744477678992));
#44460=CARTESIAN_POINT('Origin',(4.,-9.82814885840794,3.97082989020867));
#44461=CARTESIAN_POINT('',(3.85,-9.82814885840794,3.97082989020867));
#44462=CARTESIAN_POINT('',(4.,-9.82814885840794,3.97082989020867));
#44463=CARTESIAN_POINT('',(3.85,-9.35924448430463,4.97639856553044));
#44464=CARTESIAN_POINT('Origin',(4.,-10.1893739769462,2.92175597166019));
#44465=CARTESIAN_POINT('',(3.85,-10.1893739769462,2.92175597166019));
#44466=CARTESIAN_POINT('',(4.,-10.1893739769462,2.92175597166019));
#44467=CARTESIAN_POINT('',(3.85,-9.82814885840794,3.97082989020867));
#44468=CARTESIAN_POINT('Origin',(4.,-6.9210842107559,1.98458896188239));
#44469=CARTESIAN_POINT('',(3.85,-6.9210842107559,1.98458896188239));
#44470=CARTESIAN_POINT('',(4.,-6.9210842107559,1.98458896188239));
#44471=CARTESIAN_POINT('',(3.85,-10.1893739769462,2.92175597166019));
#44472=CARTESIAN_POINT('Origin',(4.,-6.67572375288087,2.69716747259457));
#44473=CARTESIAN_POINT('',(3.85,-6.67572375288087,2.69716747259457));
#44474=CARTESIAN_POINT('',(4.,-6.67572375288087,2.69716747259457));
#44475=CARTESIAN_POINT('',(3.85,-6.9210842107559,1.98458896188239));
#44476=CARTESIAN_POINT('Origin',(4.,-6.35722266858427,3.38019525205841));
#44477=CARTESIAN_POINT('',(3.85,-6.35722266858427,3.38019525205841));
#44478=CARTESIAN_POINT('',(4.,-6.35722266858427,3.38019525205841));
#44479=CARTESIAN_POINT('',(3.85,-6.67572375288087,2.69716747259457));
#44480=CARTESIAN_POINT('Origin',(4.,-5.9690705223963,4.02618890498938));
#44481=CARTESIAN_POINT('',(3.85,-5.9690705223963,4.02618890498938));
#44482=CARTESIAN_POINT('',(4.,-5.9690705223963,4.02618890498938));
#44483=CARTESIAN_POINT('',(3.85,-6.35722266858427,3.38019525205841));
#44484=CARTESIAN_POINT('Origin',(4.,-5.51551999045664,4.62807078974308));
#44485=CARTESIAN_POINT('',(3.85,-5.51551999045664,4.62807078974308));
#44486=CARTESIAN_POINT('',(4.,-5.51551999045664,4.62807078974308));
#44487=CARTESIAN_POINT('',(3.85,-5.9690705223963,4.02618890498938));
#44488=CARTESIAN_POINT('Origin',(4.,-5.00154026730478,5.17924656243829));
#44489=CARTESIAN_POINT('',(3.85,-5.00154026730478,5.17924656243829));
#44490=CARTESIAN_POINT('',(4.,-5.00154026730478,5.17924656243829));
#44491=CARTESIAN_POINT('',(3.85,-5.51551999045664,4.62807078974308));
#44492=CARTESIAN_POINT('Origin',(4.,-4.43276262234474,5.6736774259684));
#44493=CARTESIAN_POINT('',(3.85,-4.43276262234474,5.6736774259684));
#44494=CARTESIAN_POINT('',(4.,-4.43276262234474,5.6736774259684));
#44495=CARTESIAN_POINT('',(3.85,-5.00154026730478,5.17924656243829));
#44496=CARTESIAN_POINT('Origin',(4.,-6.52601163845198,8.35291398823125));
#44497=CARTESIAN_POINT('',(3.85,-4.43276262234474,5.6736774259684));
#44498=CARTESIAN_POINT('Origin',(3.85,-7.31106829964546,5.16875147505682));
#44499=CARTESIAN_POINT('Origin',(4.,-10.2851346985256,-2.56437209335648));
#44500=CARTESIAN_POINT('',(3.85,-10.2851346985256,-2.56437209335648));
#44501=CARTESIAN_POINT('',(4.,-10.2851346985256,-2.56437209335648));
#44502=CARTESIAN_POINT('',(3.85,-10.4968415286606,-1.47523487017669));
#44503=CARTESIAN_POINT('',(3.85,-10.4968415286606,-1.47523487017669));
#44504=CARTESIAN_POINT('',(4.,-10.4968415286606,-1.47523487017669));
#44505=CARTESIAN_POINT('Origin',(4.,-9.96074178033063,-3.62541351925209));
#44506=CARTESIAN_POINT('',(3.85,-9.96074178033063,-3.62541351925209));
#44507=CARTESIAN_POINT('',(4.,-9.96074178033063,-3.62541351925209));
#44508=CARTESIAN_POINT('',(3.85,-10.2851346985256,-2.56437209335648));
#44509=CARTESIAN_POINT('Origin',(4.,-9.52721689077117,-4.64673415596422));
#44510=CARTESIAN_POINT('',(3.85,-9.52721689077117,-4.64673415596422));
#44511=CARTESIAN_POINT('',(4.,-9.52721689077117,-4.64673415596422));
#44512=CARTESIAN_POINT('',(3.85,-9.96074178033063,-3.62541351925209));
#44513=CARTESIAN_POINT('Origin',(4.,-8.98930981925811,-5.61714420087197));
#44514=CARTESIAN_POINT('',(3.85,-8.98930981925811,-5.61714420087197));
#44515=CARTESIAN_POINT('',(4.,-8.98930981925811,-5.61714420087197));
#44516=CARTESIAN_POINT('',(3.85,-9.52721689077117,-4.64673415596422));
#44517=CARTESIAN_POINT('Origin',(4.,-8.35291398823125,-6.52601163845198));
#44518=CARTESIAN_POINT('',(3.85,-8.35291398823125,-6.52601163845198));
#44519=CARTESIAN_POINT('',(4.,-8.35291398823125,-6.52601163845198));
#44520=CARTESIAN_POINT('',(3.85,-8.98930981925811,-5.61714420087197));
#44521=CARTESIAN_POINT('Origin',(4.,-7.6250018835897,-7.36337872686537));
#44522=CARTESIAN_POINT('',(3.85,-7.6250018835897,-7.36337872686537));
#44523=CARTESIAN_POINT('',(4.,-7.6250018835897,-7.36337872686537));
#44524=CARTESIAN_POINT('',(3.85,-8.35291398823125,-6.52601163845198));
#44525=CARTESIAN_POINT('Origin',(4.,-5.17924656243829,-5.00154026730478));
#44526=CARTESIAN_POINT('',(3.85,-5.17924656243829,-5.00154026730478));
#44527=CARTESIAN_POINT('',(4.,-5.17924656243829,-5.00154026730478));
#44528=CARTESIAN_POINT('',(3.85,-7.6250018835897,-7.36337872686537));
#44529=CARTESIAN_POINT('Origin',(4.,-5.6736774259684,-4.43276262234474));
#44530=CARTESIAN_POINT('',(3.85,-5.6736774259684,-4.43276262234474));
#44531=CARTESIAN_POINT('',(4.,-5.6736774259684,-4.43276262234474));
#44532=CARTESIAN_POINT('',(3.85,-5.17924656243829,-5.00154026730478));
#44533=CARTESIAN_POINT('Origin',(4.,-6.10594629232627,-3.81541870247908));
#44534=CARTESIAN_POINT('',(3.85,-6.10594629232627,-3.81541870247908));
#44535=CARTESIAN_POINT('',(4.,-6.10594629232627,-3.81541870247908));
#44536=CARTESIAN_POINT('',(3.85,-5.6736774259684,-4.43276262234474));
#44537=CARTESIAN_POINT('Origin',(4.,-6.471317133354,-3.15627225688136));
#44538=CARTESIAN_POINT('',(3.85,-6.471317133354,-3.15627225688136));
#44539=CARTESIAN_POINT('',(4.,-6.471317133354,-3.15627225688136));
#44540=CARTESIAN_POINT('',(3.85,-6.10594629232627,-3.81541870247908));
#44541=CARTESIAN_POINT('Origin',(4.,-6.76578686965854,-2.46254503194481));
#44542=CARTESIAN_POINT('',(3.85,-6.76578686965854,-2.46254503194481));
#44543=CARTESIAN_POINT('',(4.,-6.76578686965854,-2.46254503194481));
#44544=CARTESIAN_POINT('',(3.85,-6.471317133354,-3.15627225688136));
#44545=CARTESIAN_POINT('Origin',(4.,-6.98612922918717,-1.74183764831761));
#44546=CARTESIAN_POINT('',(3.85,-6.98612922918717,-1.74183764831761));
#44547=CARTESIAN_POINT('',(4.,-6.98612922918717,-1.74183764831761));
#44548=CARTESIAN_POINT('',(3.85,-6.76578686965854,-2.46254503194481));
#44549=CARTESIAN_POINT('Origin',(4.,-7.12993009493931,-1.00204632691247));
#44550=CARTESIAN_POINT('',(3.85,-7.12993009493931,-1.00204632691247));
#44551=CARTESIAN_POINT('',(4.,-7.12993009493931,-1.00204632691247));
#44552=CARTESIAN_POINT('',(3.85,-6.98612922918717,-1.74183764831761));
#44553=CARTESIAN_POINT('Origin',(4.,-10.4968415286606,-1.47523487017669));
#44554=CARTESIAN_POINT('',(3.85,-7.12993009493931,-1.00204632691247));
#44555=CARTESIAN_POINT('Origin',(3.85,-7.83804404554947,-4.18271252688892));
#44556=CARTESIAN_POINT('Origin',(4.,7.36337872686537,-7.6250018835897));
#44557=CARTESIAN_POINT('',(3.85,7.36337872686537,-7.6250018835897));
#44558=CARTESIAN_POINT('',(4.,7.36337872686537,-7.6250018835897));
#44559=CARTESIAN_POINT('',(3.85,6.52601163845198,-8.35291398823125));
#44560=CARTESIAN_POINT('',(3.85,6.52601163845198,-8.35291398823125));
#44561=CARTESIAN_POINT('',(4.,6.52601163845198,-8.35291398823125));
#44562=CARTESIAN_POINT('Origin',(4.,8.12007109706117,-6.81354866267731));
#44563=CARTESIAN_POINT('',(3.85,8.12007109706117,-6.81354866267731));
#44564=CARTESIAN_POINT('',(4.,8.12007109706117,-6.81354866267731));
#44565=CARTESIAN_POINT('',(3.85,7.36337872686537,-7.6250018835897));
#44566=CARTESIAN_POINT('Origin',(4.,8.78779826908344,-5.92744477678991));
#44567=CARTESIAN_POINT('',(3.85,8.78779826908344,-5.92744477678991));
#44568=CARTESIAN_POINT('',(4.,8.78779826908344,-5.92744477678991));
#44569=CARTESIAN_POINT('',(3.85,8.12007109706117,-6.81354866267731));
#44570=CARTESIAN_POINT('Origin',(4.,9.35924448430463,-4.97639856553044));
#44571=CARTESIAN_POINT('',(3.85,9.35924448430463,-4.97639856553044));
#44572=CARTESIAN_POINT('',(4.,9.35924448430463,-4.97639856553044));
#44573=CARTESIAN_POINT('',(3.85,8.78779826908344,-5.92744477678991));
#44574=CARTESIAN_POINT('Origin',(4.,9.82814885840795,-3.97082989020866));
#44575=CARTESIAN_POINT('',(3.85,9.82814885840795,-3.97082989020866));
#44576=CARTESIAN_POINT('',(4.,9.82814885840795,-3.97082989020866));
#44577=CARTESIAN_POINT('',(3.85,9.35924448430463,-4.97639856553044));
#44578=CARTESIAN_POINT('Origin',(4.,10.1893739769462,-2.92175597166019));
#44579=CARTESIAN_POINT('',(3.85,10.1893739769462,-2.92175597166019));
#44580=CARTESIAN_POINT('',(4.,10.1893739769462,-2.92175597166019));
#44581=CARTESIAN_POINT('',(3.85,9.82814885840795,-3.97082989020866));
#44582=CARTESIAN_POINT('Origin',(4.,6.9210842107559,-1.98458896188239));
#44583=CARTESIAN_POINT('',(3.85,6.9210842107559,-1.98458896188239));
#44584=CARTESIAN_POINT('',(4.,6.9210842107559,-1.98458896188239));
#44585=CARTESIAN_POINT('',(3.85,10.1893739769462,-2.92175597166019));
#44586=CARTESIAN_POINT('Origin',(4.,6.67572375288087,-2.69716747259456));
#44587=CARTESIAN_POINT('',(3.85,6.67572375288087,-2.69716747259456));
#44588=CARTESIAN_POINT('',(4.,6.67572375288087,-2.69716747259456));
#44589=CARTESIAN_POINT('',(3.85,6.9210842107559,-1.98458896188239));
#44590=CARTESIAN_POINT('Origin',(4.,6.35722266858427,-3.38019525205841));
#44591=CARTESIAN_POINT('',(3.85,6.35722266858427,-3.38019525205841));
#44592=CARTESIAN_POINT('',(4.,6.35722266858427,-3.38019525205841));
#44593=CARTESIAN_POINT('',(3.85,6.67572375288087,-2.69716747259456));
#44594=CARTESIAN_POINT('Origin',(4.,5.9690705223963,-4.02618890498938));
#44595=CARTESIAN_POINT('',(3.85,5.9690705223963,-4.02618890498938));
#44596=CARTESIAN_POINT('',(4.,5.9690705223963,-4.02618890498938));
#44597=CARTESIAN_POINT('',(3.85,6.35722266858427,-3.38019525205841));
#44598=CARTESIAN_POINT('Origin',(4.,5.51551999045664,-4.62807078974308));
#44599=CARTESIAN_POINT('',(3.85,5.51551999045664,-4.62807078974308));
#44600=CARTESIAN_POINT('',(4.,5.51551999045664,-4.62807078974308));
#44601=CARTESIAN_POINT('',(3.85,5.9690705223963,-4.02618890498938));
#44602=CARTESIAN_POINT('Origin',(4.,5.00154026730478,-5.17924656243829));
#44603=CARTESIAN_POINT('',(3.85,5.00154026730478,-5.17924656243829));
#44604=CARTESIAN_POINT('',(4.,5.00154026730478,-5.17924656243829));
#44605=CARTESIAN_POINT('',(3.85,5.51551999045664,-4.62807078974308));
#44606=CARTESIAN_POINT('Origin',(4.,4.43276262234474,-5.6736774259684));
#44607=CARTESIAN_POINT('',(3.85,4.43276262234474,-5.6736774259684));
#44608=CARTESIAN_POINT('',(4.,4.43276262234474,-5.6736774259684));
#44609=CARTESIAN_POINT('',(3.85,5.00154026730478,-5.17924656243829));
#44610=CARTESIAN_POINT('Origin',(4.,6.52601163845198,-8.35291398823125));
#44611=CARTESIAN_POINT('',(3.85,4.43276262234474,-5.6736774259684));
#44612=CARTESIAN_POINT('Origin',(3.85,7.31106829964546,-5.16875147505682));
#44613=CARTESIAN_POINT('Origin',(0.,-1.9845889618824,-6.92108421075589));
#44614=CARTESIAN_POINT('',(0.15,-1.9845889618824,-6.92108421075589));
#44615=CARTESIAN_POINT('',(0.,-1.9845889618824,-6.92108421075589));
#44616=CARTESIAN_POINT('',(0.15,-2.69716747259457,-6.67572375288087));
#44617=CARTESIAN_POINT('',(0.15,-1.9845889618824,-6.92108421075589));
#44618=CARTESIAN_POINT('',(0.,-2.69716747259457,-6.67572375288087));
#44619=CARTESIAN_POINT('Origin',(0.,-1.2502668792019,-7.0906158216879));
#44620=CARTESIAN_POINT('',(0.15,-1.2502668792019,-7.0906158216879));
#44621=CARTESIAN_POINT('',(0.,-1.2502668792019,-7.0906158216879));
#44622=CARTESIAN_POINT('',(0.15,-1.2502668792019,-7.0906158216879));
#44623=CARTESIAN_POINT('Origin',(0.,-0.502246610957704,-7.18246116187073));
#44624=CARTESIAN_POINT('',(0.15,-0.502246610957704,-7.18246116187073));
#44625=CARTESIAN_POINT('',(0.,-0.502246610957704,-7.18246116187073));
#44626=CARTESIAN_POINT('',(0.15,-0.502246610957704,-7.18246116187073));
#44627=CARTESIAN_POINT('Origin',(0.,0.251276376258003,-7.19561395453749));
#44628=CARTESIAN_POINT('',(0.15,0.251276376258003,-7.19561395453749));
#44629=CARTESIAN_POINT('',(0.,0.251276376258003,-7.19561395453749));
#44630=CARTESIAN_POINT('',(0.15,0.251276376258003,-7.19561395453749));
#44631=CARTESIAN_POINT('Origin',(0.,1.00204632691247,-7.12993009493931));
#44632=CARTESIAN_POINT('',(0.15,1.00204632691247,-7.12993009493931));
#44633=CARTESIAN_POINT('',(0.,1.00204632691247,-7.12993009493931));
#44634=CARTESIAN_POINT('',(0.15,1.00204632691247,-7.12993009493931));
#44635=CARTESIAN_POINT('Origin',(0.,1.74183764831761,-6.98612922918718));
#44636=CARTESIAN_POINT('',(0.15,1.74183764831761,-6.98612922918718));
#44637=CARTESIAN_POINT('',(0.,1.74183764831761,-6.98612922918718));
#44638=CARTESIAN_POINT('',(0.15,1.74183764831761,-6.98612922918718));
#44639=CARTESIAN_POINT('Origin',(0.,2.56437209335647,-10.2851346985256));
#44640=CARTESIAN_POINT('',(0.15,2.56437209335647,-10.2851346985256));
#44641=CARTESIAN_POINT('',(0.,2.56437209335647,-10.2851346985256));
#44642=CARTESIAN_POINT('',(0.15,2.56437209335647,-10.2851346985256));
#44643=CARTESIAN_POINT('Origin',(0.,1.47523487017669,-10.4968415286606));
#44644=CARTESIAN_POINT('',(0.15,1.47523487017669,-10.4968415286606));
#44645=CARTESIAN_POINT('',(0.,1.47523487017669,-10.4968415286606));
#44646=CARTESIAN_POINT('',(0.15,1.47523487017669,-10.4968415286606));
#44647=CARTESIAN_POINT('Origin',(0.,0.369934665046504,-10.5935427664024));
#44648=CARTESIAN_POINT('',(0.15,0.369934665046504,-10.5935427664024));
#44649=CARTESIAN_POINT('',(0.,0.369934665046504,-10.5935427664024));
#44650=CARTESIAN_POINT('',(0.15,0.369934665046504,-10.5935427664024));
#44651=CARTESIAN_POINT('Origin',(0.,-0.739418621687731,-10.5741789327541));
#44652=CARTESIAN_POINT('',(0.15,-0.739418621687731,-10.5741789327541));
#44653=CARTESIAN_POINT('',(0.,-0.739418621687731,-10.5741789327541));
#44654=CARTESIAN_POINT('',(0.15,-0.739418621687731,-10.5741789327541));
#44655=CARTESIAN_POINT('Origin',(0.,-1.84067068326946,-10.4389621819294));
#44656=CARTESIAN_POINT('',(0.15,-1.84067068326946,-10.4389621819294));
#44657=CARTESIAN_POINT('',(0.,-1.84067068326946,-10.4389621819294));
#44658=CARTESIAN_POINT('',(0.15,-1.84067068326946,-10.4389621819294));
#44659=CARTESIAN_POINT('Origin',(0.,-2.9217559716602,-10.1893739769462));
#44660=CARTESIAN_POINT('',(0.15,-2.9217559716602,-10.1893739769462));
#44661=CARTESIAN_POINT('',(0.,-2.9217559716602,-10.1893739769462));
#44662=CARTESIAN_POINT('',(0.15,-2.9217559716602,-10.1893739769462));
#44663=CARTESIAN_POINT('Origin',(0.,-3.97082989020867,-9.82814885840794));
#44664=CARTESIAN_POINT('',(0.15,-3.97082989020867,-9.82814885840794));
#44665=CARTESIAN_POINT('',(0.,-3.97082989020867,-9.82814885840794));
#44666=CARTESIAN_POINT('',(0.15,-3.97082989020867,-9.82814885840794));
#44667=CARTESIAN_POINT('Origin',(0.,-2.69716747259457,-6.67572375288087));
#44668=CARTESIAN_POINT('',(0.15,-2.69716747259457,-6.67572375288087));
#44669=CARTESIAN_POINT('Origin',(0.15,-0.703228898426098,-8.63463325964164));
#44670=CARTESIAN_POINT('Origin',(0.,6.98612922918717,1.74183764831761));
#44671=CARTESIAN_POINT('',(0.15,6.98612922918717,1.74183764831761));
#44672=CARTESIAN_POINT('',(0.,6.98612922918717,1.74183764831761));
#44673=CARTESIAN_POINT('',(0.15,7.12993009493931,1.00204632691247));
#44674=CARTESIAN_POINT('',(0.15,6.98612922918717,1.74183764831761));
#44675=CARTESIAN_POINT('',(0.,7.12993009493931,1.00204632691247));
#44676=CARTESIAN_POINT('Origin',(0.,6.76578686965854,2.46254503194481));
#44677=CARTESIAN_POINT('',(0.15,6.76578686965854,2.46254503194481));
#44678=CARTESIAN_POINT('',(0.,6.76578686965854,2.46254503194481));
#44679=CARTESIAN_POINT('',(0.15,6.76578686965854,2.46254503194481));
#44680=CARTESIAN_POINT('Origin',(0.,6.471317133354,3.15627225688136));
#44681=CARTESIAN_POINT('',(0.15,6.471317133354,3.15627225688136));
#44682=CARTESIAN_POINT('',(0.,6.471317133354,3.15627225688136));
#44683=CARTESIAN_POINT('',(0.15,6.471317133354,3.15627225688136));
#44684=CARTESIAN_POINT('Origin',(0.,6.10594629232627,3.81541870247908));
#44685=CARTESIAN_POINT('',(0.15,6.10594629232627,3.81541870247908));
#44686=CARTESIAN_POINT('',(0.,6.10594629232627,3.81541870247908));
#44687=CARTESIAN_POINT('',(0.15,6.10594629232627,3.81541870247908));
#44688=CARTESIAN_POINT('Origin',(0.,5.6736774259684,4.43276262234474));
#44689=CARTESIAN_POINT('',(0.15,5.6736774259684,4.43276262234474));
#44690=CARTESIAN_POINT('',(0.,5.6736774259684,4.43276262234474));
#44691=CARTESIAN_POINT('',(0.15,5.6736774259684,4.43276262234474));
#44692=CARTESIAN_POINT('Origin',(0.,5.17924656243829,5.00154026730478));
#44693=CARTESIAN_POINT('',(0.15,5.17924656243829,5.00154026730478));
#44694=CARTESIAN_POINT('',(0.,5.17924656243829,5.00154026730478));
#44695=CARTESIAN_POINT('',(0.15,5.17924656243829,5.00154026730478));
#44696=CARTESIAN_POINT('Origin',(0.,7.6250018835897,7.36337872686537));
#44697=CARTESIAN_POINT('',(0.15,7.6250018835897,7.36337872686537));
#44698=CARTESIAN_POINT('',(0.,7.6250018835897,7.36337872686537));
#44699=CARTESIAN_POINT('',(0.15,7.6250018835897,7.36337872686537));
#44700=CARTESIAN_POINT('Origin',(0.,8.35291398823125,6.52601163845198));
#44701=CARTESIAN_POINT('',(0.15,8.35291398823125,6.52601163845198));
#44702=CARTESIAN_POINT('',(0.,8.35291398823125,6.52601163845198));
#44703=CARTESIAN_POINT('',(0.15,8.35291398823125,6.52601163845198));
#44704=CARTESIAN_POINT('Origin',(0.,8.98930981925811,5.61714420087197));
#44705=CARTESIAN_POINT('',(0.15,8.98930981925811,5.61714420087197));
#44706=CARTESIAN_POINT('',(0.,8.98930981925811,5.61714420087197));
#44707=CARTESIAN_POINT('',(0.15,8.98930981925811,5.61714420087197));
#44708=CARTESIAN_POINT('Origin',(0.,9.52721689077117,4.64673415596422));
#44709=CARTESIAN_POINT('',(0.15,9.52721689077117,4.64673415596422));
#44710=CARTESIAN_POINT('',(0.,9.52721689077117,4.64673415596422));
#44711=CARTESIAN_POINT('',(0.15,9.52721689077117,4.64673415596422));
#44712=CARTESIAN_POINT('Origin',(0.,9.96074178033063,3.62541351925209));
#44713=CARTESIAN_POINT('',(0.15,9.96074178033063,3.62541351925209));
#44714=CARTESIAN_POINT('',(0.,9.96074178033063,3.62541351925209));
#44715=CARTESIAN_POINT('',(0.15,9.96074178033063,3.62541351925209));
#44716=CARTESIAN_POINT('Origin',(0.,10.2851346985256,2.56437209335648));
#44717=CARTESIAN_POINT('',(0.15,10.2851346985256,2.56437209335648));
#44718=CARTESIAN_POINT('',(0.,10.2851346985256,2.56437209335648));
#44719=CARTESIAN_POINT('',(0.15,10.2851346985256,2.56437209335648));
#44720=CARTESIAN_POINT('Origin',(0.,10.4968415286606,1.47523487017669));
#44721=CARTESIAN_POINT('',(0.15,10.4968415286606,1.47523487017669));
#44722=CARTESIAN_POINT('',(0.,10.4968415286606,1.47523487017669));
#44723=CARTESIAN_POINT('',(0.15,10.4968415286606,1.47523487017669));
#44724=CARTESIAN_POINT('Origin',(0.,7.12993009493931,1.00204632691247));
#44725=CARTESIAN_POINT('',(0.15,7.12993009493931,1.00204632691247));
#44726=CARTESIAN_POINT('Origin',(0.15,7.83804404554947,4.18271252688892));
#44727=CARTESIAN_POINT('Origin',(0.,1.98458896188239,6.9210842107559));
#44728=CARTESIAN_POINT('',(0.15,1.98458896188239,6.9210842107559));
#44729=CARTESIAN_POINT('',(0.,1.98458896188239,6.9210842107559));
#44730=CARTESIAN_POINT('',(0.15,2.69716747259457,6.67572375288087));
#44731=CARTESIAN_POINT('',(0.15,1.98458896188239,6.9210842107559));
#44732=CARTESIAN_POINT('',(0.,2.69716747259457,6.67572375288087));
#44733=CARTESIAN_POINT('Origin',(0.,1.2502668792019,7.0906158216879));
#44734=CARTESIAN_POINT('',(0.15,1.2502668792019,7.0906158216879));
#44735=CARTESIAN_POINT('',(0.,1.2502668792019,7.0906158216879));
#44736=CARTESIAN_POINT('',(0.15,1.2502668792019,7.0906158216879));
#44737=CARTESIAN_POINT('Origin',(0.,0.502246610957702,7.18246116187073));
#44738=CARTESIAN_POINT('',(0.15,0.502246610957702,7.18246116187073));
#44739=CARTESIAN_POINT('',(0.,0.502246610957702,7.18246116187073));
#44740=CARTESIAN_POINT('',(0.15,0.502246610957702,7.18246116187073));
#44741=CARTESIAN_POINT('Origin',(0.,-0.251276376258007,7.19561395453749));
#44742=CARTESIAN_POINT('',(0.15,-0.251276376258007,7.19561395453749));
#44743=CARTESIAN_POINT('',(0.,-0.251276376258007,7.19561395453749));
#44744=CARTESIAN_POINT('',(0.15,-0.251276376258007,7.19561395453749));
#44745=CARTESIAN_POINT('Origin',(0.,-1.00204632691247,7.12993009493931));
#44746=CARTESIAN_POINT('',(0.15,-1.00204632691247,7.12993009493931));
#44747=CARTESIAN_POINT('',(0.,-1.00204632691247,7.12993009493931));
#44748=CARTESIAN_POINT('',(0.15,-1.00204632691247,7.12993009493931));
#44749=CARTESIAN_POINT('Origin',(0.,-1.74183764831761,6.98612922918717));
#44750=CARTESIAN_POINT('',(0.15,-1.74183764831761,6.98612922918717));
#44751=CARTESIAN_POINT('',(0.,-1.74183764831761,6.98612922918717));
#44752=CARTESIAN_POINT('',(0.15,-1.74183764831761,6.98612922918717));
#44753=CARTESIAN_POINT('Origin',(0.,-2.56437209335648,10.2851346985256));
#44754=CARTESIAN_POINT('',(0.15,-2.56437209335648,10.2851346985256));
#44755=CARTESIAN_POINT('',(0.,-2.56437209335648,10.2851346985256));
#44756=CARTESIAN_POINT('',(0.15,-2.56437209335648,10.2851346985256));
#44757=CARTESIAN_POINT('Origin',(0.,-1.4752348701767,10.4968415286606));
#44758=CARTESIAN_POINT('',(0.15,-1.47523487017669,10.4968415286606));
#44759=CARTESIAN_POINT('',(0.,-1.4752348701767,10.4968415286606));
#44760=CARTESIAN_POINT('',(0.15,-1.4752348701767,10.4968415286606));
#44761=CARTESIAN_POINT('Origin',(0.,-0.36993466504651,10.5935427664024));
#44762=CARTESIAN_POINT('',(0.15,-0.36993466504651,10.5935427664024));
#44763=CARTESIAN_POINT('',(0.,-0.36993466504651,10.5935427664024));
#44764=CARTESIAN_POINT('',(0.15,-0.36993466504651,10.5935427664024));
#44765=CARTESIAN_POINT('Origin',(0.,0.739418621687727,10.5741789327541));
#44766=CARTESIAN_POINT('',(0.15,0.739418621687727,10.5741789327541));
#44767=CARTESIAN_POINT('',(0.,0.739418621687727,10.5741789327541));
#44768=CARTESIAN_POINT('',(0.15,0.739418621687727,10.5741789327541));
#44769=CARTESIAN_POINT('Origin',(0.,1.84067068326946,10.4389621819294));
#44770=CARTESIAN_POINT('',(0.15,1.84067068326946,10.4389621819294));
#44771=CARTESIAN_POINT('',(0.,1.84067068326946,10.4389621819294));
#44772=CARTESIAN_POINT('',(0.15,1.84067068326946,10.4389621819294));
#44773=CARTESIAN_POINT('Origin',(0.,2.92175597166019,10.1893739769462));
#44774=CARTESIAN_POINT('',(0.15,2.92175597166019,10.1893739769462));
#44775=CARTESIAN_POINT('',(0.,2.92175597166019,10.1893739769462));
#44776=CARTESIAN_POINT('',(0.15,2.92175597166019,10.1893739769462));
#44777=CARTESIAN_POINT('Origin',(0.,3.97082989020867,9.82814885840795));
#44778=CARTESIAN_POINT('',(0.15,3.97082989020867,9.82814885840795));
#44779=CARTESIAN_POINT('',(0.,3.97082989020867,9.82814885840795));
#44780=CARTESIAN_POINT('',(0.15,3.97082989020867,9.82814885840795));
#44781=CARTESIAN_POINT('Origin',(0.,2.69716747259457,6.67572375288087));
#44782=CARTESIAN_POINT('',(0.15,2.69716747259457,6.67572375288087));
#44783=CARTESIAN_POINT('Origin',(0.15,0.703228898426094,8.63463325964164));
#44784=CARTESIAN_POINT('Origin',(0.,-5.00154026730478,5.17924656243829));
#44785=CARTESIAN_POINT('',(0.15,-5.00154026730478,5.17924656243829));
#44786=CARTESIAN_POINT('',(0.,-5.00154026730478,5.17924656243829));
#44787=CARTESIAN_POINT('',(0.15,-4.43276262234474,5.6736774259684));
#44788=CARTESIAN_POINT('',(0.15,-5.00154026730478,5.17924656243829));
#44789=CARTESIAN_POINT('',(0.,-4.43276262234474,5.6736774259684));
#44790=CARTESIAN_POINT('Origin',(0.,-5.51551999045664,4.62807078974308));
#44791=CARTESIAN_POINT('',(0.15,-5.51551999045664,4.62807078974308));
#44792=CARTESIAN_POINT('',(0.,-5.51551999045664,4.62807078974308));
#44793=CARTESIAN_POINT('',(0.15,-5.51551999045664,4.62807078974308));
#44794=CARTESIAN_POINT('Origin',(0.,-5.9690705223963,4.02618890498938));
#44795=CARTESIAN_POINT('',(0.15,-5.9690705223963,4.02618890498938));
#44796=CARTESIAN_POINT('',(0.,-5.9690705223963,4.02618890498938));
#44797=CARTESIAN_POINT('',(0.15,-5.9690705223963,4.02618890498938));
#44798=CARTESIAN_POINT('Origin',(0.,-6.35722266858427,3.38019525205841));
#44799=CARTESIAN_POINT('',(0.15,-6.35722266858427,3.38019525205841));
#44800=CARTESIAN_POINT('',(0.,-6.35722266858427,3.38019525205841));
#44801=CARTESIAN_POINT('',(0.15,-6.35722266858427,3.38019525205841));
#44802=CARTESIAN_POINT('Origin',(0.,-6.67572375288087,2.69716747259457));
#44803=CARTESIAN_POINT('',(0.15,-6.67572375288087,2.69716747259457));
#44804=CARTESIAN_POINT('',(0.,-6.67572375288087,2.69716747259457));
#44805=CARTESIAN_POINT('',(0.15,-6.67572375288087,2.69716747259457));
#44806=CARTESIAN_POINT('Origin',(0.,-6.9210842107559,1.98458896188239));
#44807=CARTESIAN_POINT('',(0.15,-6.9210842107559,1.98458896188239));
#44808=CARTESIAN_POINT('',(0.,-6.9210842107559,1.98458896188239));
#44809=CARTESIAN_POINT('',(0.15,-6.9210842107559,1.98458896188239));
#44810=CARTESIAN_POINT('Origin',(0.,-10.1893739769462,2.92175597166019));
#44811=CARTESIAN_POINT('',(0.15,-10.1893739769462,2.92175597166019));
#44812=CARTESIAN_POINT('',(0.,-10.1893739769462,2.92175597166019));
#44813=CARTESIAN_POINT('',(0.15,-10.1893739769462,2.92175597166019));
#44814=CARTESIAN_POINT('Origin',(0.,-9.82814885840794,3.97082989020867));
#44815=CARTESIAN_POINT('',(0.15,-9.82814885840794,3.97082989020867));
#44816=CARTESIAN_POINT('',(0.,-9.82814885840794,3.97082989020867));
#44817=CARTESIAN_POINT('',(0.15,-9.82814885840794,3.97082989020867));
#44818=CARTESIAN_POINT('Origin',(0.,-9.35924448430463,4.97639856553044));
#44819=CARTESIAN_POINT('',(0.15,-9.35924448430463,4.97639856553044));
#44820=CARTESIAN_POINT('',(0.,-9.35924448430463,4.97639856553044));
#44821=CARTESIAN_POINT('',(0.15,-9.35924448430463,4.97639856553044));
#44822=CARTESIAN_POINT('Origin',(0.,-8.78779826908344,5.92744477678992));
#44823=CARTESIAN_POINT('',(0.15,-8.78779826908344,5.92744477678992));
#44824=CARTESIAN_POINT('',(0.,-8.78779826908344,5.92744477678992));
#44825=CARTESIAN_POINT('',(0.15,-8.78779826908344,5.92744477678992));
#44826=CARTESIAN_POINT('Origin',(0.,-8.12007109706117,6.81354866267732));
#44827=CARTESIAN_POINT('',(0.15,-8.12007109706117,6.81354866267732));
#44828=CARTESIAN_POINT('',(0.,-8.12007109706117,6.81354866267732));
#44829=CARTESIAN_POINT('',(0.15,-8.12007109706117,6.81354866267732));
#44830=CARTESIAN_POINT('Origin',(0.,-7.36337872686537,7.6250018835897));
#44831=CARTESIAN_POINT('',(0.15,-7.36337872686537,7.6250018835897));
#44832=CARTESIAN_POINT('',(0.,-7.36337872686537,7.6250018835897));
#44833=CARTESIAN_POINT('',(0.15,-7.36337872686537,7.6250018835897));
#44834=CARTESIAN_POINT('Origin',(0.,-6.52601163845198,8.35291398823125));
#44835=CARTESIAN_POINT('',(0.15,-6.52601163845198,8.35291398823125));
#44836=CARTESIAN_POINT('',(0.,-6.52601163845198,8.35291398823125));
#44837=CARTESIAN_POINT('',(0.15,-6.52601163845198,8.35291398823125));
#44838=CARTESIAN_POINT('Origin',(0.,-4.43276262234474,5.6736774259684));
#44839=CARTESIAN_POINT('',(0.15,-4.43276262234474,5.6736774259684));
#44840=CARTESIAN_POINT('Origin',(0.15,-7.31106829964546,5.16875147505682));
#44841=CARTESIAN_POINT('Origin',(0.,-6.98612922918717,-1.74183764831761));
#44842=CARTESIAN_POINT('',(0.15,-6.98612922918717,-1.74183764831761));
#44843=CARTESIAN_POINT('',(0.,-6.98612922918717,-1.74183764831761));
#44844=CARTESIAN_POINT('',(0.15,-7.12993009493931,-1.00204632691247));
#44845=CARTESIAN_POINT('',(0.15,-6.98612922918717,-1.74183764831761));
#44846=CARTESIAN_POINT('',(0.,-7.12993009493931,-1.00204632691247));
#44847=CARTESIAN_POINT('Origin',(0.,-6.76578686965854,-2.46254503194481));
#44848=CARTESIAN_POINT('',(0.15,-6.76578686965854,-2.46254503194481));
#44849=CARTESIAN_POINT('',(0.,-6.76578686965854,-2.46254503194481));
#44850=CARTESIAN_POINT('',(0.15,-6.76578686965854,-2.46254503194481));
#44851=CARTESIAN_POINT('Origin',(0.,-6.471317133354,-3.15627225688136));
#44852=CARTESIAN_POINT('',(0.15,-6.471317133354,-3.15627225688136));
#44853=CARTESIAN_POINT('',(0.,-6.471317133354,-3.15627225688136));
#44854=CARTESIAN_POINT('',(0.15,-6.471317133354,-3.15627225688136));
#44855=CARTESIAN_POINT('Origin',(0.,-6.10594629232627,-3.81541870247908));
#44856=CARTESIAN_POINT('',(0.15,-6.10594629232627,-3.81541870247908));
#44857=CARTESIAN_POINT('',(0.,-6.10594629232627,-3.81541870247908));
#44858=CARTESIAN_POINT('',(0.15,-6.10594629232627,-3.81541870247908));
#44859=CARTESIAN_POINT('Origin',(0.,-5.6736774259684,-4.43276262234474));
#44860=CARTESIAN_POINT('',(0.15,-5.6736774259684,-4.43276262234474));
#44861=CARTESIAN_POINT('',(0.,-5.6736774259684,-4.43276262234474));
#44862=CARTESIAN_POINT('',(0.15,-5.6736774259684,-4.43276262234474));
#44863=CARTESIAN_POINT('Origin',(0.,-5.17924656243829,-5.00154026730478));
#44864=CARTESIAN_POINT('',(0.15,-5.17924656243829,-5.00154026730478));
#44865=CARTESIAN_POINT('',(0.,-5.17924656243829,-5.00154026730478));
#44866=CARTESIAN_POINT('',(0.15,-5.17924656243829,-5.00154026730478));
#44867=CARTESIAN_POINT('Origin',(0.,-7.6250018835897,-7.36337872686537));
#44868=CARTESIAN_POINT('',(0.15,-7.6250018835897,-7.36337872686537));
#44869=CARTESIAN_POINT('',(0.,-7.6250018835897,-7.36337872686537));
#44870=CARTESIAN_POINT('',(0.15,-7.6250018835897,-7.36337872686537));
#44871=CARTESIAN_POINT('Origin',(0.,-8.35291398823125,-6.52601163845198));
#44872=CARTESIAN_POINT('',(0.15,-8.35291398823125,-6.52601163845198));
#44873=CARTESIAN_POINT('',(0.,-8.35291398823125,-6.52601163845198));
#44874=CARTESIAN_POINT('',(0.15,-8.35291398823125,-6.52601163845198));
#44875=CARTESIAN_POINT('Origin',(0.,-8.98930981925811,-5.61714420087197));
#44876=CARTESIAN_POINT('',(0.15,-8.98930981925811,-5.61714420087197));
#44877=CARTESIAN_POINT('',(0.,-8.98930981925811,-5.61714420087197));
#44878=CARTESIAN_POINT('',(0.15,-8.98930981925811,-5.61714420087197));
#44879=CARTESIAN_POINT('Origin',(0.,-9.52721689077117,-4.64673415596422));
#44880=CARTESIAN_POINT('',(0.15,-9.52721689077117,-4.64673415596422));
#44881=CARTESIAN_POINT('',(0.,-9.52721689077117,-4.64673415596422));
#44882=CARTESIAN_POINT('',(0.15,-9.52721689077117,-4.64673415596422));
#44883=CARTESIAN_POINT('Origin',(0.,-9.96074178033063,-3.62541351925209));
#44884=CARTESIAN_POINT('',(0.15,-9.96074178033063,-3.62541351925209));
#44885=CARTESIAN_POINT('',(0.,-9.96074178033063,-3.62541351925209));
#44886=CARTESIAN_POINT('',(0.15,-9.96074178033063,-3.62541351925209));
#44887=CARTESIAN_POINT('Origin',(0.,-10.2851346985256,-2.56437209335648));
#44888=CARTESIAN_POINT('',(0.15,-10.2851346985256,-2.56437209335648));
#44889=CARTESIAN_POINT('',(0.,-10.2851346985256,-2.56437209335648));
#44890=CARTESIAN_POINT('',(0.15,-10.2851346985256,-2.56437209335648));
#44891=CARTESIAN_POINT('Origin',(0.,-10.4968415286606,-1.47523487017669));
#44892=CARTESIAN_POINT('',(0.15,-10.4968415286606,-1.47523487017669));
#44893=CARTESIAN_POINT('',(0.,-10.4968415286606,-1.47523487017669));
#44894=CARTESIAN_POINT('',(0.15,-10.4968415286606,-1.47523487017669));
#44895=CARTESIAN_POINT('Origin',(0.,-7.12993009493931,-1.00204632691247));
#44896=CARTESIAN_POINT('',(0.15,-7.12993009493931,-1.00204632691247));
#44897=CARTESIAN_POINT('Origin',(0.15,-7.83804404554947,-4.18271252688892));
#44898=CARTESIAN_POINT('Origin',(0.,5.00154026730478,-5.17924656243829));
#44899=CARTESIAN_POINT('',(0.15,5.00154026730478,-5.17924656243829));
#44900=CARTESIAN_POINT('',(0.,5.00154026730478,-5.17924656243829));
#44901=CARTESIAN_POINT('',(0.15,4.43276262234474,-5.6736774259684));
#44902=CARTESIAN_POINT('',(0.15,5.00154026730478,-5.17924656243829));
#44903=CARTESIAN_POINT('',(0.,4.43276262234474,-5.6736774259684));
#44904=CARTESIAN_POINT('Origin',(0.,5.51551999045664,-4.62807078974308));
#44905=CARTESIAN_POINT('',(0.15,5.51551999045664,-4.62807078974308));
#44906=CARTESIAN_POINT('',(0.,5.51551999045664,-4.62807078974308));
#44907=CARTESIAN_POINT('',(0.15,5.51551999045664,-4.62807078974308));
#44908=CARTESIAN_POINT('Origin',(0.,5.9690705223963,-4.02618890498938));
#44909=CARTESIAN_POINT('',(0.15,5.9690705223963,-4.02618890498938));
#44910=CARTESIAN_POINT('',(0.,5.9690705223963,-4.02618890498938));
#44911=CARTESIAN_POINT('',(0.15,5.9690705223963,-4.02618890498938));
#44912=CARTESIAN_POINT('Origin',(0.,6.35722266858427,-3.38019525205841));
#44913=CARTESIAN_POINT('',(0.15,6.35722266858427,-3.38019525205841));
#44914=CARTESIAN_POINT('',(0.,6.35722266858427,-3.38019525205841));
#44915=CARTESIAN_POINT('',(0.15,6.35722266858427,-3.38019525205841));
#44916=CARTESIAN_POINT('Origin',(0.,6.67572375288087,-2.69716747259456));
#44917=CARTESIAN_POINT('',(0.15,6.67572375288087,-2.69716747259456));
#44918=CARTESIAN_POINT('',(0.,6.67572375288087,-2.69716747259456));
#44919=CARTESIAN_POINT('',(0.15,6.67572375288087,-2.69716747259456));
#44920=CARTESIAN_POINT('Origin',(0.,6.9210842107559,-1.98458896188239));
#44921=CARTESIAN_POINT('',(0.15,6.9210842107559,-1.98458896188239));
#44922=CARTESIAN_POINT('',(0.,6.9210842107559,-1.98458896188239));
#44923=CARTESIAN_POINT('',(0.15,6.9210842107559,-1.98458896188239));
#44924=CARTESIAN_POINT('Origin',(0.,10.1893739769462,-2.92175597166019));
#44925=CARTESIAN_POINT('',(0.15,10.1893739769462,-2.92175597166019));
#44926=CARTESIAN_POINT('',(0.,10.1893739769462,-2.92175597166019));
#44927=CARTESIAN_POINT('',(0.15,10.1893739769462,-2.92175597166019));
#44928=CARTESIAN_POINT('Origin',(0.,9.82814885840795,-3.97082989020866));
#44929=CARTESIAN_POINT('',(0.15,9.82814885840795,-3.97082989020866));
#44930=CARTESIAN_POINT('',(0.,9.82814885840795,-3.97082989020866));
#44931=CARTESIAN_POINT('',(0.15,9.82814885840795,-3.97082989020866));
#44932=CARTESIAN_POINT('Origin',(0.,9.35924448430463,-4.97639856553044));
#44933=CARTESIAN_POINT('',(0.15,9.35924448430463,-4.97639856553044));
#44934=CARTESIAN_POINT('',(0.,9.35924448430463,-4.97639856553044));
#44935=CARTESIAN_POINT('',(0.15,9.35924448430463,-4.97639856553044));
#44936=CARTESIAN_POINT('Origin',(0.,8.78779826908344,-5.92744477678991));
#44937=CARTESIAN_POINT('',(0.15,8.78779826908344,-5.92744477678991));
#44938=CARTESIAN_POINT('',(0.,8.78779826908344,-5.92744477678991));
#44939=CARTESIAN_POINT('',(0.15,8.78779826908344,-5.92744477678991));
#44940=CARTESIAN_POINT('Origin',(0.,8.12007109706117,-6.81354866267731));
#44941=CARTESIAN_POINT('',(0.15,8.12007109706117,-6.81354866267731));
#44942=CARTESIAN_POINT('',(0.,8.12007109706117,-6.81354866267731));
#44943=CARTESIAN_POINT('',(0.15,8.12007109706117,-6.81354866267731));
#44944=CARTESIAN_POINT('Origin',(0.,7.36337872686537,-7.6250018835897));
#44945=CARTESIAN_POINT('',(0.15,7.36337872686537,-7.6250018835897));
#44946=CARTESIAN_POINT('',(0.,7.36337872686537,-7.6250018835897));
#44947=CARTESIAN_POINT('',(0.15,7.36337872686537,-7.6250018835897));
#44948=CARTESIAN_POINT('Origin',(0.,6.52601163845198,-8.35291398823125));
#44949=CARTESIAN_POINT('',(0.15,6.52601163845198,-8.35291398823125));
#44950=CARTESIAN_POINT('',(0.,6.52601163845198,-8.35291398823125));
#44951=CARTESIAN_POINT('',(0.15,6.52601163845198,-8.35291398823125));
#44952=CARTESIAN_POINT('Origin',(0.,4.43276262234474,-5.6736774259684));
#44953=CARTESIAN_POINT('',(0.15,4.43276262234474,-5.6736774259684));
#44954=CARTESIAN_POINT('Origin',(0.15,7.31106829964546,-5.16875147505682));
#44955=CARTESIAN_POINT('Origin',(0.,0.,0.));
#44956=CARTESIAN_POINT('',(0.,-7.16418377501202E-16,5.85));
#44957=CARTESIAN_POINT('',(0.,-7.16418377501202E-16,5.85));
#44958=CARTESIAN_POINT('Origin',(0.,5.,16.2480768092719));
#60346=UNCERTAINTY_MEASURE_WITH_UNIT(LENGTH_MEASURE(0.01),#60366,
'DISTANCE_ACCURACY_VALUE',
'Maximum model space distance between geometric entities at asserted c
onnectivities');
#60353=UNCERTAINTY_MEASURE_WITH_UNIT(LENGTH_MEASURE(0.01),#60366,
'DISTANCE_ACCURACY_VALUE',
'Maximum model space distance between geometric entities at asserted c
onnectivities');
#60358=(
GEOMETRIC_REPRESENTATION_CONTEXT(3)
GLOBAL_UNCERTAINTY_ASSIGNED_CONTEXT((#60346))
GLOBAL_UNIT_ASSIGNED_CONTEXT((#60366,#60368,#60369))
REPRESENTATION_CONTEXT('','3D')
);
#60365=(
GEOMETRIC_REPRESENTATION_CONTEXT(3)
GLOBAL_UNCERTAINTY_ASSIGNED_CONTEXT((#60353))
GLOBAL_UNIT_ASSIGNED_CONTEXT((#60366,#60368,#60369))
REPRESENTATION_CONTEXT('','3D')
);
#60366=(
LENGTH_UNIT()
NAMED_UNIT(*)
SI_UNIT(.MILLI.,.METRE.)
);
#60368=(
NAMED_UNIT(*)
PLANE_ANGLE_UNIT()
SI_UNIT($,.RADIAN.)
);
#60369=(
NAMED_UNIT(*)
SI_UNIT($,.STERADIAN.)
SOLID_ANGLE_UNIT()
);
#60374=SHAPE_DEFINITION_REPRESENTATION(#60385,#60410);
#60385=PRODUCT_DEFINITION_SHAPE('',$,#60422);
#60410=SHAPE_REPRESENTATION('',(#18938),#60358);
#60417=PRODUCT_DEFINITION_CONTEXT('part definition',#60452,'design');
#60422=PRODUCT_DEFINITION('2026-10-25-00-06-30-685','06_Thrust_Bearing',
#60433,#60417);
#60433=PRODUCT_DEFINITION_FORMATION('',$,#60458);
#60452=APPLICATION_CONTEXT(
'Core Data for Automotive Mechanical Design Process');
#60453=PRODUCT_CONTEXT('part definition',#60452,'mechanical');
#60458=PRODUCT('2026-10-25-00-06-30-685','06_Thrust_Bearing',$,(#60453));
#60521=COLOUR_RGB('Grey',0.48,0.52,0.57);
#60522=FILL_AREA_STYLE_COLOUR('',#60521);
#60523=FILL_AREA_STYLE('',(#60522));
#60524=SURFACE_STYLE_FILL_AREA(#60523);
#60525=SURFACE_SIDE_STYLE('',(#60524));
#60526=SURFACE_STYLE_USAGE(.BOTH.,#60525);
#60527=PRESENTATION_STYLE_ASSIGNMENT((#60526));
ENDSEC;
END-ISO-10303-21;
